ISO-10303-21;
HEADER;
FILE_DESCRIPTION (('STEP AP214'),
    '1' );
FILE_NAME ('Terminal Screw 3.step',
    '2026-10-05T22:38:29',
    ( '' ),
    ( '' ),
    'SwSTEP 2.0',
    'SolidWorks 2020',
    '' );
FILE_SCHEMA (( 'AUTOMOTIVE_DESIGN' ));
ENDSEC;

DATA;
#36=CARTESIAN_POINT ( 'NONE',  ( 10.55103166480599874, 2.999015536536000504, -7.570575893572789816 ) ) ;
#41=CARTESIAN_POINT ( 'NONE',  ( 9.125113844317997547, 4.288351516201100111, -6.395197822644999697 ) ) ;
#43=CARTESIAN_POINT ( 'NONE',  ( 11.67918044953561996, 5.011483761127000669, -8.027436060358800418 ) ) ;
#46=CARTESIAN_POINT ( 'NONE',  ( 8.568822372493999140, 3.671800173070400408, -8.573651380901999630 ) ) ;
#70=B_SPLINE_CURVE_WITH_KNOTS ( 'NONE', 3,
 ( #4155, #68818, #63577, #63225, #63916, #25495, #46825, #36328, #9749, #31097, #4497, #25838, #47166, #15351, #10099, #27912 ),
 .UNSPECIFIED., .F., .F.,
 ( 4, 2, 2, 2, 2, 2, 2, 4 ),
 ( 0.000000000000000000, 0.06249999999999925060, 0.1249999999999985012, 0.2499999999999987232, 0.3749999999999989453, 0.4999999999999991118, 0.7499999999999995559, 1.000000000000000000 ),
 .UNSPECIFIED. ) ;
#101=DIRECTION ( 'NONE',  ( 0.000000000000000000, 0.000000000000000000, -1.000000000000000000 ) ) ;
#124=CARTESIAN_POINT ( 'NONE',  ( 11.17901463001529905, 4.697110652903200290, -6.383488688482000128 ) ) ;
#125=CARTESIAN_POINT ( 'NONE',  ( 8.927455549952998837, 4.674761969675400586, -6.955569812538500152 ) ) ;
#136=DIRECTION ( 'NONE',  ( 0.7071067617951957152, 0.000000000000000000, -0.7071068005778986532 ) ) ;
#148=CARTESIAN_POINT ( 'NONE',  ( 10.87518447801629939, 4.865987311498500389, -7.480906371072489236 ) ) ;
#160=CARTESIAN_POINT ( 'NONE',  ( 10.94501463001509833, 4.472480213525599879, -6.743262887067199784 ) ) ;
#161=ORIENTED_EDGE ( 'NONE', *, *, #34361, .F. ) ;
#178=CARTESIAN_POINT ( 'NONE',  ( 11.32299956498189886, 2.792989229543000107, -7.174999999999999822 ) ) ;
#180=CARTESIAN_POINT ( 'NONE',  ( 9.051300837857860770, 5.190117543293265356, -7.723566111296684689 ) ) ;
#188=CARTESIAN_POINT ( 'NONE',  ( 11.59999999999999964, 4.695782097862117865, -6.595854147058993533 ) ) ;
#211=CARTESIAN_POINT ( 'NONE',  ( 10.47303166480599934, 2.862083839376000416, -7.580230465881790280 ) ) ;
#214=CARTESIAN_POINT ( 'NONE',  ( 9.577013376692997682, 3.227076647348800176, -7.107192877568799361 ) ) ;
#234=CARTESIAN_POINT ( 'NONE',  ( 9.383499245234510511, 2.750003956825025853, -7.336369100805423038 ) ) ;
#255=CARTESIAN_POINT ( 'NONE',  ( 10.94501463001509833, 4.472480213525599879, -6.743262887067199784 ) ) ;
#293=CARTESIAN_POINT ( 'NONE',  ( 11.14595257254739913, 3.168263696564200149, -7.741895249827200232 ) ) ;
#325=CARTESIAN_POINT ( 'NONE',  ( 10.45222191436347714, 4.437430566769827500, -6.743201413565676816 ) ) ;
#376=CONICAL_SURFACE ( 'NONE', #56224, 0.9999998338055000602, 0.7853981908209605178 ) ;
#377=CARTESIAN_POINT ( 'NONE',  ( 11.18687482311539938, 5.057677595549000316, -7.927326830586499007 ) ) ;
#382=CARTESIAN_POINT ( 'NONE',  ( 10.41690035061499842, 4.304339077956200299, -8.600505223349999895 ) ) ;
#384=CARTESIAN_POINT ( 'NONE',  ( 10.84226088462129844, 4.002427228022017225, -6.359261544073000039 ) ) ;
#450=ORIENTED_EDGE ( 'NONE', *, *, #10251, .T. ) ;
#467=ADVANCED_FACE ( 'NONE', ( #50232 ), #38152, .T. ) ;
#468=CARTESIAN_POINT ( 'NONE',  ( 11.63611496860034933, 5.171412538012999605, -6.899705789500199415 ) ) ;
#469=CARTESIAN_POINT ( 'NONE',  ( 10.19190035061499877, 4.267716286314199969, -8.468075389605498771 ) ) ;
#494=CARTESIAN_POINT ( 'NONE',  ( 11.14595257254739913, 3.168263696564200149, -7.741895249827200232 ) ) ;
#503=CARTESIAN_POINT ( 'NONE',  ( 11.04664311227086415, 4.444039568019538144, -8.706333095531743282 ) ) ;
#504=CARTESIAN_POINT ( 'NONE',  ( 10.56591429142999949, 4.019686495353769651, -6.466681092390999197 ) ) ;
#509=VERTEX_POINT ( 'NONE', #29617 ) ;
#513=ORIENTED_EDGE ( 'NONE', *, *, #37970, .T. ) ;
#527=ORIENTED_EDGE ( 'NONE', *, *, #38514, .F. ) ;
#540=CARTESIAN_POINT ( 'NONE',  ( 8.726787239609997471, 3.780467314030099946, -8.340498368324299250 ) ) ;
#563=CARTESIAN_POINT ( 'NONE',  ( 10.49764694612699856, 2.940513484064000149, -7.922821994243300914 ) ) ;
#567=CARTESIAN_POINT ( 'NONE',  ( 8.969113844317998741, 4.218953675027299788, -6.661091642253600398 ) ) ;
#571=ORIENTED_EDGE ( 'NONE', *, *, #6260, .F. ) ;
#605=AXIS2_PLACEMENT_3D ( 'NONE', #58152, #41390, #62024 ) ;
#629=VECTOR ( 'NONE', #51467, 1000.000000000000000 ) ;
#644=CARTESIAN_POINT ( 'NONE',  ( 11.49056651104150006, 4.085456792591960706, -6.638028001068500217 ) ) ;
#679=CARTESIAN_POINT ( 'NONE',  ( 9.446013540182333301, 3.000416447002273834, -8.268183399968640046 ) ) ;
#699=CARTESIAN_POINT ( 'NONE',  ( 9.140654977342494547, 5.049579698492543400, -6.802596805975135830 ) ) ;
#725=CARTESIAN_POINT ( 'NONE',  ( 11.06379841651039797, 3.598362324325699912, -8.567697191971999970 ) ) ;
#731=CARTESIAN_POINT ( 'NONE',  ( 10.74379975933729980, 5.078682052940000524, -7.128873141726999485 ) ) ;
#815=FACE_OUTER_BOUND ( 'NONE', #8987, .T. ) ;
#817=CARTESIAN_POINT ( 'NONE',  ( 11.14767835872009982, 3.125658946326500320, -6.948943352864199952 ) ) ;
#818=CARTESIAN_POINT ( 'NONE',  ( 9.001430433046998303, 3.145249924879699677, -6.972511033848699746 ) ) ;
#851=CARTESIAN_POINT ( 'NONE',  ( 10.44635971519499940, 4.459622816450200311, -6.735384833238199143 ) ) ;
#910=CARTESIAN_POINT ( 'NONE',  ( 10.56733863405299800, 4.788475529394700558, -8.505794571537999005 ) ) ;
#941=CYLINDRICAL_SURFACE ( 'NONE', #63297, 1.250000000000000222 ) ;
#950=CARTESIAN_POINT ( 'NONE',  ( 10.98656920625009903, 4.032067152264009913, -6.608450613814399688 ) ) ;
#960=EDGE_CURVE ( 'NONE', #28311, #4423, #4597, .T. ) ;
#1073=CARTESIAN_POINT ( 'NONE',  ( 10.45257053952200010, 3.605640676136899980, -6.577269499510100204 ) ) ;
#1080=CARTESIAN_POINT ( 'NONE',  ( 11.70379573085659786, 5.106255642043000087, -7.691418046581699919 ) ) ;
#1093=EDGE_CURVE ( 'NONE', #17729, #50078, #52151, .T. ) ;
#1141=CARTESIAN_POINT ( 'NONE',  ( 10.26693802597399952, 3.334935831489500124, -6.407263051216999017 ) ) ;
#1162=CARTESIAN_POINT ( 'NONE',  ( 10.72702344389999851, 2.995605560827999891, -6.890449684422599752 ) ) ;
#1163=CARTESIAN_POINT ( 'NONE',  ( 9.457355082327998375, 3.550486524676900402, -6.601790705997299114 ) ) ;
#1173=EDGE_CURVE ( 'NONE', #26310, #57892, #61331, .T. ) ;
#1181=B_SPLINE_CURVE_WITH_KNOTS ( 'NONE', 3,
 ( #36973, #31045, #4447, #15640 ),
 .UNSPECIFIED., .F., .F.,
 ( 4, 4 ),
 ( 0.000000000000000000, 1.000000000000000000 ),
 .UNSPECIFIED. ) ;
#1188=CARTESIAN_POINT ( 'NONE',  ( 11.02287616594229824, 3.738072157442200005, -6.674353346984900348 ) ) ;
#1224=CARTESIAN_POINT ( 'NONE',  ( 11.60000000000000320, 4.988477031107066750, -6.852161599766356304 ) ) ;
#1281=CARTESIAN_POINT ( 'NONE',  ( 11.22056920625029974, 4.047312782235129802, -6.184582852561999466 ) ) ;
#1293=CARTESIAN_POINT ( 'NONE',  ( 11.31900581613029821, 4.750686773407899466, -7.982035256002799173 ) ) ;
#1327=CARTESIAN_POINT ( 'NONE',  ( 10.33364828895399867, 4.760196147278000112, -7.915211961479200475 ) ) ;
#1378=CARTESIAN_POINT ( 'NONE',  ( 10.62309687351639020, 5.217465845835395299, -7.827184855449101697 ) ) ;
#1397=CARTESIAN_POINT ( 'NONE',  ( 9.114639751325487538, 5.184985712744430764, -7.959719964829115035 ) ) ;
#1413=CARTESIAN_POINT ( 'NONE',  ( 10.52641638348499953, 3.025038519517300184, -7.262511127784999410 ) ) ;
#1422=CARTESIAN_POINT ( 'NONE',  ( 10.39918582084299992, 3.253651555277099927, -6.637298362509499228 ) ) ;
#1436=CARTESIAN_POINT ( 'NONE',  ( 8.724507172011824352, 3.875764422069722492, -8.374507226493388856 ) ) ;
#1474=ORIENTED_EDGE ( 'NONE', *, *, #36051, .F. ) ;
#1478=CARTESIAN_POINT ( 'NONE',  ( 8.857090631127384484, 4.619515535681817830, -6.695274228472994693 ) ) ;
#1489=ADVANCED_FACE ( 'NONE', ( #54710 ), #63063, .F. ) ;
#1498=CARTESIAN_POINT ( 'NONE',  ( 9.896013540183126622, 3.000416447002273834, -8.268183399968641822 ) ) ;
#1506=CARTESIAN_POINT ( 'NONE',  ( 11.23078751119019891, 3.084247107206000038, -7.979095341142500075 ) ) ;
#1507=CARTESIAN_POINT ( 'NONE',  ( 9.482684229509999341, 3.291972602441000095, -6.787581931282099745 ) ) ;
#1529=CARTESIAN_POINT ( 'NONE',  ( 10.48133997687999930, 4.184599793140999502, -6.653701289769800020 ) ) ;
#1571=CARTESIAN_POINT ( 'NONE',  ( 8.712501735000000025, 3.641148095589300304, -8.276078370613198842 ) ) ;
#1597=CARTESIAN_POINT ( 'NONE',  ( 8.817138961223998095, 4.718363881473300658, -7.985449642667900250 ) ) ;
#1649=CARTESIAN_POINT ( 'NONE',  ( 10.83351354018309820, 2.750000000000000000, -7.336375382625529795 ) ) ;
#1677=CARTESIAN_POINT ( 'NONE',  ( 10.70287750876920008, 3.530799696887600092, -8.228113772635300194 ) ) ;
#1679=CARTESIAN_POINT ( 'NONE',  ( 9.277088727410998104, 2.862182806015999947, -7.595427884080399927 ) ) ;
#1689=ORIENTED_EDGE ( 'NONE', *, *, #47994, .F. ) ;
#1761=CARTESIAN_POINT ( 'NONE',  ( 11.15810538575740019, 5.242981041160000188, -7.202822423614300362 ) ) ;
#1770=CARTESIAN_POINT ( 'NONE',  ( 10.39503166480599994, 2.725152142215999884, -7.589885038193400213 ) ) ;
#1773=CARTESIAN_POINT ( 'NONE',  ( 10.39393020684999946, 2.750000000000000000, -7.500000000000000000 ) ) ;
#1790=CARTESIAN_POINT ( 'NONE',  ( 9.643930206848999376, 5.250000000000000000, -7.500000000000000000 ) ) ;
#1832=CARTESIAN_POINT ( 'NONE',  ( 10.16562143724499911, 4.849675135054999586, -6.543738240676099771 ) ) ;
#1853=CARTESIAN_POINT ( 'NONE',  ( 11.34287482311539996, 4.803125295093300551, -7.824481664695199790 ) ) ;
#1855=CARTESIAN_POINT ( 'NONE',  ( 10.35814141025499957, 4.483492689244800822, -8.361148840840000318 ) ) ;
#1856=CARTESIAN_POINT ( 'NONE',  ( 9.584000818238999742, 3.111278474435999808, -7.967991827203400490 ) ) ;
#1866=CARTESIAN_POINT ( 'NONE',  ( 9.480191603681626944, 4.150249255682260774, -6.638050216028796413 ) ) ;
#1882=CARTESIAN_POINT ( 'NONE',  ( 10.53057053952199951, 3.659587858614300249, -6.703496287302799672 ) ) ;
#1949=CARTESIAN_POINT ( 'NONE',  ( 8.724265421554999733, 3.837285628664199866, -8.341695632489900092 ) ) ;
#1965=EDGE_CURVE ( 'NONE', #26060, #24715, #65012, .T. ) ;
#2028=CARTESIAN_POINT ( 'NONE',  ( 11.11718313518939816, 3.377550038693600154, -8.287087605365499599 ) ) ;
#2030=CARTESIAN_POINT ( 'NONE',  ( 9.657025935145998830, 3.834207658792500251, -6.370288821165999593 ) ) ;
#2090=CARTESIAN_POINT ( 'NONE',  ( 9.181310023244000362, 4.573021367100345458, -6.377665258770703005 ) ) ;
#2114=CARTESIAN_POINT ( 'NONE',  ( 10.69456919669529960, 5.093991349577000172, -7.823222900359999343 ) ) ;
#2121=CARTESIAN_POINT ( 'NONE',  ( 10.34580110216399973, 2.909301855364999856, -6.833896451085399448 ) ) ;
#2181=CARTESIAN_POINT ( 'NONE',  ( 10.31759632033899976, 2.815618218644000414, -7.016653143730500197 ) ) ;
#2204=CARTESIAN_POINT ( 'NONE',  ( 10.40749413291699987, 4.788043169210699723, -7.140435631538599281 ) ) ;
#2206=CARTESIAN_POINT ( 'NONE',  ( 10.64391429142989765, 4.022379549362480766, -6.325326139450999641 ) ) ;
#2207=CARTESIAN_POINT ( 'NONE',  ( 9.455342523874998406, 2.871335344632000020, -7.327226901081999699 ) ) ;
#2215=CARTESIAN_POINT ( 'NONE',  ( 9.378875014952626543, 4.868116531169106587, -7.390885577342253931 ) ) ;
#2227=CARTESIAN_POINT ( 'NONE',  ( 11.78179573085659904, 4.973133828855400118, -7.668383662421899061 ) ) ;
#2287=CARTESIAN_POINT ( 'NONE',  ( 10.19810941423799910, 4.946022705791000007, -6.640722727400100389 ) ) ;
#2315=CARTESIAN_POINT ( 'NONE',  ( 10.68035971519489813, 4.678140486081599825, -6.371865185335000348 ) ) ;
#2318=ORIENTED_EDGE ( 'NONE', *, *, #22954, .F. ) ;
#2334=B_SPLINE_CURVE_WITH_KNOTS ( 'NONE', 3,
 ( #28072, #11982, #33320, #49046, #1498, #44164, #54985, #44850, #7082, #17932, #12681, #28776, #66157, #34363, #39596, #46905, #19993, #9146 ),
 .UNSPECIFIED., .F., .F.,
 ( 4, 2, 2, 2, 2, 2, 2, 2, 4 ),
 ( 0.000000000000000000, 0.1250000000000000000, 0.2500000000000000000, 0.3750000000000000000, 0.5000000000000000000, 0.6250000000000000000, 0.7500000000000000000, 0.8750000000000000000, 1.000000000000000000 ),
 .UNSPECIFIED. ) ;
#2366=CARTESIAN_POINT ( 'NONE',  ( 11.04749144726329924, 3.499163784537000055, -6.793273974143599681 ) ) ;
#2368=CARTESIAN_POINT ( 'NONE',  ( 9.503038493598998215, 4.726907342723099426, -6.806856425099999441 ) ) ;
#2443=EDGE_LOOP ( 'NONE', ( #13712, #30939, #31368, #19628 ) ) ;
#2449=CARTESIAN_POINT ( 'NONE',  ( 10.52226222744799955, 3.119510978356100139, -8.225278704382400718 ) ) ;
#2456=CARTESIAN_POINT ( 'NONE',  ( 10.15303300763299887, 4.787165141710600480, -8.325626572044798834 ) ) ;
#2517=CARTESIAN_POINT ( 'NONE',  ( 10.49490035061499782, 4.340961869598300105, -8.732935057095000175 ) ) ;
#2535=CARTESIAN_POINT ( 'NONE',  ( 11.66287348028854964, 3.238044298475899918, -7.911973420841600380 ) ) ;
#2537=CARTESIAN_POINT ( 'NONE',  ( 11.52677869730533011, 3.596497913043499750, -6.704332466833498927 ) ) ;
#2539=CARTESIAN_POINT ( 'NONE',  ( 9.581988259785999773, 3.850604015305000072, -8.631996151823999597 ) ) ;
#2548=CARTESIAN_POINT ( 'NONE',  ( 10.16407857760462718, 3.262163830883630489, -7.970244675898661590 ) ) ;
#2560=CARTESIAN_POINT ( 'NONE',  ( 10.55518582084299872, 3.433275964779900047, -6.844925608615599621 ) ) ;
#2633=DIRECTION ( 'NONE',  ( 0.000000000000000000, 1.000000000000000000, 0.000000000000000000 ) ) ;
#2649=SURFACE_STYLE_USAGE ( .BOTH. , #56826 ) ;
#2672=ORIENTED_EDGE ( 'NONE', *, *, #65261, .F. ) ;
#2677=MECHANICAL_DESIGN_GEOMETRIC_PRESENTATION_REPRESENTATION('',(#6002),#38399);
#2709=CARTESIAN_POINT ( 'NONE',  ( 10.48133997687999930, 4.184599793140999502, -6.653701289769800020 ) ) ;
#2712=CARTESIAN_POINT ( 'NONE',  ( 9.756329965421999262, 3.302375896175799852, -8.222608407156599242 ) ) ;
#2783=CARTESIAN_POINT ( 'NONE',  ( 11.13459739833729856, 3.176841881612200158, -7.825000000000000178 ) ) ;
#2791=CARTESIAN_POINT ( 'NONE',  ( 11.50271932425157040, 3.812601581225100400, -8.764198628556998827 ) ) ;
#2799=CARTESIAN_POINT ( 'NONE',  ( 11.50271932425157040, 3.812601581225100400, -8.764198628556998827 ) ) ;
#2859=CARTESIAN_POINT ( 'NONE',  ( 9.177784697135001224, 4.694174896253500151, -6.425520776924999566 ) ) ;
#2862=VERTEX_POINT ( 'NONE', #40446 ) ;
#2881=CARTESIAN_POINT ( 'NONE',  ( 11.53979707368350027, 3.569730287184500472, -6.748224392138099326 ) ) ;
#2883=CARTESIAN_POINT ( 'NONE',  ( 10.32169598648999909, 4.766524664146899681, -7.956401575444799867 ) ) ;
#2884=CARTESIAN_POINT ( 'NONE',  ( 9.860608878791998322, 3.741427262966100287, -6.387851364408000165 ) ) ;
#2888=ORIENTED_EDGE ( 'NONE', *, *, #40786, .T. ) ;
#2892=CARTESIAN_POINT ( 'NONE',  ( 9.657495633957626779, 3.225830943932614048, -7.907669647568630111 ) ) ;
#2967=CARTESIAN_POINT ( 'NONE',  ( 9.082867883171827472, 4.782673203840020371, -8.474986547786114599 ) ) ;
#2996=CARTESIAN_POINT ( 'NONE',  ( 11.43345123989529810, 4.540230239159599890, -8.543317325199000223 ) ) ;
#3046=CARTESIAN_POINT ( 'NONE',  ( 10.82179975933729921, 4.948878321068100661, -7.173532873542499466 ) ) ;
#3050=CARTESIAN_POINT ( 'NONE',  ( 9.300405316139999101, 3.786750623988900166, -8.481512610189300361 ) ) ;
#3134=PRODUCT ( 'Terminal Screw 3', 'Terminal Screw 3', '', ( #25347 ) ) ;
#3135=CARTESIAN_POINT ( 'NONE',  ( 10.27610941423800028, 4.844410192686099847, -6.733017893878099791 ) ) ;
#3144=CARTESIAN_POINT ( 'NONE',  ( 10.91195257254739914, 2.772832764353999835, -7.856899084262298771 ) ) ;
#3169=CARTESIAN_POINT ( 'NONE',  ( 11.41486084871699802, 2.792989229543000107, -7.825000000000000178 ) ) ;
#3191=CARTESIAN_POINT ( 'NONE',  ( 9.729346873516670158, 3.836375382625535124, -6.249999999999999112 ) ) ;
#3208=CARTESIAN_POINT ( 'NONE',  ( 9.025809814041000578, 4.782507962695600412, -8.511961036725999463 ) ) ;
#3212=AXIS2_PLACEMENT_3D ( 'NONE', #68224, #20342, #15102 ) ;
#3229=CARTESIAN_POINT ( 'NONE',  ( 11.24441369783139777, 3.956299011112040187, -8.365094684940499903 ) ) ;
#3232=CARTESIAN_POINT ( 'NONE',  ( 9.404684229509999938, 3.195116560491999991, -6.690125258578699885 ) ) ;
#3237=B_SPLINE_CURVE_WITH_KNOTS ( 'NONE', 3,
 ( #26257, #2783, #44067, #65368, #17488, #33571 ),
 .UNSPECIFIED., .F., .F.,
 ( 4, 1, 1, 4 ),
 ( 0.000000000000000000, 0.3333333333333000081, 0.6666666666667000474, 1.000000000000000000 ),
 .UNSPECIFIED. ) ;
#3241=CARTESIAN_POINT ( 'NONE',  ( 9.100254395947628083, 3.149024541069663563, -7.296596368717002790 ) ) ;
#3310=CARTESIAN_POINT ( 'NONE',  ( 9.065735834902588053, 4.411345979885467727, -8.662764376609992212 ) ) ;
#3323=DIRECTION ( 'NONE',  ( 0.7071067388045961799, 0.7071068235684964121, -1.176037761303994353E-10 ) ) ;
#3339=CARTESIAN_POINT ( 'NONE',  ( 10.81524174883999834, 3.971581146373189597, -8.533115712456000423 ) ) ;
#3384=FACE_OUTER_BOUND ( 'NONE', #65595, .T. ) ;
#3387=CARTESIAN_POINT ( 'NONE',  ( 10.32949413291699869, 4.912929163218899831, -7.083453279150199400 ) ) ;
#3389=CARTESIAN_POINT ( 'NONE',  ( 10.00962143724499853, 4.667147537636399335, -6.749162825004299648 ) ) ;
#3413=VERTEX_POINT ( 'NONE', #38212 ) ;
#3428=CARTESIAN_POINT ( 'NONE',  ( 11.84388784977539899, 2.744254309011999737, -7.428242901739219306 ) ) ;
#3433=ORIENTED_EDGE ( 'NONE', *, *, #13109, .T. ) ;
#3472=CARTESIAN_POINT ( 'NONE',  ( 10.76426088462129904, 4.002719309691810778, -6.221990224628999755 ) ) ;
#3522=CARTESIAN_POINT ( 'NONE',  ( 9.833513540183332680, 2.750000000000000000, -7.336375382625529795 ) ) ;
#3540=CARTESIAN_POINT ( 'NONE',  ( 9.684367640780997988, 4.603017491986999943, -6.371835875489000323 ) ) ;
#3560=CARTESIAN_POINT ( 'NONE',  ( 11.56025819896753859, 3.013900664291200293, -7.685900384398899554 ) ) ;
#3562=CARTESIAN_POINT ( 'NONE',  ( 10.28014141025500017, 4.417352327511700594, -8.243346240911998635 ) ) ;
#3563=CARTESIAN_POINT ( 'NONE',  ( 9.784621437244998887, 4.758411336345700349, -6.646450532840099790 ) ) ;
#3664=PRESENTATION_STYLE_ASSIGNMENT (( #2649 ) ) ;
#3671=CARTESIAN_POINT ( 'NONE',  ( 11.26723293495529887, 2.826061044294000180, -7.452807962566580180 ) ) ;
#3674=ORIENTED_EDGE ( 'NONE', *, *, #7441, .T. ) ;
#3724=CARTESIAN_POINT ( 'NONE',  ( 10.79718447801629999, 5.003225587801999552, -7.477880487566260115 ) ) ;
#3728=CARTESIAN_POINT ( 'NONE',  ( 9.021784697134998865, 4.545051930576500254, -6.656340890368899643 ) ) ;
#3749=FACE_OUTER_BOUND ( 'NONE', #51580, .T. ) ;
#3756=ORIENTED_EDGE ( 'NONE', *, *, #27217, .T. ) ;
#3765=CARTESIAN_POINT ( 'NONE',  ( 11.52166954483529793, 4.562096242626500597, -6.632714178206799538 ) ) ;
#3815=CIRCLE ( 'NONE', #47352, 0.7499999936418002555 ) ;
#3900=CARTESIAN_POINT ( 'NONE',  ( 11.53564291764652872, 3.004110626587600308, -7.376893506359599506 ) ) ;
#3902=CARTESIAN_POINT ( 'NONE',  ( 10.52946886766499901, 3.569835351907400423, -6.718432993015899690 ) ) ;
#3903=CARTESIAN_POINT ( 'NONE',  ( 8.972076168957999087, 3.350848599899200142, -8.602264418015000302 ) ) ;
#3912=CARTESIAN_POINT ( 'NONE',  ( 8.998937807218627682, 3.944921334759000420, -6.626788336335921237 ) ) ;
#3985=CARTESIAN_POINT ( 'NONE',  ( 9.696013540182335078, 4.999583552997727054, -6.731816600031361730 ) ) ;
#4014=CARTESIAN_POINT ( 'NONE',  ( 11.23078751119019891, 3.084247107206000038, -7.979095341142500075 ) ) ;
#4067=CARTESIAN_POINT ( 'NONE',  ( 11.38379707368349969, 3.433355370490100533, -6.509947486183500054 ) ) ;
#4069=CARTESIAN_POINT ( 'NONE',  ( 10.26090035061499961, 4.231093494672100164, -8.335645555860798694 ) ) ;
#4082=ORIENTED_EDGE ( 'NONE', *, *, #11426, .T. ) ;
#4109=CARTESIAN_POINT ( 'NONE',  ( 10.60235971519489873, 4.605301262871499546, -6.493038401303000029 ) ) ;
#4153=CARTESIAN_POINT ( 'NONE',  ( 10.81349144726329925, 3.261052100888700345, -6.457276458983999490 ) ) ;
#4155=CARTESIAN_POINT ( 'NONE',  ( 11.59999999999999964, 3.116215992411100366, -7.825000000000000178 ) ) ;
#4185=CARTESIAN_POINT ( 'NONE',  ( 10.52606775832647656, 3.656473597603909553, -6.696209471835564919 ) ) ;
#4201=CARTESIAN_POINT ( 'NONE',  ( 11.18220574173929904, 5.136173005413447790, -6.911917091190550089 ) ) ;
#4245=CARTESIAN_POINT ( 'NONE',  ( 11.43718179236249988, 3.790319673775199849, -6.518682001772900136 ) ) ;
#4250=CARTESIAN_POINT ( 'NONE',  ( 8.693455549952998851, 4.995562869655000071, -6.696732323226999739 ) ) ;
#4260=CARTESIAN_POINT ( 'NONE',  ( 8.751496707488000126, 4.081676005979390176, -8.356402621895700378 ) ) ;
#4329=CARTESIAN_POINT ( 'NONE',  ( 10.76346886766499900, 3.365322927604099679, -6.346853961441000003 ) ) ;
#4330=CARTESIAN_POINT ( 'NONE',  ( 9.940621437244999470, 4.575883738927100097, -6.851875117168399143 ) ) ;
#4359=SHAPE_DEFINITION_REPRESENTATION ( #39978, #55423 ) ;
#4363=CARTESIAN_POINT ( 'NONE',  ( 11.60477869730532774, 3.532552483170099844, -6.578238193496799724 ) ) ;
#4415=CARTESIAN_POINT ( 'NONE',  ( 11.45348876160960039, 3.114179898019400206, -8.421216112044099589 ) ) ;
#4418=CARTESIAN_POINT ( 'NONE',  ( 8.844480666858999030, 4.334888990546500231, -8.446938520915798776 ) ) ;
#4423=VERTEX_POINT ( 'NONE', #21118 ) ;
#4429=EDGE_CURVE ( 'NONE', #44304, #5638, #42444, .T. ) ;
#4447=CARTESIAN_POINT ( 'NONE',  ( 11.00009108335970609, 5.118893581675404647, -7.597657431955929574 ) ) ;
#4449=ORIENTED_EDGE ( 'NONE', *, *, #19883, .F. ) ;
#4452=CARTESIAN_POINT ( 'NONE',  ( 10.81013259637009938, 2.968328969579000276, -8.062151801142800167 ) ) ;
#4472=CARTESIAN_POINT ( 'NONE',  ( 11.41544519387737289, 4.732426395176744016, -7.017892448335746103 ) ) ;
#4494=CARTESIAN_POINT ( 'NONE',  ( 10.27195525820100031, 3.879327850572200198, -6.227697122196000024 ) ) ;
#4497=CARTESIAN_POINT ( 'NONE',  ( 11.59999999999999964, 3.801977891258315978, -8.571335789050444021 ) ) ;
#4505=CARTESIAN_POINT ( 'NONE',  ( 10.20851354018233437, 4.163624617374472869, -6.250000000000001776 ) ) ;
#4512=EDGE_CURVE ( 'NONE', #22792, #3413, #17600, .T. ) ;
#4588=CARTESIAN_POINT ( 'NONE',  ( 10.42795525820099911, 3.905250696375530239, -6.501013802764199490 ) ) ;
#4592=CARTESIAN_POINT ( 'NONE',  ( 9.048063610504998522, 4.524705472883399970, -8.666648427848999248 ) ) ;
#4597=B_SPLINE_CURVE_WITH_KNOTS ( 'NONE', 3,
 ( #48767, #22530, #180, #33034, #21497, #37578, #22190, #42831, #37926, #49106 ),
 .UNSPECIFIED., .F., .F.,
 ( 4, 2, 2, 2, 4 ),
 ( 0.000000000000000000, 0.2500000000000000000, 0.5000000000000000000, 0.7500000000000000000, 1.000000000000000000 ),
 .UNSPECIFIED. ) ;
#4669=CARTESIAN_POINT ( 'NONE',  ( 8.952784697134999803, 4.470490447737899942, -6.771750947090999340 ) ) ;
#4674=CARTESIAN_POINT ( 'NONE',  ( 9.654346873515669003, 5.250000000000002665, -7.336375382625537789 ) ) ;
#4688=CARTESIAN_POINT ( 'NONE',  ( 8.748821772879614045, 4.302364887094737966, -8.374063393888503626 ) ) ;
#4702=CARTESIAN_POINT ( 'NONE',  ( 10.48280513895999988, 4.903310631086600146, -6.997844089834400094 ) ) ;
#4758=CARTESIAN_POINT ( 'NONE',  ( 10.69456919669529960, 5.093991349577000172, -7.823222900359999343 ) ) ;
#4760=CARTESIAN_POINT ( 'NONE',  ( 9.374380199233998567, 4.860242402105300563, -7.391875284387199763 ) ) ;
#4774=EDGE_CURVE ( 'NONE', #57892, #35475, #16465, .T. ) ;
#4778=CARTESIAN_POINT ( 'NONE',  ( 10.10478570706233370, 5.131706358131709500, -8.113400509224881318 ) ) ;
#4798=CARTESIAN_POINT ( 'NONE',  ( 11.14256920625030034, 4.042230905578960254, -6.325872106312999676 ) ) ;
#4811=ORIENTED_EDGE ( 'NONE', *, *, #11700, .F. ) ;
#4842=CARTESIAN_POINT ( 'NONE',  ( 11.76133460557259980, 4.139849081322200419, -8.354833838171700222 ) ) ;
#4843=CARTESIAN_POINT ( 'NONE',  ( 10.66579975933730040, 5.208485784810999775, -7.084213409908699965 ) ) ;
#4936=CARTESIAN_POINT ( 'NONE',  ( 11.36333594839950045, 4.659759757475400832, -6.743912759487099784 ) ) ;
#4941=CARTESIAN_POINT ( 'NONE',  ( 9.681292290062998518, 5.106256438265999620, -6.857675253263499471 ) ) ;
#4951=EDGE_CURVE ( 'NONE', #42349, #26060, #49594, .T. ) ;
#4995=CARTESIAN_POINT ( 'NONE',  ( 10.68559687351635112, 5.092232985442825210, -6.870476274536379435 ) ) ;
#5001=CARTESIAN_POINT ( 'NONE',  ( 8.849999778957998942, 4.000000000000000000, -7.500000000000000000 ) ) ;
#5020=CARTESIAN_POINT ( 'NONE',  ( 10.88813259637009878, 2.844182332072999753, -8.129798612793599943 ) ) ;
#5021=CARTESIAN_POINT ( 'NONE',  ( 9.003442991499998271, 3.945420918055940085, -6.634708680083400090 ) ) ;
#5057=CARTESIAN_POINT ( 'NONE',  ( 11.52677869730533011, 3.596497913043499750, -6.704332466833498927 ) ) ;
#5109=CARTESIAN_POINT ( 'NONE',  ( 10.59610807141099897, 4.052703327804870526, -8.639522915742999132 ) ) ;
#5112=CARTESIAN_POINT ( 'NONE',  ( 8.945797255587999430, 5.003512473869000665, -7.457514444071220439 ) ) ;
#5151=CARTESIAN_POINT ( 'NONE',  ( 10.64391429142989765, 4.022379549362480766, -6.325326139450999641 ) ) ;
#5184=CARTESIAN_POINT ( 'NONE',  ( 8.797364180957998769, 3.929432544163579788, -8.475895758763700272 ) ) ;
#5192=CARTESIAN_POINT ( 'NONE',  ( 11.78594988689359901, 4.393436444036099786, -8.271690446953899212 ) ) ;
#5209=CARTESIAN_POINT ( 'NONE',  ( 11.14975833414749928, 3.203462856645999945, -7.825000000000000178 ) ) ;
#5250=STYLED_ITEM ( 'NONE', ( #43093 ), #64411 ) ;
#5280=CARTESIAN_POINT ( 'NONE',  ( 9.403734463322997783, 4.118936914955599882, -8.635600483553998785 ) ) ;
#5282=CARTESIAN_POINT ( 'NONE',  ( 11.21149010443640037, 5.137564434800999891, -7.585072163144589652 ) ) ;
#5286=CARTESIAN_POINT ( 'NONE',  ( 9.731950584426998674, 4.507735863714500191, -6.325866838823999139 ) ) ;
#5292=EDGE_CURVE ( 'NONE', #12138, #42349, #3815, .T. ) ;
#5337=CARTESIAN_POINT ( 'NONE',  ( 10.65434687351636178, 5.250000000000002665, -7.336375382625537789 ) ) ;
#5344=B_SPLINE_CURVE_WITH_KNOTS ( 'NONE', 3,
 ( #60380, #39751, #34519, #40424, #61415, #24697, #12485, #18428, #34852, #56167 ),
 .UNSPECIFIED., .F., .F.,
 ( 4, 2, 2, 2, 4 ),
 ( 0.000000000000000000, 0.2500000000000000000, 0.5000000000000000000, 0.7500000000000000000, 1.000000000000000000 ),
 .UNSPECIFIED. ) ;
#5369=CARTESIAN_POINT ( 'NONE',  ( 10.97124174884019965, 3.963805917081910213, -8.815770025351000072 ) ) ;
#5370=CARTESIAN_POINT ( 'NONE',  ( 10.11792546752099931, 3.135062625344399834, -7.440072690703440017 ) ) ;
#5392=CARTESIAN_POINT ( 'NONE',  ( 11.26902897915239876, 4.221721321201099997, -8.337339982364900592 ) ) ;
#5406=CARTESIAN_POINT ( 'NONE',  ( 11.15278751119019773, 3.209519379020799867, -7.913556523549700294 ) ) ;
#5424=ORIENTED_EDGE ( 'NONE', *, *, #960, .T. ) ;
#5460=CARTESIAN_POINT ( 'NONE',  ( 10.91610672858429965, 3.088399709291500095, -6.814233985789400094 ) ) ;
#5462=CARTESIAN_POINT ( 'NONE',  ( 9.627671671056999614, 3.144964309357700216, -7.643603315539799326 ) ) ;
#5499=CARTESIAN_POINT ( 'NONE',  ( 11.11123293495519881, 3.108594079907299967, -7.464165716332529676 ) ) ;
#5510=CARTESIAN_POINT ( 'NONE',  ( 10.67726354018259904, 4.629523725463628558, -6.407767014557180119 ) ) ;
#5528=CARTESIAN_POINT ( 'NONE',  ( 8.741501215035997419, 3.771222299067000350, -8.375893644236599656 ) ) ;
#5536=CARTESIAN_POINT ( 'NONE',  ( 11.46595122972049907, 4.343798595649099425, -6.704952129760900270 ) ) ;
#5537=EDGE_CURVE ( 'NONE', #37649, #17729, #61555, .T. ) ;
#5563=CARTESIAN_POINT ( 'NONE',  ( 10.59991360228957191, 3.150711065775904984, -7.293123446196289272 ) ) ;
#5614=CARTESIAN_POINT ( 'NONE',  ( 11.35918179236250047, 3.761636028845500412, -6.384440618559000136 ) ) ;
#5621=CARTESIAN_POINT ( 'NONE',  ( 9.023797255587998833, 5.140789995332999851, -7.451702546394010085 ) ) ;
#5623=CARTESIAN_POINT ( 'NONE',  ( 11.45764291764649911, 2.867875922590999771, -7.360052904210999891 ) ) ;
#5638=VERTEX_POINT ( 'NONE', #7129 ) ;
#5679=FILL_AREA_STYLE ('',( #53585 ) ) ;
#5685=CARTESIAN_POINT ( 'NONE',  ( 10.39393020684999946, 2.750000000000000000, -7.500000000000000000 ) ) ;
#5700=EDGE_LOOP ( 'NONE', ( #21842, #2888, #35871, #30193 ) ) ;
#5708=CARTESIAN_POINT ( 'NONE',  ( 9.889963142879999225, 4.848366390061300102, -7.321163726496699553 ) ) ;
#5729=CARTESIAN_POINT ( 'NONE',  ( 11.24441369783139777, 3.956299011112040187, -8.365094684940499903 ) ) ;
#5740=CARTESIAN_POINT ( 'NONE',  ( 10.48791429142999831, 4.016993441347180394, -6.608036045330599961 ) ) ;
#5759=ORIENTED_EDGE ( 'NONE', *, *, #54309, .T. ) ;
#5782=DIRECTION ( 'NONE',  ( -1.000000000000000000, 0.000000000000000000, 0.000000000000000000 ) ) ;
#5784=ORIENTED_EDGE ( 'NONE', *, *, #9101, .F. ) ;
#5790=B_SPLINE_CURVE_WITH_KNOTS ( 'NONE', 3,
 ( #65452, #23500, #28064, #18265 ),
 .UNSPECIFIED., .F., .F.,
 ( 4, 4 ),
 ( 0.000000000000000000, 1.000000000000000000 ),
 .UNSPECIFIED. ) ;
#5793=CARTESIAN_POINT ( 'NONE',  ( 10.20226357027499908, 5.120085139777000194, -7.716099591766099053 ) ) ;
#5837=CARTESIAN_POINT ( 'NONE',  ( 11.02812378248509795, 3.583106837161099900, -6.711274001288999536 ) ) ;
#5858=EDGE_LOOP ( 'NONE', ( #30264, #4082, #21481, #58613 ) ) ;
#5959=CARTESIAN_POINT ( 'NONE',  ( 11.13764426047339917, 4.613828180779599997, -8.461511872390000022 ) ) ;
#5966=CARTESIAN_POINT ( 'NONE',  ( 10.25149413291699929, 5.037815157227999663, -7.026470926762800495 ) ) ;
#5969=CARTESIAN_POINT ( 'NONE',  ( 8.490822372493999737, 3.632306086542600010, -8.702849744394999476 ) ) ;
#6002=STYLED_ITEM ( 'NONE', ( #3664 ), #31079 ) ;
#6049=CARTESIAN_POINT ( 'NONE',  ( 11.31389666366019853, 3.954123449088899900, -8.532487796751999198 ) ) ;
#6050=CARTESIAN_POINT ( 'NONE',  ( 9.026759580228999269, 3.023107159668900312, -7.266499081715599218 ) ) ;
#6074=CARTESIAN_POINT ( 'NONE',  ( 11.12133729122639991, 3.134101783108900197, -7.477221318588949117 ) ) ;
#6111=CARTESIAN_POINT ( 'NONE',  ( 11.59999999999999964, 3.205140046301732326, -7.075514291626551433 ) ) ;
#6137=CARTESIAN_POINT ( 'NONE',  ( 10.64118447801629941, 5.277702140407999565, -7.471828720557429193 ) ) ;
#6175=CARTESIAN_POINT ( 'NONE',  ( 10.61257802013489737, 3.108115747127599970, -7.479237407015119743 ) ) ;
#6260=EDGE_CURVE ( 'NONE', #7747, #43855, #7187, .T. ) ;
#6275=CARTESIAN_POINT ( 'NONE',  ( 11.59999999999999964, 4.000000000000000000, -7.500000000000000000 ) ) ;
#6299=CARTESIAN_POINT ( 'NONE',  ( 11.03918313518939875, 3.292400735470800033, -8.394758848575399668 ) ) ;
#6306=CARTESIAN_POINT ( 'NONE',  ( 10.62072335273219892, 4.397090433355999473, -8.569396700949999612 ) ) ;
#6310=CARTESIAN_POINT ( 'NONE',  ( 8.566809814040999171, 4.782507962695600412, -8.511961036725999463 ) ) ;
#6369=CARTESIAN_POINT ( 'NONE',  ( 10.38351354018329253, 2.750000000000000000, -7.336375382625530683 ) ) ;
#6386=CARTESIAN_POINT ( 'NONE',  ( 11.57299956498156845, 5.207010770456999893, -7.825000000000000178 ) ) ;
#6389=CARTESIAN_POINT ( 'NONE',  ( 9.099999931440999390, 5.250000000000000000, -7.500000000000000000 ) ) ;
#6391=CARTESIAN_POINT ( 'NONE',  ( 11.78594988689359901, 4.393436444036099786, -8.271690446953899212 ) ) ;
#6393=CARTESIAN_POINT ( 'NONE',  ( 11.26723293495529887, 2.826061044294000180, -7.452807962566580180 ) ) ;
#6395=CARTESIAN_POINT ( 'NONE',  ( 9.887950584426999256, 4.398663815465100768, -6.578094656394299911 ) ) ;
#6416=CARTESIAN_POINT ( 'NONE',  ( 10.92441504065829960, 4.694414232677499577, -6.982228367137699898 ) ) ;
#6444=ORIENTED_EDGE ( 'NONE', *, *, #4951, .F. ) ;
#6456=CARTESIAN_POINT ( 'NONE',  ( 11.59999999999999787, 4.363617849674654714, -6.469788275435901959 ) ) ;
#6463=CARTESIAN_POINT ( 'NONE',  ( 8.705449068729999240, 3.636021264089499994, -8.287166017043100297 ) ) ;
#6474=ORIENTED_EDGE ( 'NONE', *, *, #60714, .F. ) ;
#6485=CARTESIAN_POINT ( 'NONE',  ( 10.12426357027499790, 5.254871132332000094, -7.742104041724699570 ) ) ;
#6516=CARTESIAN_POINT ( 'NONE',  ( 11.46989666366029859, 3.941571897678119996, -8.814970315645998866 ) ) ;
#6517=ORIENTED_EDGE ( 'NONE', *, *, #42251, .T. ) ;
#6549=VERTEX_POINT ( 'NONE', #58994 ) ;
#6566=DIRECTION ( 'NONE',  ( -0.5000000000000150990, -0.08222066253632250021, 0.8621135439442261239 ) ) ;
#6568=CARTESIAN_POINT ( 'NONE',  ( 10.94903032197929882, 4.503839166471300004, -6.795411691360399686 ) ) ;
#6582=ORIENTED_EDGE ( 'NONE', *, *, #62650, .F. ) ;
#6610=B_SPLINE_SURFACE_WITH_KNOTS ( 'NONE', 3, 3, ( 
 ( #43840, #43496, #21134, #16905, #10634, #53291, #48387, #16223, #65141, #10982, #53634, #27766, #42802, #32321, #27411, #32659, #12017, #59909, #64444, #38235, #38585, #64794, #59564, #53969, #63768, #5392, #5729, #21466, #22497, #49075, #494, #6074, #27070, #26730, #11661, #1188, #21809, #16569, #48046, #6416, #17262, #148, #69020, #64108, #43143, #37895, #33353, #59216, #48737, #50120, #44881, #23889, #65492, #18306, #2560, #1882, #55363, #1529, #13066, #50459, #60263, #49417, #12368, #23198, #65841, #34396, #28811 ),
 ( #2227, #12716, #44548, #33698, #23542, #55714, #38945, #45224, #66186, #39630, #55018, #60952, #66530, #7810, #29151, #18649, #39983, #13416, #61296, #17965, #60605, #34048, #49771, #34735, #54668, #6765, #28104, #39284, #22847, #7119, #7458, #44198, #28457, #17619, #59793, #54899, #59104, #7000, #11544, #27645, #27994, #63993, #11210, #43029, #65023, #17139, #47936, #54198, #11897, #32546, #64331, #36, #1413, #38120, #49301, #1073, #33235, #16792, #48964, #27298, #22035, #21356, #12253, #22729, #44079, #54555, #37436 ),
 ( #42685, #16451, #22386, #26957, #58759, #38472, #10863, #16111, #33581, #6651, #37780, #53524, #65377, #17498, #32209, #5614, #38821, #60147, #43725, #48271, #53859, #48622, #377, #21693, #5959, #59447, #43382, #725, #6299, #32888, #64682, #29039, #39167, #19211, #18535, #40208, #50349, #39512, #66416, #61524, #24117, #23774, #2114, #44770, #23431, #39864, #66070, #8041, #18190, #2449, #34277, #61861, #55939, #45107, #55597, #50003, #29384, #34965, #7345, #3135, #50695, #45451, #60836, #34626, #45790, #66765, #18880 ),
 ( #12949, #7698, #28333, #56624, #61184, #28690, #2791, #13304, #29730, #33927, #13639, #56282, #8388, #51035, #67103, #24465, #40537, #13982, #35307, #49653, #1761, #23080, #44427, #65725, #17849, #60489, #12599, #55248, #41231, #47510, #30742, #25146, #41914, #46134, #4153, #8729, #3472, #52050, #25493, #36326, #4843, #26184, #15000, #51374, #24809, #57641, #68816, #31095, #63222, #47164, #15688, #68465, #14326, #67439, #30071, #19562, #4494, #40884, #36677, #20938, #42271, #25834, #62205, #20588, #35650, #56962, #46822 ) ),
 .UNSPECIFIED., .F., .F., .F.,
 ( 4, 4 ),
 ( 4, 1, 1, 1, 1, 1, 1, 1, 1, 1, 1, 1, 1, 1, 1, 1, 1, 1, 1, 1, 1, 1, 1, 1, 1, 1, 1, 1, 1, 1, 1, 1, 1, 1, 1, 1, 1, 1, 1, 1, 1, 1, 1, 1, 1, 1, 1, 1, 1, 1, 1, 1, 1, 1, 1, 1, 1, 1, 1, 1, 1, 1, 1, 1, 4 ),
 ( -0.02000000000000000042, 1.020000000000000018 ),
 ( 0.008747244164287000176, 0.02453926110774999961, 0.04033127805120999970, 0.05612329499467000327, 0.07191531193812999989, 0.08770732888158999652, 0.1034993458251000087, 0.1192913627684999978, 0.1350833797120000179, 0.1508753966553999792, 0.1666674135988999994, 0.1824594305423999918, 0.1982514474858000086, 0.2140434644293000011, 0.2298354813727000179, 0.2456274983162000103, 0.2614195152596999749, 0.2772115322030999640, 0.2930035491465999842, 0.3087955660900000288, 0.3245875830334999934, 0.3403795999769999581, 0.3561716169204000026, 0.3719636338639000228, 0.3877556508073999875, 0.4035476677507999765, 0.4193396846942999967, 0.4351317016376999858, 0.4509237185811999504, 0.4667157355247000261, 0.4825077524681000152, 0.4982997694115999798, 0.5140917863550000799, 0.5298838032985000446, 0.5456758202420000092, 0.5614678371854000538, 0.5772598541289000185, 0.5930518710723000630, 0.6088438880158000277, 0.6246359049592999924, 0.6404279219027000369, 0.6562199388462000016, 0.6720119557896999662, 0.6878039727331000108, 0.7035959896765999755, 0.7193880066200000201, 0.7351800235634999847, 0.7509720405069999494, 0.7667640574504001050, 0.7825560743939000696, 0.7983480913373000032, 0.8141401082808000789, 0.8299321252243000435, 0.8457241421676999771, 0.8615161591112000528, 0.8773081760545999863, 0.8931001929981000620, 0.9088922099416000266, 0.9246842268849999602, 0.9404762438285000359, 0.9562682607720000005, 0.9720602777153999341, 0.9878522946589000098, 1.003644311601999961, 1.019436328545999970 ),
 .UNSPECIFIED. ) ;
#6651=CARTESIAN_POINT ( 'NONE',  ( 11.50687348028854906, 2.996540789803000315, -8.042549288197099244 ) ) ;
#6660=CARTESIAN_POINT ( 'NONE',  ( 10.91610672858429965, 3.088399709291500095, -6.814233985789400094 ) ) ;
#6741=CARTESIAN_POINT ( 'NONE',  ( 10.69057802013490033, 2.966773425016000054, -7.475947032624040034 ) ) ;
#6742=CARTESIAN_POINT ( 'NONE',  ( 9.761304848515999666, 4.913464051101100516, -7.917643062525700159 ) ) ;
#6751=CARTESIAN_POINT ( 'NONE',  ( 10.11342028323962694, 3.127145521393861038, -7.439524153027672781 ) ) ;
#6765=CARTESIAN_POINT ( 'NONE',  ( 11.19102897915239936, 4.256858847510399890, -8.470038342183499935 ) ) ;
#6775=CARTESIAN_POINT ( 'NONE',  ( 11.49200216175158396, 3.580169417146517485, -8.702070774814039567 ) ) ;
#6795=CARTESIAN_POINT ( 'NONE',  ( 11.25361999289386539, 3.455907502640804374, -6.342116603374310380 ) ) ;
#6809=CARTESIAN_POINT ( 'NONE',  ( 8.691343736187999269, 3.625767601089900261, -8.309341309902798400 ) ) ;
#6850=ORIENTED_EDGE ( 'NONE', *, *, #67342, .T. ) ;
#6874=CARTESIAN_POINT ( 'NONE',  ( 10.37199293566600034, 4.633387186021100668, -8.276990458557699881 ) ) ;
#6875=CARTESIAN_POINT ( 'NONE',  ( 11.58810207955109917, 3.203462856645999945, -7.174999999999999822 ) ) ;
#6913=CARTESIAN_POINT ( 'NONE',  ( 11.48641235500450009, 3.260080192309100067, -6.822158181405299615 ) ) ;
#6917=CARTESIAN_POINT ( 'NONE',  ( 9.505051052051998184, 5.120555153167999585, -7.719295683256799379 ) ) ;
#7000=CARTESIAN_POINT ( 'NONE',  ( 10.89564560330029863, 4.307504762655200103, -6.544808043482999160 ) ) ;
#7010=CARTESIAN_POINT ( 'NONE',  ( 11.42887348028849992, 2.875789035466000065, -8.107837221875000111 ) ) ;
#7064=CARTESIAN_POINT ( 'NONE',  ( 8.956149159797568871, 2.922971693198220144, -7.209669135134798346 ) ) ;
#7070=CARTESIAN_POINT ( 'NONE',  ( 10.29226717315700057, 3.026371913119300316, -6.670281532133299329 ) ) ;
#7082=CARTESIAN_POINT ( 'NONE',  ( 9.958513540182876156, 3.836375382625530239, -8.749999999999998224 ) ) ;
#7095=CARTESIAN_POINT ( 'NONE',  ( 11.10612378248509913, 3.517039242046199998, -6.586279795136899651 ) ) ;
#7096=CARTESIAN_POINT ( 'NONE',  ( 9.305380199233999505, 4.996570247675600207, -7.374740103075099640 ) ) ;
#7119=CARTESIAN_POINT ( 'NONE',  ( 11.09256785386839894, 3.167490253789400523, -8.060248494254899754 ) ) ;
#7129=CARTESIAN_POINT ( 'NONE',  ( 9.048601287889788125, 4.000000467705929985, -8.698595322193607871 ) ) ;
#7186=CARTESIAN_POINT ( 'NONE',  ( 10.83810672858429847, 2.978701842912999886, -6.731711997412900494 ) ) ;
#7187=B_SPLINE_CURVE_WITH_KNOTS ( 'NONE', 3,
 ( #52366, #41531, #57258, #41877, #9359, #69134, #47474, #51675, #21240, #52013, #19867, #41198, #56929, #26494, #30704, #14289, #36638, #20898 ),
 .UNSPECIFIED., .F., .F.,
 ( 4, 2, 2, 2, 2, 2, 2, 2, 4 ),
 ( 0.000000000000000000, 0.1250000000000000000, 0.2500000000000000000, 0.3750000000000000000, 0.5000000000000000000, 0.6250000000000000000, 0.7500000000000000000, 0.8750000000000000000, 1.000000000000000000 ),
 .UNSPECIFIED. ) ;
#7202=FACE_OUTER_BOUND ( 'NONE', #17132, .T. ) ;
#7264=CARTESIAN_POINT ( 'NONE',  ( 10.92441504065829960, 4.694414232677499577, -6.982228367137699898 ) ) ;
#7267=CARTESIAN_POINT ( 'NONE',  ( 9.809000818239997699, 2.989704013253000614, -8.032011717116800398 ) ) ;
#7321=CARTESIAN_POINT ( 'NONE',  ( 9.110163692916374956, 5.234200089434220438, -7.245561603203542589 ) ) ;
#7345=CARTESIAN_POINT ( 'NONE',  ( 10.30072469555899950, 4.570852684939899824, -6.512367818249299667 ) ) ;
#7352=CARTESIAN_POINT ( 'NONE',  ( 11.13349010443639919, 5.274453806861999716, -7.595309363461700158 ) ) ;
#7413=CARTESIAN_POINT ( 'NONE',  ( 10.44424205625099944, 3.541248877825399877, -8.694123841252999085 ) ) ;
#7416=ORIENTED_EDGE ( 'NONE', *, *, #54800, .F. ) ;
#7433=CARTESIAN_POINT ( 'NONE',  ( 10.57980110216399972, 3.260758259645400337, -7.048535450274799885 ) ) ;
#7435=CARTESIAN_POINT ( 'NONE',  ( 11.56322412107030928, 4.054600656575539475, -6.467939235001000320 ) ) ;
#7436=CARTESIAN_POINT ( 'NONE',  ( 10.06525461470299909, 3.026595211686900377, -7.747639695388999215 ) ) ;
#7437=LINE ( 'NONE', #8821, #629 ) ;
#7441=EDGE_CURVE ( 'NONE', #50078, #59647, #45967, .T. ) ;
#7446=CARTESIAN_POINT ( 'NONE',  ( 10.06276198887462847, 3.334064478527818842, -6.932494801640175730 ) ) ;
#7458=CARTESIAN_POINT ( 'NONE',  ( 11.06795257254739973, 3.036453385827900142, -7.780229861306499295 ) ) ;
#7504=CIRCLE ( 'NONE', #34324, 1.249999999999999778 ) ;
#7521=CARTESIAN_POINT ( 'NONE',  ( 10.39503166480599994, 2.725152142215999884, -7.589885038193400213 ) ) ;
#7535=B_SPLINE_CURVE_WITH_KNOTS ( 'NONE', 3,
 ( #18911, #51066, #8762, #3169 ),
 .UNSPECIFIED., .F., .F.,
 ( 4, 4 ),
 ( 0.000000000000000000, 1.000000000000000000 ),
 .UNSPECIFIED. ) ;
#7580=ORIENTED_EDGE ( 'NONE', *, *, #960, .F. ) ;
#7600=CARTESIAN_POINT ( 'NONE',  ( 10.53521345716899837, 4.924890298941200228, -8.340879262988799780 ) ) ;
#7610=CARTESIAN_POINT ( 'NONE',  ( 11.70794988689359961, 4.455786710255300598, -8.393984925606600811 ) ) ;
#7612=CARTESIAN_POINT ( 'NONE',  ( 10.49288779216199785, 5.056118594996999782, -7.880862084500499520 ) ) ;
#7651=AXIS2_PLACEMENT_3D ( 'NONE', #55097, #13829, #28537 ) ;
#7655=EDGE_CURVE ( 'NONE', #21434, #63258, #50053, .T. ) ;
#7658=ADVANCED_FACE ( 'NONE', ( #62429 ), #14548, .T. ) ;
#7673=DIRECTION ( 'NONE',  ( -1.000000000000000000, 0.000000000000000000, 0.000000000000000000 ) ) ;
#7698=CARTESIAN_POINT ( 'NONE',  ( 11.61759063708296047, 5.217265640542000149, -7.842242470354300110 ) ) ;
#7707=CARTESIAN_POINT ( 'NONE',  ( 11.55194988689359903, 4.580487242693600081, -8.638573882912000457 ) ) ;
#7747=VERTEX_POINT ( 'NONE', #47392 ) ;
#7786=CARTESIAN_POINT ( 'NONE',  ( 11.09672200990539892, 3.182132064022000328, -7.214709569664399247 ) ) ;
#7788=CARTESIAN_POINT ( 'NONE',  ( 10.29399293566599916, 4.546741702992100009, -8.170700474995699736 ) ) ;
#7789=CARTESIAN_POINT ( 'NONE',  ( 9.328696787962998727, 4.196076320588900010, -6.375149554610999303 ) ) ;
#7810=CARTESIAN_POINT ( 'NONE',  ( 11.48641235500450009, 3.260080192309100067, -6.822158181405299615 ) ) ;
#7819=B_SPLINE_CURVE_WITH_KNOTS ( 'NONE', 3,
 ( #56682, #45162, #18930, #8781, #60889, #40255, #13005, #34677, #30124, #3191, #66468, #67152, #40594, #23825, #51427, #34331, #3522, #55650 ),
 .UNSPECIFIED., .F., .F.,
 ( 4, 2, 2, 2, 2, 2, 2, 2, 4 ),
 ( 0.000000000000000000, 0.1249999999999996669, 0.2499999999999993339, 0.3749999999999990008, 0.4999999999999986677, 0.6249999999999990008, 0.7499999999999993339, 0.8749999999999996669, 1.000000000000000000 ),
 .UNSPECIFIED. ) ;
#7835=B_SPLINE_CURVE_WITH_KNOTS ( 'NONE', 3,
 ( #64485, #37585, #26772, #1224, #37248, #43875, #65181, #32358, #48084, #188, #37932, #64834, #6456, #16943, #38275, #42837, #16607, #27110, #21504, #54009, #11021, #59251, #11701, #27806, #11358, #42498, #63806, #64147, #6111, #33040 ),
 .UNSPECIFIED., .F., .F.,
 ( 4, 2, 1, 1, 2, 2, 2, 2, 2, 2, 2, 2, 2, 2, 2, 4 ),
 ( 0.000000000000000000, 0.1249999999999982792, 0.1874999999999971134, 0.2187499999999965583, 0.2343749999999966416, 0.2499999999999967248, 0.3749999999999978351, 0.4374999999999978906, 0.4999999999999980016, 0.5624999999999981126, 0.6249999999999982236, 0.6874999999999984457, 0.7499999999999985567, 0.8124999999999986677, 0.8749999999999987788, 1.000000000000000000 ),
 .UNSPECIFIED. ) ;
#7911=EDGE_CURVE ( 'NONE', #50154, #14855, #36676, .T. ) ;
#7927=CARTESIAN_POINT ( 'NONE',  ( 10.39393020684999946, 2.750000000000000000, -7.500000000000000000 ) ) ;
#7957=CARTESIAN_POINT ( 'NONE',  ( 10.99826088462129903, 4.001843064679911244, -6.633804182961699603 ) ) ;
#7960=CARTESIAN_POINT ( 'NONE',  ( 9.376392757686998536, 4.677963304775400566, -8.241085728986799808 ) ) ;
#8003=CARTESIAN_POINT ( 'NONE',  ( 11.01279632507519857, 4.624908853805600906, -8.658468685623999406 ) ) ;
#8012=CARTESIAN_POINT ( 'NONE',  ( 11.14975833414749928, 3.203462856645999945, -7.825000000000000178 ) ) ;
#8019=CARTESIAN_POINT ( 'NONE',  ( 9.048601287889788125, 4.000000467705929985, -8.698595322193607871 ) ) ;
#8041=CARTESIAN_POINT ( 'NONE',  ( 10.57149279008999798, 3.703313553258400059, -8.601484120896000007 ) ) ;
#8049=CARTESIAN_POINT ( 'NONE',  ( 10.73964560330029983, 4.391636236366600166, -6.283473206644000442 ) ) ;
#8054=CARTESIAN_POINT ( 'NONE',  ( 11.59999999999999964, 5.179498027601999510, -7.174999999999999822 ) ) ;
#8108=CARTESIAN_POINT ( 'NONE',  ( 8.903317944506801140, 3.725094887964650603, -6.473766235688634296 ) ) ;
#8131=CARTESIAN_POINT ( 'NONE',  ( 11.26902897915239876, 4.221721321201099997, -8.337339982364900592 ) ) ;
#8136=CARTESIAN_POINT ( 'NONE',  ( 9.354025935145999782, 3.834207658792500251, -6.370288821165999593 ) ) ;
#8144=CARTESIAN_POINT ( 'NONE',  ( 10.31021345716899873, 4.636538040886300394, -8.078719053813800954 ) ) ;
#8181=ORIENTED_EDGE ( 'NONE', *, *, #5292, .T. ) ;
#8249=CARTESIAN_POINT ( 'NONE',  ( 10.89835090130999973, 4.878966983716200190, -8.043647632228999811 ) ) ;
#8277=CARTESIAN_POINT ( 'NONE',  ( 11.16486084871730000, 5.207010770456999893, -7.174999999999999822 ) ) ;
#8302=CARTESIAN_POINT ( 'NONE',  ( 11.11302897915239818, 4.291996373817799970, -8.602736702002999891 ) ) ;
#8305=CARTESIAN_POINT ( 'NONE',  ( 9.806988259785999418, 3.868581654116200141, -8.495776841814999258 ) ) ;
#8337=EDGE_LOOP ( 'NONE', ( #10384, #513, #62071, #6474, #6517 ) ) ;
#8345=CARTESIAN_POINT ( 'NONE',  ( 11.09590547754519996, 5.315605332491999846, -7.541753805330609239 ) ) ;
#8363=CARTESIAN_POINT ( 'NONE',  ( 9.022188178962251115, 3.408865106546499657, -8.523911321890818016 ) ) ;
#8388=CARTESIAN_POINT ( 'NONE',  ( 11.35502763632549872, 2.839566963815999934, -6.964545474268299508 ) ) ;
#8395=CARTESIAN_POINT ( 'NONE',  ( 10.98579841651039857, 3.550031058388499972, -8.696179055230999211 ) ) ;
#8455=( NAMED_UNIT ( * ) PLANE_ANGLE_UNIT ( ) SI_UNIT ( $, .RADIAN. ) );
#8458=CARTESIAN_POINT ( 'NONE',  ( 9.431076168958000494, 3.350848599899200142, -8.602264418015000302 ) ) ;
#8477=CARTESIAN_POINT ( 'NONE',  ( 11.68748876160954886, 3.399618311400500303, -8.124372018288600117 ) ) ;
#8479=CARTESIAN_POINT ( 'NONE',  ( 10.65413259636999932, 3.216622244594500302, -7.926858177843299380 ) ) ;
#8480=CARTESIAN_POINT ( 'NONE',  ( 9.885938025973999288, 3.406370524467499994, -6.524634174392399899 ) ) ;
#8488=CARTESIAN_POINT ( 'NONE',  ( 9.150912690312626552, 3.194792839887663938, -7.842306439064141266 ) ) ;
#8519=CARTESIAN_POINT ( 'NONE',  ( 8.795853127542962113, 4.029789221522052323, -8.445853177989366856 ) ) ;
#8559=CARTESIAN_POINT ( 'NONE',  ( 10.34588779216199939, 4.801941500727100021, -7.789199634454999632 ) ) ;
#8577=B_SPLINE_CURVE_WITH_KNOTS ( 'NONE', 3,
 ( #47399, #58224, #52986, #51011, #31320, #41464, #21167, #30981, #24444 ),
 .UNSPECIFIED., .F., .F.,
 ( 4, 1, 1, 1, 1, 1, 4 ),
 ( 0.000000000000000000, 0.1176715969261405564, 0.3173201826739889819, 0.5169687684225861002, 0.7166173541704345951, 0.9162659399182834230, 1.000000000000000000 ),
 .UNSPECIFIED. ) ;
#8590=CARTESIAN_POINT ( 'NONE',  ( 11.14767835872009982, 3.125658946326500320, -6.948943352864199952 ) ) ;
#8624=ORIENTED_EDGE ( 'NONE', *, *, #36751, .T. ) ;
#8640=CARTESIAN_POINT ( 'NONE',  ( 11.18687482311539938, 5.057677595549000316, -7.927326830586499007 ) ) ;
#8643=CARTESIAN_POINT ( 'NONE',  ( 9.452380199233999747, 4.996570247675600207, -7.374740103075099640 ) ) ;
#8662=ORIENTED_EDGE ( 'NONE', *, *, #30159, .F. ) ;
#8665=AXIS2_PLACEMENT_3D ( 'NONE', #50632, #9337, #66356 ) ;
#8684=CARTESIAN_POINT ( 'NONE',  ( 11.76077869730539938, 3.404661623424200201, -6.326049646822999861 ) ) ;
#8729=CARTESIAN_POINT ( 'NONE',  ( 10.78887616594230003, 3.613544262574699850, -6.281817606595999415 ) ) ;
#8748=EDGE_CURVE ( 'NONE', #18146, #42619, #3237, .T. ) ;
#8762=CARTESIAN_POINT ( 'NONE',  ( 11.48513281071060277, 2.915426916004881353, -7.824999134348144203 ) ) ;
#8781=CARTESIAN_POINT ( 'NONE',  ( 9.635596873516668381, 5.092232985442826099, -6.870476274536379435 ) ) ;
#8799=CARTESIAN_POINT ( 'NONE',  ( 9.608380199233998553, 5.269225938816000543, -7.340469740450900282 ) ) ;
#8808=CARTESIAN_POINT ( 'NONE',  ( 9.893930206848997599, 2.750000000000000000, -7.500000000000000000 ) ) ;
#8816=CARTESIAN_POINT ( 'NONE',  ( 11.46595122972049907, 4.343798595649099425, -6.704952129760900270 ) ) ;
#8818=B_SPLINE_CURVE_WITH_KNOTS ( 'NONE', 3,
 ( #27686, #49000, #10904, #33278, #32582, #59140, #59482, #58454, #28033, #42724 ),
 .UNSPECIFIED., .F., .F.,
 ( 4, 2, 2, 2, 4 ),
 ( 0.000000000000000000, 0.2500000000000000000, 0.5000000000000000000, 0.7500000000000000000, 1.000000000000000000 ),
 .UNSPECIFIED. ) ;
#8820=CARTESIAN_POINT ( 'NONE',  ( 9.151392757686998891, 4.770706668257700400, -8.342464052342599246 ) ) ;
#8821=CARTESIAN_POINT ( 'NONE',  ( 11.59999999999999964, 5.207010770456999893, -7.825000000000000178 ) ) ;
#8828=CARTESIAN_POINT ( 'NONE',  ( 8.922950365671626471, 4.680938325111460685, -6.950586433956124743 ) ) ;
#8836=ADVANCED_FACE ( 'NONE', ( #26173 ), #26266, .F. ) ;
#8914=EDGE_CURVE ( 'NONE', #32326, #11941, #19076, .T. ) ;
#8934=CARTESIAN_POINT ( 'NONE',  ( 10.52799293566599914, 4.806678152079100208, -8.489570425681801424 ) ) ;
#8941=EDGE_LOOP ( 'NONE', ( #23986, #46338, #7580, #60553, #59756, #14186 ) ) ;
#8950=CARTESIAN_POINT ( 'NONE',  ( 11.39975833414730033, 4.796537143354000499, -7.174999999999999822 ) ) ;
#8961=ORIENTED_EDGE ( 'NONE', *, *, #7655, .T. ) ;
#8970=CARTESIAN_POINT ( 'NONE',  ( 10.38528584683667688, 4.732620749361600154, -8.166081851074052267 ) ) ;
#8973=VERTEX_POINT ( 'NONE', #11804 ) ;
#8977=PLANE ( 'NONE',  #48824 ) ;
#8980=CARTESIAN_POINT ( 'NONE',  ( 10.92026088462129962, 4.002135146349410810, -6.496532863517000322 ) ) ;
#8982=CARTESIAN_POINT ( 'NONE',  ( 9.072442991499999110, 3.936771438983030169, -6.497580701799000380 ) ) ;
#8987=EDGE_LOOP ( 'NONE', ( #55378, #31073, #13094 ) ) ;
#9021=CARTESIAN_POINT ( 'NONE',  ( 10.43614141025499897, 4.549633050978300730, -8.478951440767898973 ) ) ;
#9101=EDGE_CURVE ( 'NONE', #50154, #62603, #12400, .T. ) ;
#9146=CARTESIAN_POINT ( 'NONE',  ( 10.09393020684899867, 5.250000000000000000, -7.500000000000000000 ) ) ;
#9151=CARTESIAN_POINT ( 'NONE',  ( 11.58487348028854846, 3.117292544139400157, -7.977261354519500358 ) ) ;
#9154=CARTESIAN_POINT ( 'NONE',  ( 10.94501463001509833, 4.472480213525599879, -6.743262887067199784 ) ) ;
#9155=CARTESIAN_POINT ( 'NONE',  ( 8.872772138681998655, 3.575113238066399912, -6.440186012775000357 ) ) ;
#9199=CARTESIAN_POINT ( 'NONE',  ( 9.973631561148998514, 3.315688435009791490, -8.575598637068459595 ) ) ;
#9236=CARTESIAN_POINT ( 'NONE',  ( 9.883513540182333301, 2.750000000000000000, -7.336375382625530683 ) ) ;
#9262=CARTESIAN_POINT ( 'NONE',  ( 10.60235971519489873, 4.605301262871499546, -6.493038401303000029 ) ) ;
#9315=CARTESIAN_POINT ( 'NONE',  ( 10.60026222744819790, 3.225465054973100099, -8.138001937130599828 ) ) ;
#9317=CARTESIAN_POINT ( 'NONE',  ( 10.06027973160899869, 4.090130512164860122, -6.499640669006000238 ) ) ;
#9337=DIRECTION ( 'NONE',  ( -1.000000000000000000, 0.000000000000000000, 0.000000000000000000 ) ) ;
#9353=CARTESIAN_POINT ( 'NONE',  ( 10.85168717260509830, 3.386210853237200169, -8.501809683958001074 ) ) ;
#9359=CARTESIAN_POINT ( 'NONE',  ( 9.396013540183334456, 3.000416447002273834, -8.268183399968641822 ) ) ;
#9375=EDGE_CURVE ( 'NONE', #26060, #12138, #44437, .T. ) ;
#9427=CARTESIAN_POINT ( 'NONE',  ( 10.69837472757367713, 3.526507217177279330, -8.234774922628410820 ) ) ;
#9490=CARTESIAN_POINT ( 'NONE',  ( 10.25564828895399927, 4.880669054351300495, -7.981013126389099099 ) ) ;
#9493=CARTESIAN_POINT ( 'NONE',  ( 9.428000818238999159, 2.868129552070000088, -8.096031607030200306 ) ) ;
#9504=CARTESIAN_POINT ( 'NONE',  ( 8.897621218489625505, 4.818672874536578554, -7.191281694476484354 ) ) ;
#9574=CARTESIAN_POINT ( 'NONE',  ( 11.34523293495530005, 2.684794526488000432, -7.447129085684729866 ) ) ;
#9575=CARTESIAN_POINT ( 'NONE',  ( 10.24457120343299898, 3.957971921952620598, -8.365991721916298474 ) ) ;
#9580=CARTESIAN_POINT ( 'NONE',  ( 9.685596873515667227, 5.092232985442825210, -6.870476274536379435 ) ) ;
#9610=CARTESIAN_POINT ( 'NONE',  ( 10.93990547754509812, 5.032986398992000510, -7.532784233952049213 ) ) ;
#9624=LINE ( 'NONE', #61406, #37656 ) ;
#9661=CARTESIAN_POINT ( 'NONE',  ( 10.99410672858429905, 3.198097575668700010, -6.896755974168000236 ) ) ;
#9663=CARTESIAN_POINT ( 'NONE',  ( 9.121088727410999297, 3.136022381937999981, -7.572461161969050281 ) ) ;
#9676=AXIS2_PLACEMENT_3D ( 'NONE', #40345, #19020, #18341 ) ;
#9704=CARTESIAN_POINT ( 'NONE',  ( 11.43856039236529831, 5.032284719763000069, -7.550239075043479353 ) ) ;
#9749=CARTESIAN_POINT ( 'NONE',  ( 11.60000000000000142, 3.528833218773709035, -8.438845841270557813 ) ) ;
#9777=CARTESIAN_POINT ( 'NONE',  ( 11.01837338474678063, 3.735675910162961078, -6.666799917282374643 ) ) ;
#9793=CARTESIAN_POINT ( 'NONE',  ( 11.30361999289329766, 3.455907502640805262, -6.342116603374313044 ) ) ;
#9841=CARTESIAN_POINT ( 'NONE',  ( 10.92026088462129962, 4.002135146349410810, -6.496532863517000322 ) ) ;
#9844=CARTESIAN_POINT ( 'NONE',  ( 9.326684229509998758, 3.098260518542999886, -6.592668585875199661 ) ) ;
#9860=EDGE_CURVE ( 'NONE', #11941, #17206, #23678, .T. ) ;
#9895=CONICAL_SURFACE ( 'NONE', #7651, 0.9346783463124002100, 0.7853981908209605178 ) ;
#9926=CARTESIAN_POINT ( 'NONE',  ( 10.55569598648999907, 5.130952141044000214, -8.173387776112500447 ) ) ;
#9927=CARTESIAN_POINT ( 'NONE',  ( 9.839304848515999069, 4.788504886021700102, -7.860510733857099197 ) ) ;
#9945=EDGE_CURVE ( 'NONE', #17206, #48127, #5344, .T. ) ;
#9954=DIRECTION ( 'NONE',  ( 0.000000000000000000, 1.000000000000000000, 0.000000000000000000 ) ) ;
#9962=CARTESIAN_POINT ( 'NONE',  ( 10.73724174883999893, 3.975468761016990094, -8.391788556008700439 ) ) ;
#9978=DIRECTION ( 'NONE',  ( -1.000000000000000000, 0.000000000000000000, 0.000000000000000000 ) ) ;
#9998=CARTESIAN_POINT ( 'NONE',  ( 10.46029575260939026, 4.828733415692241238, -8.253465265694869046 ) ) ;
#10011=CARTESIAN_POINT ( 'NONE',  ( 11.47810404293059960, 3.436653965247300047, -8.647151967355000579 ) ) ;
#10013=CARTESIAN_POINT ( 'NONE',  ( 8.971126402771000485, 4.939810497841199854, -7.145601175474399547 ) ) ;
#10053=CARTESIAN_POINT ( 'NONE',  ( 10.56080513895999928, 5.026880838510000338, -6.929150654994399083 ) ) ;
#10099=CARTESIAN_POINT ( 'NONE',  ( 11.60000000000000320, 4.924024592270518141, -8.335607184109882439 ) ) ;
#10109=CARTESIAN_POINT ( 'NONE',  ( 10.26059687351566652, 3.370476274536378547, -6.407767014557177454 ) ) ;
#10131=CARTESIAN_POINT ( 'NONE',  ( 11.59999999999999964, 3.116215992411100366, -7.825000000000000178 ) ) ;
#10189=CARTESIAN_POINT ( 'NONE',  ( 11.16641369783139837, 3.949373449607799902, -8.502191501283999031 ) ) ;
#10193=CARTESIAN_POINT ( 'NONE',  ( 9.883925467520999320, 2.723846966067000164, -7.411581555133209598 ) ) ;
#10251=EDGE_CURVE ( 'NONE', #22879, #53681, #7835, .T. ) ;
#10270=CARTESIAN_POINT ( 'NONE',  ( 9.358051052051999719, 4.850870049477099322, -7.666517576877299511 ) ) ;
#10276=CARTESIAN_POINT ( 'NONE',  ( 11.59999999999999964, 5.179498027601999510, -7.174999999999999822 ) ) ;
#10302=CARTESIAN_POINT ( 'NONE',  ( 11.08482133862618113, 4.942979055179590908, -8.373613860257941965 ) ) ;
#10356=CARTESIAN_POINT ( 'NONE',  ( 11.37964291764649971, 2.731641218595000087, -7.343212302062899433 ) ) ;
#10359=CARTESIAN_POINT ( 'NONE',  ( 8.996455549952997899, 4.781695603001899997, -6.869290649434700136 ) ) ;
#10373=CARTESIAN_POINT ( 'NONE',  ( 9.289752973821551407, 3.672827138550766257, -6.282573595533350819 ) ) ;
#10384=ORIENTED_EDGE ( 'NONE', *, *, #14666, .T. ) ;
#10395=CARTESIAN_POINT ( 'NONE',  ( 11.31389666366019853, 3.954123449088899900, -8.532487796751999198 ) ) ;
#10484=VECTOR ( 'NONE', #6566, 1000.000000000000114 ) ;
#10525=CARTESIAN_POINT ( 'NONE',  ( 9.302417874593999159, 2.949199072237000063, -7.946712276748498560 ) ) ;
#10527=CARTESIAN_POINT ( 'NONE',  ( 10.87103032197929942, 4.583685623598699799, -6.683751296690399357 ) ) ;
#10530=CARTESIAN_POINT ( 'NONE',  ( 8.946747021775999897, 3.038503783616799847, -8.343747244947598674 ) ) ;
#10586=CARTESIAN_POINT ( 'NONE',  ( 10.72726354018300121, 4.629523725463627670, -6.407767014557179230 ) ) ;
#10590=CARTESIAN_POINT ( 'NONE',  ( 10.32101354018304207, 3.231816600031359510, -6.500416447002272946 ) ) ;
#10611=CARTESIAN_POINT ( 'NONE',  ( 9.662000818238999145, 3.232852935619000334, -7.903971937289999694 ) ) ;
#10634=CARTESIAN_POINT ( 'NONE',  ( 11.78594988689359901, 4.393436444036099786, -8.271690446953899212 ) ) ;
#10645=CARTESIAN_POINT ( 'NONE',  ( 11.02812378248509795, 3.583106837161099900, -6.711274001288999536 ) ) ;
#10695=CARTESIAN_POINT ( 'NONE',  ( 10.86687616594229944, 3.655053560864600204, -6.412662853391999818 ) ) ;
#10699=CARTESIAN_POINT ( 'NONE',  ( 10.10892546752099896, 3.135062625344399834, -7.440072690703440017 ) ) ;
#10709=ORIENTED_EDGE ( 'NONE', *, *, #23791, .T. ) ;
#10722=EDGE_CURVE ( 'NONE', #43345, #64217, #41142, .T. ) ;
#10749=ORIENTED_EDGE ( 'NONE', *, *, #56665, .T. ) ;
#10757=CYLINDRICAL_SURFACE ( 'NONE', #31958, 1.250000000000000222 ) ;
#10770=CARTESIAN_POINT ( 'NONE',  ( 8.748004441081999261, 3.610923974646400136, -8.341443180570399463 ) ) ;
#10777=CARTESIAN_POINT ( 'NONE',  ( 11.68748876160954886, 3.399618311400500303, -8.124372018288600117 ) ) ;
#10818=CARTESIAN_POINT ( 'NONE',  ( 9.571013540182331525, 4.768183399968643599, -8.499583552997725278 ) ) ;
#10863=CARTESIAN_POINT ( 'NONE',  ( 11.58071932425156980, 3.832730087831799803, -8.628410767520000135 ) ) ;
#10870=CARTESIAN_POINT ( 'NONE',  ( 10.18893802597399834, 3.406370524467499994, -6.524634174392399899 ) ) ;
#10873=CARTESIAN_POINT ( 'NONE',  ( 11.23610538575739959, 5.109472165990999848, -7.234742334405199315 ) ) ;
#10904=CARTESIAN_POINT ( 'NONE',  ( 11.30671024775549505, 4.620655945117460028, -8.119376818724933997 ) ) ;
#10915=ORIENTED_EDGE ( 'NONE', *, *, #62650, .T. ) ;
#10938=CARTESIAN_POINT ( 'NONE',  ( 10.28976354018291239, 3.672815144550904076, -6.282534154164603812 ) ) ;
#10961=CARTESIAN_POINT ( 'NONE',  ( 11.84388784977539899, 2.744254309011999737, -7.428242901739219306 ) ) ;
#10962=CARTESIAN_POINT ( 'NONE',  ( 9.611342523874998989, 3.142972170141900001, -7.368808371628100318 ) ) ;
#10982=CARTESIAN_POINT ( 'NONE',  ( 11.66287348028854964, 3.238044298475899918, -7.911973420841600380 ) ) ;
#10994=CARTESIAN_POINT ( 'NONE',  ( 11.31900581613029821, 4.750686773407899466, -7.982035256002799173 ) ) ;
#11017=ORIENTED_EDGE ( 'NONE', *, *, #32606, .T. ) ;
#11021=CARTESIAN_POINT ( 'NONE',  ( 11.59999999999999787, 3.695216987067940551, -6.544326332797708368 ) ) ;
#11050=CARTESIAN_POINT ( 'NONE',  ( 10.22687885159599830, 5.132709421626000079, -7.364871923548499844 ) ) ;
#11052=CARTESIAN_POINT ( 'NONE',  ( 8.920468108405998464, 4.966402032527499344, -7.773695785133000413 ) ) ;
#11089=CARTESIAN_POINT ( 'NONE',  ( 10.44125056272499918, 5.033400911533000510, -7.515315513715298934 ) ) ;
#11122=ORIENTED_EDGE ( 'NONE', *, *, #9375, .F. ) ;
#11210=CARTESIAN_POINT ( 'NONE',  ( 10.77256919669529900, 4.962345366016100101, -7.784327714719899483 ) ) ;
#11216=CARTESIAN_POINT ( 'NONE',  ( 11.50687348028854906, 2.996540789803000315, -8.042549288197099244 ) ) ;
#11296=CARTESIAN_POINT ( 'NONE',  ( 11.67403632436368888, 3.023821283238099955, -7.272033745815799755 ) ) ;
#11297=CARTESIAN_POINT ( 'NONE',  ( 9.280051052051998539, 4.985712601322500603, -7.692906630067099627 ) ) ;
#11343=CYLINDRICAL_SURFACE ( 'NONE', #34257, 1.250000000000000222 ) ;
#11358=CARTESIAN_POINT ( 'NONE',  ( 11.60000000000000142, 3.430179236374871099, -6.730205196242793342 ) ) ;
#11379=CARTESIAN_POINT ( 'NONE',  ( 8.751496707488000126, 4.081676005979390176, -8.356402621895700378 ) ) ;
#11382=CARTESIAN_POINT ( 'NONE',  ( 11.50271932425157040, 3.812601581225100400, -8.764198628556998827 ) ) ;
#11386=DIRECTION ( 'NONE',  ( -1.000000000000000000, 0.000000000000000000, 0.000000000000000000 ) ) ;
#11407=EDGE_LOOP ( 'NONE', ( #49502, #56631, #16574, #52617 ) ) ;
#11424=CARTESIAN_POINT ( 'NONE',  ( 10.73724174883999893, 3.975468761016990094, -8.391788556008700439 ) ) ;
#11426=EDGE_CURVE ( 'NONE', #17729, #17206, #40434, .T. ) ;
#11463=CARTESIAN_POINT ( 'NONE',  ( 11.19518313518939934, 3.462699341914400097, -8.179416362154199760 ) ) ;
#11469=B_SPLINE_SURFACE_WITH_KNOTS ( 'NONE', 3, 3, ( 
 ( #27555, #64600, #16025, #16708, #5192, #4842, #53092, #26183, #10777, #59363, #42270, #32124, #37020, #47509, #63574, #58332, #644, #5536, #26530, #37354, #47857, #69164, #21274, #63914, #26876, #16368, #53440, #53778, #11463, #48191, #293, #64255, #21613, #39428, #2366, #65294, #7957, #55160, #6568, #7264, #17766, #60747, #17411, #43990, #13217, #28958, #55508, #18450, #1677, #28604, #23688, #12862, #29296, #34542, #50607, #45023, #64939, #2709, #43642, #39084, #55855, #17053, #33152, #1327, #38386, #39776, #49914 ),
 ( #59711, #23345, #11811, #65981, #7610, #34192, #54468, #27910, #49219, #50261, #22645, #38735, #66329, #6913, #60064, #12168, #61095, #33499, #54813, #28247, #49567, #22993, #44343, #44689, #65640, #60407, #12513, #33844, #2028, #18108, #13559, #30320, #31007, #9661, #14237, #51629, #8980, #51290, #25061, #41487, #3046, #3724, #13897, #50950, #29647, #18799, #67696, #56882, #40796, #9315, #68045, #19474, #41151, #62119, #35566, #46392, #40451, #61776, #46739, #24379, #3387, #45709, #67018, #66675, #24033, #62797, #24723 ),
 ( #19820, #19126, #34876, #14918, #57213, #46048, #62460, #67354, #35224, #20160, #14580, #35897, #30656, #51966, #4067, #25403, #36241, #57557, #45367, #40127, #56195, #56536, #8640, #52321, #61439, #8302, #29991, #20504, #32042, #31691, #26796, #32724, #43209, #5460, #26099, #10695, #15607, #47425, #53699, #64512, #58251, #53357, #4758, #63136, #16632, #37612, #5109, #48111, #26446, #31348, #563, #211, #21532, #42864, #37273, #64173, #53013, #16287, #58943, #20851, #42184, #11050, #5793, #32386, #27135, #68732, #37960 ),
 ( #63487, #48455, #15945, #36938, #47777, #59280, #11382, #10011, #4415, #21872, #25753, #10356, #69085, #47082, #68384, #41830, #15263, #36586, #57912, #52661, #21191, #42521, #63830, #58595, #65904, #34111, #22565, #33417, #49834, #27476, #48801, #33765, #23605, #7186, #18032, #23266, #61016, #18373, #54035, #39347, #39695, #6137, #60668, #17327, #910, #64860, #55430, #22223, #13134, #43560, #12782, #7521, #54735, #55081, #16971, #38303, #59632, #11726, #33068, #2287, #54384, #60326, #6485, #27834, #44264, #12434, #39008 ) ),
 .UNSPECIFIED., .F., .F., .F.,
 ( 4, 4 ),
 ( 4, 1, 1, 1, 1, 1, 1, 1, 1, 1, 1, 1, 1, 1, 1, 1, 1, 1, 1, 1, 1, 1, 1, 1, 1, 1, 1, 1, 1, 1, 1, 1, 1, 1, 1, 1, 1, 1, 1, 1, 1, 1, 1, 1, 1, 1, 1, 1, 1, 1, 1, 1, 1, 1, 1, 1, 1, 1, 1, 1, 1, 1, 1, 1, 4 ),
 ( -0.02000000000000000042, 1.020000000000000018 ),
 ( 0.008747244164287000176, 0.02453926110774999961, 0.04033127805120999970, 0.05612329499467000327, 0.07191531193812999989, 0.08770732888158999652, 0.1034993458251000087, 0.1192913627684999978, 0.1350833797120000179, 0.1508753966553999792, 0.1666674135988999994, 0.1824594305423999918, 0.1982514474858000086, 0.2140434644293000011, 0.2298354813727000179, 0.2456274983162000103, 0.2614195152596999749, 0.2772115322030999640, 0.2930035491465999842, 0.3087955660900000288, 0.3245875830334999934, 0.3403795999769999581, 0.3561716169204000026, 0.3719636338639000228, 0.3877556508073999875, 0.4035476677507999765, 0.4193396846942999967, 0.4351317016376999858, 0.4509237185811999504, 0.4667157355247000261, 0.4825077524681000152, 0.4982997694115999798, 0.5140917863550000799, 0.5298838032985000446, 0.5456758202420000092, 0.5614678371854000538, 0.5772598541289000185, 0.5930518710723000630, 0.6088438880158000277, 0.6246359049592999924, 0.6404279219027000369, 0.6562199388462000016, 0.6720119557896999662, 0.6878039727331000108, 0.7035959896765999755, 0.7193880066200000201, 0.7351800235634999847, 0.7509720405069999494, 0.7667640574504001050, 0.7825560743939000696, 0.7983480913373000032, 0.8141401082808000789, 0.8299321252243000435, 0.8457241421676999771, 0.8615161591112000528, 0.8773081760545999863, 0.8931001929981000620, 0.9088922099416000266, 0.9246842268849999602, 0.9404762438285000359, 0.9562682607720000005, 0.9720602777153999341, 0.9878522946589000098, 1.003644311601999961, 1.019436328545999970 ),
 .UNSPECIFIED. ) ;
#11544=CARTESIAN_POINT ( 'NONE',  ( 10.87103032197929942, 4.583685623598699799, -6.683751296690399357 ) ) ;
#11551=CARTESIAN_POINT ( 'NONE',  ( 10.37457053952199892, 3.551693493661699730, -6.451042711717000167 ) ) ;
#11603=AXIS2_PLACEMENT_3D ( 'NONE', #49073, #49415, #43494 ) ;
#11615=CARTESIAN_POINT ( 'NONE',  ( 10.27934687351620724, 3.836375382625536012, -6.249999999999999112 ) ) ;
#11637=CARTESIAN_POINT ( 'NONE',  ( 11.39700581613019992, 4.869652672166700391, -8.058426314824099990 ) ) ;
#11638=CARTESIAN_POINT ( 'NONE',  ( 10.03992546752099990, 2.997990738918999920, -7.430575645513339822 ) ) ;
#11661=CARTESIAN_POINT ( 'NONE',  ( 11.04749144726329924, 3.499163784537000055, -6.793273974143599681 ) ) ;
#11700=EDGE_CURVE ( 'NONE', #50078, #11941, #43192, .T. ) ;
#11701=CARTESIAN_POINT ( 'NONE',  ( 11.60000000000000142, 3.552887809908069627, -6.627718330236056055 ) ) ;
#11726=CARTESIAN_POINT ( 'NONE',  ( 10.24733997687999931, 4.272363749081500295, -6.251346978035999591 ) ) ;
#11729=CARTESIAN_POINT ( 'NONE',  ( 10.34393020684899867, 2.750000000000000000, -7.500000000000000000 ) ) ;
#11770=CARTESIAN_POINT ( 'NONE',  ( 11.60988784977536348, 3.148894096305599799, -7.451365240271489832 ) ) ;
#11785=CARTESIAN_POINT ( 'NONE',  ( 10.84393020684979980, 2.750000000000000000, -7.500000000000000000 ) ) ;
#11804=CARTESIAN_POINT ( 'NONE',  ( 11.08810207955139937, 3.203462856645999945, -7.174999999999999822 ) ) ;
#11809=CARTESIAN_POINT ( 'NONE',  ( 10.35987047770899672, 2.749999999999999556, -7.750389189149368363 ) ) ;
#11811=CARTESIAN_POINT ( 'NONE',  ( 11.75718044953559804, 4.889766368533900120, -7.963966784336999005 ) ) ;
#11858=CARTESIAN_POINT ( 'NONE',  ( 10.59184687351642751, 4.999583552997727054, -8.268183399968643599 ) ) ;
#11897=CARTESIAN_POINT ( 'NONE',  ( 10.62487750876920067, 3.456442671114800191, -8.343502390669698343 ) ) ;
#11904=CARTESIAN_POINT ( 'NONE',  ( 11.60533460557258323, 4.184174550317700358, -8.625775273268001087 ) ) ;
#11907=CARTESIAN_POINT ( 'NONE',  ( 8.592138961223998450, 5.059894361919000438, -8.216246114996598848 ) ) ;
#11930=CARTESIAN_POINT ( 'NONE',  ( 11.59999999999999964, 4.000000000000000000, -7.500000000000000000 ) ) ;
#11941=VERTEX_POINT ( 'NONE', #28858 ) ;
#11964=( LENGTH_UNIT ( ) NAMED_UNIT ( * ) SI_UNIT ( .MILLI., .METRE. ) );
#11982=CARTESIAN_POINT ( 'NONE',  ( 9.854346873516623972, 2.749999999999999112, -7.663624617374463099 ) ) ;
#11993=CARTESIAN_POINT ( 'NONE',  ( 11.18412378248529926, 3.450971646934100079, -6.461285588983000316 ) ) ;
#11994=CARTESIAN_POINT ( 'NONE',  ( 8.824126402770998467, 4.939810497841199854, -7.145601175474399547 ) ) ;
#11998=EDGE_LOOP ( 'NONE', ( #62347, #57776, #18350, #6850, #20978, #62931, #42407, #22467, #37662, #4449, #20005 ) ) ;
#12017=CARTESIAN_POINT ( 'NONE',  ( 11.49056651104150006, 4.085456792591960706, -6.638028001068500217 ) ) ;
#12043=DIRECTION ( 'NONE',  ( -1.000000000000000000, 0.000000000000000000, 0.000000000000000000 ) ) ;
#12094=ORIENTED_EDGE ( 'NONE', *, *, #6260, .T. ) ;
#12118=CARTESIAN_POINT ( 'NONE',  ( 11.51145123989532948, 4.605239108938600445, -8.668865425277999748 ) ) ;
#12130=CARTESIAN_POINT ( 'NONE',  ( 10.48791429142999831, 4.016993441347180394, -6.608036045330599961 ) ) ;
#12138=VERTEX_POINT ( 'NONE', #20064 ) ;
#12141=CARTESIAN_POINT ( 'NONE',  ( 10.63559687351579974, 5.092232985442826099, -6.870476274536379435 ) ) ;
#12160=CARTESIAN_POINT ( 'NONE',  ( 8.749283493600000128, 4.089987329977850194, -8.350279134800100422 ) ) ;
#12168=CARTESIAN_POINT ( 'NONE',  ( 11.43718179236249988, 3.790319673775199849, -6.518682001772900136 ) ) ;
#12172=CARTESIAN_POINT ( 'NONE',  ( 9.479721904869998994, 4.995641764568400589, -8.058956102599799109 ) ) ;
#12231=ADVANCED_FACE ( 'NONE', ( #51531 ), #40695, .T. ) ;
#12253=CARTESIAN_POINT ( 'NONE',  ( 10.28026357027499849, 4.985299147223100746, -7.690095141806899903 ) ) ;
#12261=CARTESIAN_POINT ( 'NONE',  ( 10.71503032197929883, 4.743378537856500543, -6.460430507351999196 ) ) ;
#12262=CARTESIAN_POINT ( 'NONE',  ( 8.541480666858999982, 4.426512626096299918, -8.706015266875999359 ) ) ;
#12317=CARTESIAN_POINT ( 'NONE',  ( 8.936337454063531638, 3.131903168333550536, -6.831783586538417552 ) ) ;
#12343=CARTESIAN_POINT ( 'NONE',  ( 10.93479632507519916, 4.557787252275099732, -8.534037301706000278 ) ) ;
#12344=CARTESIAN_POINT ( 'NONE',  ( 10.09058376188599837, 3.152987476450699766, -8.039825975318500184 ) ) ;
#12353=CARTESIAN_POINT ( 'NONE',  ( 9.834799664234624927, 4.795722374051563541, -7.863810627050381363 ) ) ;
#12364=B_SPLINE_SURFACE_WITH_KNOTS ( 'NONE', 3, 3, ( 
 ( #22132, #64770, #16884, #38211, #6391, #49054, #40625, #24204, #8477, #2535, #61957, #56721, #34024, #23863, #2881, #35395, #13040, #8816, #55337, #56024, #14071, #30160, #1853, #45547, #60582, #8131, #3229, #23171, #44520, #35055, #66852, #65813, #7786, #50432, #17938, #29821, #23515, #61610, #18966, #34370, #66164, #39257, #24556, #61273, #45879, #40292, #13726, #39956, #56373, #45200, #66505, #18283, #12687, #7433, #28784, #51126, #29126, #67189, #19301, #50095, #2204, #39602, #50786, #44857, #60928, #55689, #18627 ),
 ( #13390, #34712, #29477, #57052, #67532, #51802, #35734, #57730, #68559, #9151, #3560, #3900, #42360, #25235, #15440, #4245, #63661, #63312, #4936, #14753, #46569, #62964, #26276, #62299, #20680, #30489, #10189, #41661, #36765, #20332, #67878, #21026, #37107, #58422, #52491, #40975, #9841, #52841, #10527, #24895, #58086, #25925, #46224, #57386, #30832, #51463, #31519, #19998, #42011, #47255, #36070, #41322, #19654, #47601, #15092, #68909, #4588, #15777, #36416, #14417, #52142, #25584, #62628, #9490, #46911, #68214, #31186 ),
 ( #1080, #37445, #43, #53185, #21363, #11904, #65030, #21700, #16798, #11216, #54205, #5623, #27653, #38126, #58766, #47943, #32217, #16119, #59453, #48974, #10873, #5282, #53531, #22737, #26964, #17147, #53865, #44086, #43732, #54563, #64340, #48278, #43390, #6660, #42693, #22395, #384, #59802, #22043, #38479, #731, #43036, #16457, #64001, #37789, #6306, #59110, #33242, #60157, #28001, #64690, #49310, #65385, #38829, #1422, #11551, #17506, #32552, #31867, #26624, #5966, #27304, #48628, #32894, #2456, #13312, #40215 ),
 ( #29046, #60845, #45460, #56291, #7707, #33590, #2799, #66077, #65733, #7010, #55605, #29740, #49661, #29392, #13646, #28342, #34973, #55256, #61532, #45117, #39174, #7352, #23781, #17856, #54907, #34284, #50356, #8395, #51043, #19219, #3144, #50702, #24125, #66772, #28697, #66424, #24473, #8049, #12261, #12957, #50011, #18890, #18545, #39872, #61191, #18198, #33937, #34634, #12606, #67110, #45797, #1770, #40545, #2121, #60497, #23438, #23088, #44436, #44777, #39520, #55946, #68474, #62550, #52755, #47517, #24816, #14673 ) ),
 .UNSPECIFIED., .F., .F., .F.,
 ( 4, 4 ),
 ( 4, 1, 1, 1, 1, 1, 1, 1, 1, 1, 1, 1, 1, 1, 1, 1, 1, 1, 1, 1, 1, 1, 1, 1, 1, 1, 1, 1, 1, 1, 1, 1, 1, 1, 1, 1, 1, 1, 1, 1, 1, 1, 1, 1, 1, 1, 1, 1, 1, 1, 1, 1, 1, 1, 1, 1, 1, 1, 1, 1, 1, 1, 1, 1, 4 ),
 ( -0.02000000000000000042, 1.020000000000000018 ),
 ( 0.008747244164287000176, 0.02453926110774999961, 0.04033127805120999970, 0.05612329499467000327, 0.07191531193812999989, 0.08770732888158999652, 0.1034993458251000087, 0.1192913627684999978, 0.1350833797120000179, 0.1508753966553999792, 0.1666674135988999994, 0.1824594305423999918, 0.1982514474858000086, 0.2140434644293000011, 0.2298354813727000179, 0.2456274983162000103, 0.2614195152596999749, 0.2772115322030999640, 0.2930035491465999842, 0.3087955660900000288, 0.3245875830334999934, 0.3403795999769999581, 0.3561716169204000026, 0.3719636338639000228, 0.3877556508073999875, 0.4035476677507999765, 0.4193396846942999967, 0.4351317016376999858, 0.4509237185811999504, 0.4667157355247000261, 0.4825077524681000152, 0.4982997694115999798, 0.5140917863550000799, 0.5298838032985000446, 0.5456758202420000092, 0.5614678371854000538, 0.5772598541289000185, 0.5930518710723000630, 0.6088438880158000277, 0.6246359049592999924, 0.6404279219027000369, 0.6562199388462000016, 0.6720119557896999662, 0.6878039727331000108, 0.7035959896765999755, 0.7193880066200000201, 0.7351800235634999847, 0.7509720405069999494, 0.7667640574504001050, 0.7825560743939000696, 0.7983480913373000032, 0.8141401082808000789, 0.8299321252243000435, 0.8457241421676999771, 0.8615161591112000528, 0.8773081760545999863, 0.8931001929981000620, 0.9088922099416000266, 0.9246842268849999602, 0.9404762438285000359, 0.9562682607720000005, 0.9720602777153999341, 0.9878522946589000098, 1.003644311601999961, 1.019436328545999970 ),
 .UNSPECIFIED. ) ;
#12368=CARTESIAN_POINT ( 'NONE',  ( 10.35826357027499789, 4.850513154668600002, -7.664090691848299386 ) ) ;
#12400=B_SPLINE_CURVE_WITH_KNOTS ( 'NONE', 3,
 ( #22518, #55039, #23223, #48756 ),
 .UNSPECIFIED., .F., .F.,
 ( 4, 4 ),
 ( 0.000000000000000000, 1.000000000000000000 ),
 .UNSPECIFIED. ) ;
#12434=CARTESIAN_POINT ( 'NONE',  ( 10.05862282008599884, 4.666276081381299790, -8.574682153725998290 ) ) ;
#12436=CARTESIAN_POINT ( 'NONE',  ( 8.893126402770997530, 4.811247217215600003, -7.194081880505399873 ) ) ;
#12476=EDGE_LOOP ( 'NONE', ( #40734, #15506, #58824, #18949 ) ) ;
#12485=CARTESIAN_POINT ( 'NONE',  ( 10.99664311227126312, 4.444039568019539033, -8.706333095531745059 ) ) ;
#12489=DIRECTION ( 'NONE',  ( -1.000000000000000000, 0.000000000000000000, 1.554312234491000161E-14 ) ) ;
#12513=CARTESIAN_POINT ( 'NONE',  ( 11.16641369783139837, 3.949373449607799902, -8.502191501283999031 ) ) ;
#12515=VECTOR ( 'NONE', #37427, 1000.000000000000227 ) ;
#12516=B_SPLINE_CURVE_WITH_KNOTS ( 'NONE', 3,
 ( #37391, #20973, #63611, #16405, #26221, #10818, #16061, #54154, #59061, #63259, #32498, #53476, #15727, #679, #15386, #62003, #16744, #58369 ),
 .UNSPECIFIED., .F., .F.,
 ( 4, 2, 2, 2, 2, 2, 2, 2, 4 ),
 ( 0.000000000000000000, 0.1250000000000000000, 0.2500000000000000000, 0.3750000000000000000, 0.5000000000000000000, 0.6250000000000000000, 0.7500000000000000000, 0.8750000000000000000, 1.000000000000000000 ),
 .UNSPECIFIED. ) ;
#12517=CARTESIAN_POINT ( 'NONE',  ( 9.910317406968998100, 4.212364169857599983, -8.621889436328999068 ) ) ;
#12599=CARTESIAN_POINT ( 'NONE',  ( 11.01041369783139956, 3.935522326596939902, -8.776385133971000840 ) ) ;
#12606=CARTESIAN_POINT ( 'NONE',  ( 10.46887750876899936, 3.307728619566300043, -8.574279626736998949 ) ) ;
#12627=CARTESIAN_POINT ( 'NONE',  ( 11.59213512191444018, 3.196550831395155168, -7.174950736703190834 ) ) ;
#12632=DIRECTION ( 'NONE',  ( 0.000000000000000000, -1.000000000000000000, 0.000000000000000000 ) ) ;
#12662=( NAMED_UNIT ( * ) SI_UNIT ( $, .STERADIAN. ) SOLID_ANGLE_UNIT ( ) );
#12681=CARTESIAN_POINT ( 'NONE',  ( 9.989763540182750035, 4.327184855449099921, -8.717465845835395299 ) ) ;
#12687=CARTESIAN_POINT ( 'NONE',  ( 10.60441638348510018, 3.158410350011299883, -7.294998899090099798 ) ) ;
#12689=CARTESIAN_POINT ( 'NONE',  ( 10.51925056272499859, 5.174767082365999471, -7.517410630436119234 ) ) ;
#12690=CARTESIAN_POINT ( 'NONE',  ( 8.748138961223999033, 4.832207374954999857, -8.062381800110799190 ) ) ;
#12699=CARTESIAN_POINT ( 'NONE',  ( 10.18940772478662637, 3.446387339840331965, -8.177528816364860731 ) ) ;
#12716=CARTESIAN_POINT ( 'NONE',  ( 11.77359063708300013, 4.955772084214699724, -7.768721787835699999 ) ) ;
#12782=CARTESIAN_POINT ( 'NONE',  ( 10.41964694612699915, 2.813019656517000477, -7.973702485506099613 ) ) ;
#12841=LINE ( 'NONE', #60036, #52052 ) ;
#12862=CARTESIAN_POINT ( 'NONE',  ( 10.62903166480609940, 3.135947233695900227, -7.560921321260908989 ) ) ;
#12865=CARTESIAN_POINT ( 'NONE',  ( 9.986304848515999311, 5.038423216181000086, -7.974775391194199869 ) ) ;
#12872=ADVANCED_FACE ( 'NONE', ( #32917 ), #49333, .F. ) ;
#12906=CARTESIAN_POINT ( 'NONE',  ( 10.72191429142990060, 4.025072603369280522, -6.183971186511000084 ) ) ;
#12949=CARTESIAN_POINT ( 'NONE',  ( 11.62579573085663043, 5.239377455231000624, -7.714452430741599365 ) ) ;
#12957=CARTESIAN_POINT ( 'NONE',  ( 10.69041504065829962, 5.024558373595999328, -6.736065107693399945 ) ) ;
#13005=CARTESIAN_POINT ( 'NONE',  ( 9.677263540183332680, 4.629523725463628558, -6.407767014557180119 ) ) ;
#13040=CARTESIAN_POINT ( 'NONE',  ( 11.49056651104150006, 4.085456792591960706, -6.638028001068500217 ) ) ;
#13043=CARTESIAN_POINT ( 'NONE',  ( 10.48791429142999831, 4.016993441347180394, -6.608036045330599961 ) ) ;
#13044=CARTESIAN_POINT ( 'NONE',  ( 9.303367640780999537, 4.538247246588100303, -6.493012239633999982 ) ) ;
#13066=CARTESIAN_POINT ( 'NONE',  ( 10.45672469555900008, 4.433465011431599656, -6.750062220519700062 ) ) ;
#13094=ORIENTED_EDGE ( 'NONE', *, *, #19883, .T. ) ;
#13109=EDGE_CURVE ( 'NONE', #64314, #6549, #12516, .T. ) ;
#13134=CARTESIAN_POINT ( 'NONE',  ( 10.46887750876899936, 3.307728619566300043, -8.574279626736998949 ) ) ;
#13198=EDGE_LOOP ( 'NONE', ( #36900, #42485, #39870, #64051 ) ) ;
#13217=CARTESIAN_POINT ( 'NONE',  ( 10.80133863405319872, 4.534404523786000674, -8.181696703306599261 ) ) ;
#13219=CARTESIAN_POINT ( 'NONE',  ( 10.31357120343299982, 3.951311476804090006, -8.503230697164999796 ) ) ;
#13304=CARTESIAN_POINT ( 'NONE',  ( 11.47810404293059960, 3.436653965247300047, -8.647151967355000579 ) ) ;
#13310=ORIENTED_EDGE ( 'NONE', *, *, #37918, .T. ) ;
#13312=CARTESIAN_POINT ( 'NONE',  ( 10.13662282008599824, 4.594711216567399781, -8.459250300176799797 ) ) ;
#13370=CARTESIAN_POINT ( 'NONE',  ( 10.39358376188600097, 2.921249888908000081, -8.187519150726398465 ) ) ;
#13379=AXIS2_PLACEMENT_3D ( 'NONE', #69023, #15548, #9954 ) ;
#13390=CARTESIAN_POINT ( 'NONE',  ( 11.78179573085659904, 4.973133828855400118, -7.668383662421899061 ) ) ;
#13394=CARTESIAN_POINT ( 'NONE',  ( 9.759292290062999697, 4.987433183662999703, -6.926667499798199401 ) ) ;
#13402=CARTESIAN_POINT ( 'NONE',  ( 10.08809113605762597, 3.189914598996232975, -7.169403702379763210 ) ) ;
#13416=CARTESIAN_POINT ( 'NONE',  ( 11.38795122972049967, 4.398282450130399646, -6.578956058177199751 ) ) ;
#13510=CARTESIAN_POINT ( 'NONE',  ( 11.64633327354034797, 3.135095881599500256, -6.934277916748599502 ) ) ;
#13528=CARTESIAN_POINT ( 'NONE',  ( 10.52934687351650389, 4.163624617374466652, -8.749999999999998224 ) ) ;
#13531=DIRECTION ( 'NONE',  ( 1.000000000000000000, 0.000000000000000000, 0.000000000000000000 ) ) ;
#13559=CARTESIAN_POINT ( 'NONE',  ( 11.06795257254739973, 3.036453385827900142, -7.780229861306499295 ) ) ;
#13561=CARTESIAN_POINT ( 'NONE',  ( 8.973138961223998677, 4.946050868436800307, -8.139313957553699908 ) ) ;
#13578=ADVANCED_FACE ( 'NONE', ( #49515 ), #941, .T. ) ;
#13601=CARTESIAN_POINT ( 'NONE',  ( 11.51145123989532948, 4.605239108938600445, -8.668865425277999748 ) ) ;
#13617=CARTESIAN_POINT ( 'NONE',  ( 9.041999884715581359, 3.843103124197280618, -8.691999950321772417 ) ) ;
#13639=CARTESIAN_POINT ( 'NONE',  ( 11.40425819896749893, 2.744109752373000255, -7.736761623643599428 ) ) ;
#13646=CARTESIAN_POINT ( 'NONE',  ( 11.30579707368350029, 3.365167912142600137, -6.390809033205999690 ) ) ;
#13709=CARTESIAN_POINT ( 'NONE',  ( 9.127126402770999292, 5.196937059091999878, -7.048639765412399782 ) ) ;
#13712=ORIENTED_EDGE ( 'NONE', *, *, #40786, .F. ) ;
#13726=CARTESIAN_POINT ( 'NONE',  ( 10.75210807141120029, 4.040019166404060336, -8.365272822098500427 ) ) ;
#13729=CARTESIAN_POINT ( 'NONE',  ( 9.480671671056999372, 2.873958896683999953, -7.689118697196099639 ) ) ;
#13737=CARTESIAN_POINT ( 'NONE',  ( 9.074925248765625341, 3.255423617190434271, -7.040502144637257764 ) ) ;
#13758=DIRECTION ( 'NONE',  ( 0.000000000000000000, 1.000000000000000000, 0.000000000000000000 ) ) ;
#13766=ORIENTED_EDGE ( 'NONE', *, *, #39815, .T. ) ;
#13788=B_SPLINE_CURVE_WITH_KNOTS ( 'NONE', 3,
 ( #36723, #68172, #30445, #9793, #20289, #31144, #67144, #62250, #4201, #40582 ),
 .UNSPECIFIED., .F., .F.,
 ( 4, 2, 2, 2, 4 ),
 ( 0.000000000000000000, 0.2500000000000002220, 0.5000000000000004441, 0.7500000000000002220, 1.000000000000000000 ),
 .UNSPECIFIED. ) ;
#13804=ORIENTED_EDGE ( 'NONE', *, *, #10722, .F. ) ;
#13829=DIRECTION ( 'NONE',  ( 1.000000000000000000, 0.000000000000000000, 0.000000000000000000 ) ) ;
#13838=ORIENTED_EDGE ( 'NONE', *, *, #1173, .F. ) ;
#13842=LINE ( 'NONE', #34493, #60006 ) ;
#13844=CARTESIAN_POINT ( 'NONE',  ( 11.18923293495519822, 2.967327562101000016, -7.458486839450950256 ) ) ;
#13877=ORIENTED_EDGE ( 'NONE', *, *, #40286, .F. ) ;
#13897=CARTESIAN_POINT ( 'NONE',  ( 10.77256919669529900, 4.962345366016100101, -7.784327714719899483 ) ) ;
#13899=CARTESIAN_POINT ( 'NONE',  ( 10.23758376188599861, 3.152987476450699766, -8.039825975318500184 ) ) ;
#13982=CARTESIAN_POINT ( 'NONE',  ( 11.23195122972050086, 4.507250159094099651, -6.326963915009999440 ) ) ;
#13993=DIRECTION ( 'NONE',  ( -1.000000000000000000, 0.000000000000000000, 0.000000000000000000 ) ) ;
#14050=CARTESIAN_POINT ( 'NONE',  ( 9.557721904870000174, 5.115452802765999785, -8.126218358304999612 ) ) ;
#14071=CARTESIAN_POINT ( 'NONE',  ( 11.39210538575740017, 4.842454415653899780, -7.298582155985900322 ) ) ;
#14075=CARTESIAN_POINT ( 'NONE',  ( 10.11390035061499937, 4.304339077956200299, -8.600505223349999895 ) ) ;
#14083=CARTESIAN_POINT ( 'NONE',  ( 8.772923981633081070, 4.310454296184184741, -8.314671747086004316 ) ) ;
#14120=ORIENTED_EDGE ( 'NONE', *, *, #56579, .T. ) ;
#14127=VERTEX_POINT ( 'NONE', #22081 ) ;
#14178=FILL_AREA_STYLE_COLOUR ( '', #64036 ) ;
#14185=CARTESIAN_POINT ( 'NONE',  ( 11.14256920625030034, 4.042230905578960254, -6.325872106312999676 ) ) ;
#14186=ORIENTED_EDGE ( 'NONE', *, *, #66296, .T. ) ;
#14192=( GEOMETRIC_REPRESENTATION_CONTEXT ( 3 ) GLOBAL_UNCERTAINTY_ASSIGNED_CONTEXT ( ( #44874 ) ) GLOBAL_UNIT_ASSIGNED_CONTEXT ( ( #66138, #8455, #12662 ) ) REPRESENTATION_CONTEXT ( 'NONE', 'WORKASPACE' ) );
#14194=EDGE_CURVE ( 'NONE', #57302, #63258, #13788, .T. ) ;
#14206=CARTESIAN_POINT ( 'NONE',  ( 8.599999999999999645, 4.000000000000000000, -7.500000000000000000 ) ) ;
#14237=CARTESIAN_POINT ( 'NONE',  ( 10.96949144726329806, 3.419793223320000131, -6.681274802424499448 ) ) ;
#14241=CARTESIAN_POINT ( 'NONE',  ( 9.325734463322998380, 4.104624583183299258, -8.498947444525299488 ) ) ;
#14282=CARTESIAN_POINT ( 'NONE',  ( 11.67766954483535891, 4.715882430684499305, -6.395429936871999566 ) ) ;
#14289=CARTESIAN_POINT ( 'NONE',  ( 9.573096873516668381, 5.217465845835396188, -7.827184855449103473 ) ) ;
#14326=CARTESIAN_POINT ( 'NONE',  ( 10.37041638348499895, 2.758294858530000226, -7.197535585171899619 ) ) ;
#14343=DIRECTION ( 'NONE',  ( 0.000000000000000000, 0.8514543052404082157, -0.5244287998266055073 ) ) ;
#14397=CARTESIAN_POINT ( 'NONE',  ( 9.583051052052001140, 5.255397705012999410, -7.745684736446600382 ) ) ;
#14417=CARTESIAN_POINT ( 'NONE',  ( 10.35410941423799791, 4.742797679580299963, -6.825313060354999628 ) ) ;
#14419=CARTESIAN_POINT ( 'NONE',  ( 11.23589666366019912, 3.960399224793059947, -8.391246537305399045 ) ) ;
#14420=CARTESIAN_POINT ( 'NONE',  ( 10.16455864497999961, 4.898932057185599653, -8.204026508301600629 ) ) ;
#14428=CARTESIAN_POINT ( 'NONE',  ( 9.201570984676626708, 3.555997837402618877, -8.253919324947762703 ) ) ;
#14492=EDGE_CURVE ( 'NONE', #53681, #22879, #9624, .T. ) ;
#14532=CARTESIAN_POINT ( 'NONE',  ( 10.55569598648999907, 5.130952141044000214, -8.173387776112500447 ) ) ;
#14548=PLANE ( 'NONE',  #45033 ) ;
#14580=CARTESIAN_POINT ( 'NONE',  ( 11.48225819896749833, 2.879005208331999910, -7.711331004020999913 ) ) ;
#14582=CARTESIAN_POINT ( 'NONE',  ( 9.629684229509999582, 3.291972602441000095, -6.787581931282099745 ) ) ;
#14584=CARTESIAN_POINT ( 'NONE',  ( 11.00000000000000000, 5.079754677601000523, -7.825000000000000178 ) ) ;
#14620=CARTESIAN_POINT ( 'NONE',  ( 10.81524174883999834, 3.971581146373189597, -8.533115712456000423 ) ) ;
#14666=EDGE_CURVE ( 'NONE', #68105, #33345, #61335, .T. ) ;
#14673=CARTESIAN_POINT ( 'NONE',  ( 10.05041772631199848, 4.549624259497900169, -8.631352948887998977 ) ) ;
#14749=CARTESIAN_POINT ( 'NONE',  ( 11.32299956498189886, 2.792989229543000107, -7.174999999999999822 ) ) ;
#14753=CARTESIAN_POINT ( 'NONE',  ( 11.33872066707849768, 4.858611803369300652, -6.980638253271099103 ) ) ;
#14756=CARTESIAN_POINT ( 'NONE',  ( 9.630633995698000049, 5.271405458160000279, -7.641111829547599932 ) ) ;
#14767=CARTESIAN_POINT ( 'NONE',  ( 8.846962924124625260, 4.841836872161519700, -7.738417548727159812 ) ) ;
#14835=CARTESIAN_POINT ( 'NONE',  ( 9.712659112603999390, 3.623260508844300176, -8.280881105104999307 ) ) ;
#14840=CARTESIAN_POINT ( 'NONE',  ( 9.758513540182331525, 4.163624617374472869, -6.250000000000000888 ) ) ;
#14855=VERTEX_POINT ( 'NONE', #16765 ) ;
#14866=CARTESIAN_POINT ( 'NONE',  ( 10.56080513895999928, 5.026880838510000338, -6.929150654994399083 ) ) ;
#14886=EDGE_LOOP ( 'NONE', ( #527, #21062, #55765, #161, #31287, #16843, #5784, #18521, #16076, #54341, #54404 ) ) ;
#14913=ADVANCED_FACE ( 'NONE', ( #63015 ), #54177, .T. ) ;
#14918=CARTESIAN_POINT ( 'NONE',  ( 11.65456516821461008, 4.802916961510000249, -8.310318115935698913 ) ) ;
#14920=CARTESIAN_POINT ( 'NONE',  ( 9.197076168957998732, 3.560025096655699883, -8.247081005603298820 ) ) ;
#14956=CARTESIAN_POINT ( 'NONE',  ( 11.26723293495529887, 2.826061044294000180, -7.452807962566580180 ) ) ;
#14988=ORIENTED_EDGE ( 'NONE', *, *, #7441, .F. ) ;
#14998=VECTOR ( 'NONE', #18559, 1000.000000000000000 ) ;
#15000=CARTESIAN_POINT ( 'NONE',  ( 10.61656919669529842, 5.225637333137999718, -7.862118085997298778 ) ) ;
#15092=CARTESIAN_POINT ( 'NONE',  ( 10.47718582084299932, 3.343463760027599818, -6.741111985563299491 ) ) ;
#15095=CARTESIAN_POINT ( 'NONE',  ( 10.11188779216199940, 5.183207142131999845, -7.926693309523199282 ) ) ;
#15102=DIRECTION ( 'NONE',  ( -1.000000000000000000, 0.000000000000000000, 0.000000000000000000 ) ) ;
#15172=CARTESIAN_POINT ( 'NONE',  ( 10.63880513895979973, 5.150451045932999961, -6.860457220153399760 ) ) ;
#15173=CARTESIAN_POINT ( 'NONE',  ( 8.876797255587998592, 4.866234952405400271, -7.463326341748410364 ) ) ;
#15227=CARTESIAN_POINT ( 'NONE',  ( 11.25740844561608611, 5.045781347359230118, -7.175000373111195984 ) ) ;
#15263=CARTESIAN_POINT ( 'NONE',  ( 11.25656651104150008, 4.126085365637900182, -6.228222165170999247 ) ) ;
#15266=CARTESIAN_POINT ( 'NONE',  ( 10.00760887879199856, 3.803658216258800184, -6.655513263298900029 ) ) ;
#15288=VECTOR ( 'NONE', #34486, 1000.000000000000114 ) ;
#15306=CARTESIAN_POINT ( 'NONE',  ( 10.76857802013509868, 2.825431102905000103, -7.472656658230009796 ) ) ;
#15351=CARTESIAN_POINT ( 'NONE',  ( 11.60000000000000320, 4.738901876697420690, -8.470724288896152032 ) ) ;
#15386=CARTESIAN_POINT ( 'NONE',  ( 9.435596873515667227, 2.907767014557176566, -8.129523725463622341 ) ) ;
#15440=CARTESIAN_POINT ( 'NONE',  ( 11.46179707368349909, 3.501542828836900156, -6.629085939160999530 ) ) ;
#15443=CARTESIAN_POINT ( 'NONE',  ( 8.921417874593998931, 2.822750429186000165, -8.000467616829000761 ) ) ;
#15506=ORIENTED_EDGE ( 'NONE', *, *, #38048, .T. ) ;
#15521=CARTESIAN_POINT ( 'NONE',  ( 11.68277869730536977, 3.468607053297499743, -6.452143920160000157 ) ) ;
#15522=CARTESIAN_POINT ( 'NONE',  ( 8.902126402770997871, 4.811247217215600003, -7.194081880505399873 ) ) ;
#15548=DIRECTION ( 'NONE',  ( -1.000000000000000000, 0.000000000000000000, 0.000000000000000000 ) ) ;
#15558=CARTESIAN_POINT ( 'NONE',  ( 11.59603632436369125, 3.157359628034400068, -7.303218851299499548 ) ) ;
#15607=CARTESIAN_POINT ( 'NONE',  ( 10.84226088462129844, 4.002427228022017225, -6.359261544073000039 ) ) ;
#15609=CARTESIAN_POINT ( 'NONE',  ( 9.551684229509998403, 3.388828644390000200, -6.885038603985500494 ) ) ;
#15626=CARTESIAN_POINT ( 'NONE',  ( 9.143927823787141307, 5.249988444743199700, -7.499999844943244121 ) ) ;
#15640=CARTESIAN_POINT ( 'NONE',  ( 11.00000000000000000, 5.079754677601000523, -7.825000000000000178 ) ) ;
#15645=CARTESIAN_POINT ( 'NONE',  ( 11.51656039236534923, 5.173498198882000132, -7.557111631074219460 ) ) ;
#15688=CARTESIAN_POINT ( 'NONE',  ( 10.41964694612699915, 2.813019656517000477, -7.973702485506099613 ) ) ;
#15721=CARTESIAN_POINT ( 'NONE',  ( 10.84606641549978256, 4.838299037060044938, -7.747677868960886727 ) ) ;
#15727=CARTESIAN_POINT ( 'NONE',  ( 9.466846873515667227, 3.231816600031355069, -8.499583552997723501 ) ) ;
#15776=CARTESIAN_POINT ( 'NONE',  ( 9.201101285863998669, 3.264788442324599860, -6.626387721327399838 ) ) ;
#15777=CARTESIAN_POINT ( 'NONE',  ( 10.40333997687999990, 4.213854445120500003, -6.519583185858300212 ) ) ;
#15781=CARTESIAN_POINT ( 'NONE',  ( 9.301355082327999568, 3.427502311996299955, -6.356045986629998978 ) ) ;
#15835=CARTESIAN_POINT ( 'NONE',  ( 10.21684687351595677, 4.768183399968648040, -6.500416447002277387 ) ) ;
#15854=EDGE_CURVE ( 'NONE', #57059, #44304, #49364, .T. ) ;
#15855=ADVANCED_FACE ( 'NONE', ( #3749 ), #19153, .F. ) ;
#15857=CARTESIAN_POINT ( 'NONE',  ( 9.079430433046999482, 3.262177192690499883, -7.044669955395099770 ) ) ;
#15862=CARTESIAN_POINT ( 'NONE',  ( 9.873096873515667227, 2.782534154164606921, -7.172815144550898303 ) ) ;
#15890=CARTESIAN_POINT ( 'NONE',  ( 10.39969598649000027, 4.888000489779200208, -8.028730309000598808 ) ) ;
#15945=CARTESIAN_POINT ( 'NONE',  ( 11.60118044953561878, 5.133201153721000054, -8.090905336380599167 ) ) ;
#15948=CARTESIAN_POINT ( 'NONE',  ( 10.33688779216199904, 4.801941500727100021, -7.789199634454999632 ) ) ;
#15957=ORIENTED_EDGE ( 'NONE', *, *, #66296, .F. ) ;
#15985=CARTESIAN_POINT ( 'NONE',  ( 10.56591429142999949, 4.019686495353769651, -6.466681092390999197 ) ) ;
#16017=CARTESIAN_POINT ( 'NONE',  ( 8.790860954911998704, 4.097566467530549872, -8.421893466755800972 ) ) ;
#16024=AXIS2_PLACEMENT_3D ( 'NONE', #23960, #23611, #2633 ) ;
#16025=CARTESIAN_POINT ( 'NONE',  ( 11.83518044953559922, 4.768048975940600620, -7.900497508315099893 ) ) ;
#16055=CARTESIAN_POINT ( 'NONE',  ( 10.37837607040047594, 4.867967756586605965, -7.396454632467190926 ) ) ;
#16061=CARTESIAN_POINT ( 'NONE',  ( 9.560596873515667227, 4.629523725463624118, -8.592232985442823434 ) ) ;
#16071=CARTESIAN_POINT ( 'NONE',  ( 10.64393020684969926, 5.250000000000000000, -7.500000000000000000 ) ) ;
#16076=ORIENTED_EDGE ( 'NONE', *, *, #7655, .F. ) ;
#16111=CARTESIAN_POINT ( 'NONE',  ( 11.55610404293055993, 3.497163090439000310, -8.523936114709998790 ) ) ;
#16117=CARTESIAN_POINT ( 'NONE',  ( 9.099784697134998268, 4.619613413415000203, -6.540930833646799947 ) ) ;
#16119=CARTESIAN_POINT ( 'NONE',  ( 11.30995122972050027, 4.452766304612699955, -6.452959986593999275 ) ) ;
#16122=CARTESIAN_POINT ( 'NONE',  ( 10.03590035061499997, 4.340961869598300105, -8.732935057095000175 ) ) ;
#16180=CARTESIAN_POINT ( 'NONE',  ( 10.14393020684899938, 5.250000000000000000, -7.500000000000000000 ) ) ;
#16202=CARTESIAN_POINT ( 'NONE',  ( 10.26788779216199821, 4.929030047862200448, -7.835030859477799758 ) ) ;
#16223=CARTESIAN_POINT ( 'NONE',  ( 11.71210404293059959, 3.618181340822599790, -8.277504409418298792 ) ) ;
#16234=CARTESIAN_POINT ( 'NONE',  ( 11.44366954483529852, 4.485203148598100320, -6.751356298874699569 ) ) ;
#16271=ADVANCED_FACE ( 'NONE', ( #36524 ), #20789, .T. ) ;
#16287=CARTESIAN_POINT ( 'NONE',  ( 10.32533997688000049, 4.243109097101799954, -6.385465081946999355 ) ) ;
#16291=CARTESIAN_POINT ( 'NONE',  ( 9.526355082327999213, 3.611978631017199959, -6.724663065681199647 ) ) ;
#16307=CARTESIAN_POINT ( 'NONE',  ( 9.248087964304161801, 4.327168543240617282, -6.282577178243121452 ) ) ;
#16343=CARTESIAN_POINT ( 'NONE',  ( 10.73976354018279977, 3.672815144550903632, -6.282534154164605589 ) ) ;
#16368=CARTESIAN_POINT ( 'NONE',  ( 11.26902897915239876, 4.221721321201099997, -8.337339982364900592 ) ) ;
#16399=CARTESIAN_POINT ( 'NONE',  ( 10.87068169682078178, 4.873909797778569697, -7.480731692978241476 ) ) ;
#16405=CARTESIAN_POINT ( 'NONE',  ( 9.602263540182329749, 5.092232985442822546, -8.129523725463620565 ) ) ;
#16451=CARTESIAN_POINT ( 'NONE',  ( 11.69559063708295987, 5.086518862378000883, -7.805482129094999166 ) ) ;
#16457=CARTESIAN_POINT ( 'NONE',  ( 10.69456919669529960, 5.093991349577000172, -7.823222900359999343 ) ) ;
#16460=CARTESIAN_POINT ( 'NONE',  ( 8.516151519676999015, 4.027664626136379766, -8.778912113473998247 ) ) ;
#16465=B_SPLINE_CURVE_WITH_KNOTS ( 'NONE', 3,
 ( #48041, #21463, #63765, #31976, #4688, #68316 ),
 .UNSPECIFIED., .F., .F.,
 ( 4, 2, 4 ),
 ( 0.000000000000000000, 0.5000000000000000000, 1.000000000000000000 ),
 .UNSPECIFIED. ) ;
#16545=CARTESIAN_POINT ( 'NONE',  ( 11.42834208742529967, 3.293478249981899975, -8.610579932818998472 ) ) ;
#16546=CARTESIAN_POINT ( 'NONE',  ( 9.913279731609000223, 4.090130512164860122, -6.499640669006000238 ) ) ;
#16569=CARTESIAN_POINT ( 'NONE',  ( 10.97364560330029981, 4.265439025801100570, -6.675475461903199736 ) ) ;
#16574=ORIENTED_EDGE ( 'NONE', *, *, #37918, .F. ) ;
#16582=CARTESIAN_POINT ( 'NONE',  ( 10.61257802013489737, 3.108115747127599970, -7.479237407015119743 ) ) ;
#16607=CARTESIAN_POINT ( 'NONE',  ( 11.59999999999999964, 4.016704963253245886, -6.452290402036156891 ) ) ;
#16612=CARTESIAN_POINT ( 'NONE',  ( 8.719914745407999490, 3.934662526658240012, -8.403568966271999230 ) ) ;
#16620=CARTESIAN_POINT ( 'NONE',  ( 11.16486084871730000, 5.207010770456999893, -7.174999999999999822 ) ) ;
#16632=CARTESIAN_POINT ( 'NONE',  ( 10.64533863405319991, 4.703785194191100416, -8.397761948794601139 ) ) ;
#16681=ORIENTED_EDGE ( 'NONE', *, *, #50834, .T. ) ;
#16708=CARTESIAN_POINT ( 'NONE',  ( 11.81056516821459823, 4.609678151793300316, -8.115298063151199059 ) ) ;
#16744=CARTESIAN_POINT ( 'NONE',  ( 9.404346873515669003, 2.750000000000000000, -7.663624617374465764 ) ) ;
#16765=CARTESIAN_POINT ( 'NONE',  ( 11.32299956498189886, 2.792989229543000107, -7.174999999999999822 ) ) ;
#16792=CARTESIAN_POINT ( 'NONE',  ( 10.40333997687999990, 4.213854445120500003, -6.519583185858300212 ) ) ;
#16798=CARTESIAN_POINT ( 'NONE',  ( 11.53148876160955005, 3.209326035813000022, -8.322268080792200706 ) ) ;
#16843=ORIENTED_EDGE ( 'NONE', *, *, #44885, .F. ) ;
#16857=CARTESIAN_POINT ( 'NONE',  ( 10.74809687351632448, 4.327184855449106138, -6.282534154164607365 ) ) ;
#16862=CARTESIAN_POINT ( 'NONE',  ( 10.19601354018254291, 4.999583552997727054, -6.731816600031361730 ) ) ;
#16863=EDGE_CURVE ( 'NONE', #14127, #8973, #34406, .T. ) ;
#16884=CARTESIAN_POINT ( 'NONE',  ( 11.83518044953559922, 4.768048975940600620, -7.900497508315099893 ) ) ;
#16886=CARTESIAN_POINT ( 'NONE',  ( 10.85679632507500081, 4.490665650747399873, -8.409605917786398877 ) ) ;
#16887=CARTESIAN_POINT ( 'NONE',  ( 9.685317406968998455, 4.186809223719299311, -8.486886322867700727 ) ) ;
#16905=CARTESIAN_POINT ( 'NONE',  ( 11.81056516821459823, 4.609678151793300316, -8.115298063151199059 ) ) ;
#16929=FACE_OUTER_BOUND ( 'NONE', #13198, .T. ) ;
#16943=CARTESIAN_POINT ( 'NONE',  ( 11.60000000000000142, 4.247874375640066980, -6.451199048602686226 ) ) ;
#16971=CARTESIAN_POINT ( 'NONE',  ( 10.32118582084299874, 3.163839350524900063, -6.533484739457099622 ) ) ;
#17014=CARTESIAN_POINT ( 'NONE',  ( 11.36056039236529891, 4.891071240644300211, -7.543366519014379712 ) ) ;
#17019=CARTESIAN_POINT ( 'NONE',  ( 10.53521345716899837, 4.924890298941200228, -8.340879262988799780 ) ) ;
#17022=VECTOR ( 'NONE', #17527, 1000.000000000000000 ) ;
#17027=CARTESIAN_POINT ( 'NONE',  ( 10.70851354018270030, 4.163624617374472869, -6.250000000000001776 ) ) ;
#17053=CARTESIAN_POINT ( 'NONE',  ( 10.38287885159599888, 4.860099138268600072, -7.397393329751199786 ) ) ;
#17132=EDGE_LOOP ( 'NONE', ( #17163, #53582, #14120, #30196 ) ) ;
#17139=CARTESIAN_POINT ( 'NONE',  ( 10.69872335273220010, 4.349306362047499874, -8.440710326446700051 ) ) ;
#17147=CARTESIAN_POINT ( 'NONE',  ( 11.11302897915239818, 4.291996373817799970, -8.602736702002999891 ) ) ;
#17163=ORIENTED_EDGE ( 'NONE', *, *, #53955, .F. ) ;
#17206=VERTEX_POINT ( 'NONE', #17721 ) ;
#17207=CARTESIAN_POINT ( 'NONE',  ( 10.75851354018298522, 4.163624617374472869, -6.250000000000000888 ) ) ;
#17215=CARTESIAN_POINT ( 'NONE',  ( 10.11496314287999887, 5.251703735191999733, -7.236139910592400248 ) ) ;
#17239=CARTESIAN_POINT ( 'NONE',  ( 10.47769598648999967, 5.009476315410999803, -8.101059042556599366 ) ) ;
#17240=CARTESIAN_POINT ( 'NONE',  ( 8.900113844317997902, 4.253652595614200393, -6.528144732449299603 ) ) ;
#17253=APPLICATION_CONTEXT ( 'automotive_design' ) ;
#17262=CARTESIAN_POINT ( 'NONE',  ( 10.89979975933730039, 4.819074589197400726, -7.218192605361100078 ) ) ;
#17324=CARTESIAN_POINT ( 'NONE',  ( 8.737760194560388882, 3.933854210954582431, -8.370465981241707709 ) ) ;
#17327=CARTESIAN_POINT ( 'NONE',  ( 10.59195391537400077, 5.057233422790000432, -8.218034727798299244 ) ) ;
#17370=CARTESIAN_POINT ( 'NONE',  ( 10.77879632507499785, 4.423544049216699747, -8.285174533868300273 ) ) ;
#17382=CARTESIAN_POINT ( 'NONE',  ( 10.59393020684899867, 5.250000000000000000, -7.500000000000000000 ) ) ;
#17411=CARTESIAN_POINT ( 'NONE',  ( 10.85056919669530018, 4.830699382454300306, -7.745432529082900253 ) ) ;
#17413=CARTESIAN_POINT ( 'NONE',  ( 10.44222949779799947, 4.633452903845899584, -8.449985803660998940 ) ) ;
#17488=CARTESIAN_POINT ( 'NONE',  ( 11.01811411617009817, 2.973039408543999951, -7.825000000000000178 ) ) ;
#17498=CARTESIAN_POINT ( 'NONE',  ( 11.40841235500449891, 3.158861363519000154, -6.729431436870699557 ) ) ;
#17506=CARTESIAN_POINT ( 'NONE',  ( 10.34995525820099971, 3.892289273474800471, -6.364355462479999836 ) ) ;
#17527=DIRECTION ( 'NONE',  ( -1.000000000000000000, 0.000000000000000000, 0.000000000000000000 ) ) ;
#17569=CARTESIAN_POINT ( 'NONE',  ( 10.14029229006299992, 5.106256438265999620, -6.857675253263499471 ) ) ;
#17593=CARTESIAN_POINT ( 'NONE',  ( 10.44999293566599974, 4.720032669050099550, -8.383280442119700027 ) ) ;
#17594=CARTESIAN_POINT ( 'NONE',  ( 9.837292290062999101, 4.868609929059700470, -6.995659746333000584 ) ) ;
#17600=B_SPLINE_CURVE_WITH_KNOTS ( 'NONE', 3,
 ( #8144, #60251, #44871, #45214, #50109, #61286, #12699, #2548, #39969, #6751, #13402, #7446, #34383, #50800, #66175, #28796, #55701, #18639, #29138, #50446, #12353, #22835, #65480, #33341, #29493, #33686, #38572, #2892, #54656, #60593, #28090, #49404, #55003, #28442, #1866, #65826, #23529, #34037, #2215, #62311, #52157, #24906, #20009, #51814, #36084, #14428, #57399, #8488, #41334, #3241, #13737, #40303, #40988, #3912, #62641, #20346, #8828, #9504, #19313, #14767, #35070, #30846, #14083, #68227, #4260 ),
 .UNSPECIFIED., .F., .F.,
 ( 4, 1, 1, 1, 1, 1, 1, 1, 1, 1, 1, 1, 1, 1, 1, 1, 1, 1, 1, 1, 1, 1, 1, 1, 1, 1, 1, 1, 1, 1, 1, 1, 1, 1, 1, 1, 1, 1, 1, 1, 1, 1, 1, 1, 1, 1, 1, 1, 1, 1, 1, 1, 1, 1, 1, 1, 1, 1, 1, 1, 1, 1, 4 ),
 ( 0.000000000000000000, 0.01249986222369741350, 0.02874986775682985066, 0.04499987328996228608, 0.06124987882309472498, 0.07749988435622716387, 0.09374988988935960277, 0.1099998954224920417, 0.1262499009556244944, 0.1424999064887569056, 0.1587499120218893722, 0.1749999175550217834, 0.1912499230881542500, 0.2074999286212866612, 0.2237499341544191278, 0.2399999396875515389, 0.2562499452206840056, 0.2724999507538165000, 0.2887499562869488834, 0.3049999618200813223, 0.3212499673532137612, 0.3374999728863462556, 0.3537499784194786390, 0.3699999839526110779, 0.3862499894857435168, 0.4024999950188760112, 0.4187500005520083945, 0.4350000060851408334, 0.4512500116182732723, 0.4675000171514057667, 0.4837500226845381501, 0.5000000282176706445, 0.5162500337508029169, 0.5325000392839354113, 0.5487500448170677947, 0.5650000503502002891, 0.5812500558833327835, 0.5975000614164651669, 0.6137500669495976613, 0.6300000724827300447, 0.6462500780158624281, 0.6625000835489949225, 0.6787500890821273059, 0.6950000946152598003, 0.7112501001483922947, 0.7275001056815246780, 0.7437501112146571725, 0.7600001167477895558, 0.7762501222809219392, 0.7925001278140544336, 0.8087501333471868170, 0.8250001388803193114, 0.8412501444134518058, 0.8575001499465841892, 0.8737501554797166836, 0.8900001610128490670, 0.9062501665459814504, 0.9225001720791139448, 0.9387501776122463282, 0.9550001831453788226, 0.9712501886785112060, 0.9875001942116437004, 1.000000000000000000 ),
 .UNSPECIFIED. ) ;
#17619=CARTESIAN_POINT ( 'NONE',  ( 10.99410672858429905, 3.198097575668700010, -6.896755974168000236 ) ) ;
#17715=CARTESIAN_POINT ( 'NONE',  ( 10.97124174884019965, 3.963805917081910213, -8.815770025351000072 ) ) ;
#17721=CARTESIAN_POINT ( 'NONE',  ( 10.84393020684979980, 2.750000000000000000, -7.500000000000000000 ) ) ;
#17729=VERTEX_POINT ( 'NONE', #30792 ) ;
#17731=B_SPLINE_CURVE_WITH_KNOTS ( 'NONE', 3,
 ( #15626, #32741, #41849, #58271, #20868, #42885, #36957, #16307, #63155, #68400, #10373, #42206, #54057, #48475, #37293, #27154, #234, #58964 ),
 .UNSPECIFIED., .F., .F.,
 ( 4, 2, 2, 2, 2, 2, 2, 2, 4 ),
 ( 0.1494581667962512628, 0.2557758959467198445, 0.3620936250971884540, 0.4684113542476570080, 0.5747290833981256730, 0.6810468125485942270, 0.7873645416990627810, 0.8936822708495314460, 1.000000000000000000 ),
 .UNSPECIFIED. ) ;
#17740=CARTESIAN_POINT ( 'NONE',  ( 11.57299956498156845, 5.207010770456999893, -7.825000000000000178 ) ) ;
#17766=CARTESIAN_POINT ( 'NONE',  ( 10.89979975933730039, 4.819074589197400726, -7.218192605361100078 ) ) ;
#17769=CARTESIAN_POINT ( 'NONE',  ( 9.960975701332998256, 4.837683410033799980, -8.275900091855099561 ) ) ;
#17849=CARTESIAN_POINT ( 'NONE',  ( 11.05964426047339799, 4.687693494822500639, -8.577215873335999774 ) ) ;
#17856=CARTESIAN_POINT ( 'NONE',  ( 11.08425954179440076, 4.982976321082899673, -8.316745941391600283 ) ) ;
#17932=CARTESIAN_POINT ( 'NONE',  ( 9.979346873516126593, 4.163624617374466652, -8.749999999999998224 ) ) ;
#17938=CARTESIAN_POINT ( 'NONE',  ( 11.04749144726329924, 3.499163784537000055, -6.793273974143599681 ) ) ;
#17940=CARTESIAN_POINT ( 'NONE',  ( 11.10101463001529964, 4.622233839778099984, -6.503413421344399481 ) ) ;
#17942=CARTESIAN_POINT ( 'NONE',  ( 9.381367640780998940, 4.473477001189199775, -6.614188603779100006 ) ) ;
#17965=CARTESIAN_POINT ( 'NONE',  ( 11.33872066707849768, 4.858611803369300652, -6.980638253271099103 ) ) ;
#17973=CARTESIAN_POINT ( 'NONE',  ( 11.56914347478616634, 4.748726180097643912, -8.529874251157636422 ) ) ;
#18032=CARTESIAN_POINT ( 'NONE',  ( 10.81349144726329925, 3.261052100888700345, -6.457276458983999490 ) ) ;
#18035=CARTESIAN_POINT ( 'NONE',  ( 8.842468108405999061, 4.834201109053600121, -7.736255015838599647 ) ) ;
#18059=CARTESIAN_POINT ( 'NONE',  ( 10.76346886766499900, 3.365322927604099679, -6.346853961441000003 ) ) ;
#18081=CARTESIAN_POINT ( 'NONE',  ( 11.48052502238429895, 5.045683737783986267, -7.824990984965952912 ) ) ;
#18108=CARTESIAN_POINT ( 'NONE',  ( 11.09256785386839894, 3.167490253789400523, -8.060248494254899754 ) ) ;
#18112=CARTESIAN_POINT ( 'NONE',  ( 10.31558376188599802, 3.037118682679400106, -8.113672563022399586 ) ) ;
#18146=VERTEX_POINT ( 'NONE', #8012 ) ;
#18150=CARTESIAN_POINT ( 'NONE',  ( 10.92968717260509948, 3.312350236372100021, -8.622362941748999532 ) ) ;
#18190=CARTESIAN_POINT ( 'NONE',  ( 10.54687750876899877, 3.382085645339300228, -8.458891008702400072 ) ) ;
#18198=CARTESIAN_POINT ( 'NONE',  ( 10.54272335273199879, 4.444874504667400750, -8.698083075453000745 ) ) ;
#18256=CARTESIAN_POINT ( 'NONE',  ( 8.876902336861421716, 4.269588175475919734, -6.500155937682548846 ) ) ;
#18257=SHAPE_REPRESENTATION_RELATIONSHIP ( 'NONE' , 'NONE' ,  #55423, #64411 ) ;
#18265=CARTESIAN_POINT ( 'NONE',  ( 11.33810207955129812, 4.796537143354000499, -7.825000000000000178 ) ) ;
#18283=CARTESIAN_POINT ( 'NONE',  ( 10.62903166480609940, 3.135947233695900227, -7.560921321260908989 ) ) ;
#18285=CARTESIAN_POINT ( 'NONE',  ( 10.77368717260499942, 3.460071470104900015, -8.381256426168800289 ) ) ;
#18286=CARTESIAN_POINT ( 'NONE',  ( 9.708633995697999453, 5.134843509922999871, -7.625954975973699312 ) ) ;
#18306=CARTESIAN_POINT ( 'NONE',  ( 10.57980110216399972, 3.260758259645400337, -7.048535450274799885 ) ) ;
#18334=B_SPLINE_CURVE_WITH_KNOTS ( 'NONE', 3,
 ( #55221, #7321, #49975, #699, #48943, #43701, #2090, #44745, #59421, #38446, #61837, #45085, #56598, #56255, #51351, #57268, #67752, #30048 ),
 .UNSPECIFIED., .F., .F.,
 ( 4, 2, 2, 2, 2, 2, 2, 2, 4 ),
 ( 0.000000000000000000, 0.1250000000000000000, 0.2500000000000000000, 0.3750000000000000000, 0.5000000000000000000, 0.6250000000000000000, 0.7500000000000000000, 0.8750000000000000000, 1.000000000000000000 ),
 .UNSPECIFIED. ) ;
#18341=DIRECTION ( 'NONE',  ( 1.000000000000000000, 0.000000000000000000, 0.000000000000000000 ) ) ;
#18350=ORIENTED_EDGE ( 'NONE', *, *, #20871, .F. ) ;
#18373=CARTESIAN_POINT ( 'NONE',  ( 10.73964560330029983, 4.391636236366600166, -6.283473206644000442 ) ) ;
#18404=CARTESIAN_POINT ( 'NONE',  ( 11.80233327354039830, 2.898463260143000042, -6.779499720266399798 ) ) ;
#18428=CARTESIAN_POINT ( 'NONE',  ( 11.03482133862663517, 4.942979055179590908, -8.373613860257943742 ) ) ;
#18450=CARTESIAN_POINT ( 'NONE',  ( 10.72749279009019929, 3.774717370312400178, -8.336388861178200216 ) ) ;
#18455=CARTESIAN_POINT ( 'NONE',  ( 9.477709346417000802, 4.907312911337299965, -7.069157126958599768 ) ) ;
#18496=CARTESIAN_POINT ( 'NONE',  ( 11.59456039236534330, 5.314711678001000195, -7.563984187103470092 ) ) ;
#18521=ORIENTED_EDGE ( 'NONE', *, *, #36470, .F. ) ;
#18535=CARTESIAN_POINT ( 'NONE',  ( 10.89149144726329865, 3.340422662105400065, -6.569275630703699242 ) ) ;
#18545=CARTESIAN_POINT ( 'NONE',  ( 10.61656919669529842, 5.225637333137999718, -7.862118085997298778 ) ) ;
#18559=DIRECTION ( 'NONE',  ( -1.000000000000000000, 0.000000000000000000, 2.886579864060000134E-14 ) ) ;
#18627=CARTESIAN_POINT ( 'NONE',  ( 10.28441772631199846, 4.372518460886800185, -8.266796319406900295 ) ) ;
#18629=CARTESIAN_POINT ( 'NONE',  ( 10.86190547754509872, 4.891676932241900033, -7.528299448264639260 ) ) ;
#18630=CARTESIAN_POINT ( 'NONE',  ( 8.948759580228999866, 2.889471124893000287, -7.234556850645999404 ) ) ;
#18639=CARTESIAN_POINT ( 'NONE',  ( 9.910787105781626138, 4.756649759826824919, -7.060667085372605456 ) ) ;
#18649=CARTESIAN_POINT ( 'NONE',  ( 11.43718179236249988, 3.790319673775199849, -6.518682001772900136 ) ) ;
#18658=CARTESIAN_POINT ( 'NONE',  ( 11.44571737393083133, 2.988799872700407700, -8.273761053885758443 ) ) ;
#18676=CARTESIAN_POINT ( 'NONE',  ( 10.00551210286899995, 3.782771630962269871, -8.756187319522087620 ) ) ;
#18741=DIRECTION ( 'NONE',  ( 0.000000000000000000, 1.000000000000000000, 0.000000000000000000 ) ) ;
#18748=CARTESIAN_POINT ( 'NONE',  ( 11.76077869730539938, 3.404661623424200201, -6.326049646822999861 ) ) ;
#18760=ADVANCED_FACE ( 'NONE', ( #815 ), #12364, .F. ) ;
#18799=CARTESIAN_POINT ( 'NONE',  ( 10.69872335273220010, 4.349306362047499874, -8.440710326446700051 ) ) ;
#18801=CARTESIAN_POINT ( 'NONE',  ( 9.173759580228997734, 3.023107159668900312, -7.266499081715599218 ) ) ;
#18880=CARTESIAN_POINT ( 'NONE',  ( 10.12841772631199966, 4.490588993294299947, -8.509834072393999804 ) ) ;
#18890=CARTESIAN_POINT ( 'NONE',  ( 10.64118447801629941, 5.277702140407999565, -7.471828720557429193 ) ) ;
#18911=CARTESIAN_POINT ( 'NONE',  ( 11.59999999999999964, 3.116215992411100366, -7.825000000000000178 ) ) ;
#18918=CARTESIAN_POINT ( 'NONE',  ( 11.01053724730969918, 3.051574408741400291, -7.174999999999999822 ) ) ;
#18930=CARTESIAN_POINT ( 'NONE',  ( 9.614763540183330903, 5.217465845835394411, -7.172815144550904520 ) ) ;
#18946=CARTESIAN_POINT ( 'NONE',  ( 9.355088727410999283, 2.725263018055000153, -7.606911245136100064 ) ) ;
#18949=ORIENTED_EDGE ( 'NONE', *, *, #38514, .T. ) ;
#18966=CARTESIAN_POINT ( 'NONE',  ( 10.94903032197929882, 4.503839166471300004, -6.795411691360399686 ) ) ;
#18968=CARTESIAN_POINT ( 'NONE',  ( 10.36325056272499978, 4.892034740700499817, -7.513220396995270001 ) ) ;
#18969=CARTESIAN_POINT ( 'NONE',  ( 8.771455549952998254, 4.888629236328500660, -6.783011486330899231 ) ) ;
#19014=ORIENTED_EDGE ( 'NONE', *, *, #28409, .T. ) ;
#19016=CARTESIAN_POINT ( 'NONE',  ( 8.734814475091132735, 4.056037006134289413, -8.383485082298649971 ) ) ;
#19020=DIRECTION ( 'NONE',  ( 0.000000000000000000, 0.000000000000000000, 1.000000000000000000 ) ) ;
#19074=CARTESIAN_POINT ( 'NONE',  ( 10.64391429142989765, 4.022379549362480766, -6.325326139450999641 ) ) ;
#19076=B_SPLINE_CURVE_WITH_KNOTS ( 'NONE', 3,
 ( #7600, #65972, #64929, #39420 ),
 .UNSPECIFIED., .F., .F.,
 ( 4, 4 ),
 ( 0.000000000000000000, 1.000000000000000000 ),
 .UNSPECIFIED. ) ;
#19097=CARTESIAN_POINT ( 'NONE',  ( 10.40434687351665310, 2.750000000000000000, -7.663624617374465764 ) ) ;
#19108=ORIENTED_EDGE ( 'NONE', *, *, #4512, .F. ) ;
#19126=CARTESIAN_POINT ( 'NONE',  ( 11.69559063708295987, 5.086518862378000883, -7.805482129094999166 ) ) ;
#19129=CARTESIAN_POINT ( 'NONE',  ( 9.984292290062997566, 4.868609929059700470, -6.995659746333000584 ) ) ;
#19148=ORIENTED_EDGE ( 'NONE', *, *, #67102, .T. ) ;
#19153=PLANE ( 'NONE',  #8665 ) ;
#19170=CARTESIAN_POINT ( 'NONE',  ( 11.83003632436370012, 2.756744593645999775, -7.209663534847899236 ) ) ;
#19188=CARTESIAN_POINT ( 'NONE',  ( 8.995772571291157149, 2.998508658148201889, -8.076234199639099387 ) ) ;
#19211=CARTESIAN_POINT ( 'NONE',  ( 10.91610672858429965, 3.088399709291500095, -6.814233985789400094 ) ) ;
#19219=CARTESIAN_POINT ( 'NONE',  ( 10.93656785386839836, 2.939720539848000413, -8.213529149347399638 ) ) ;
#19284=CARTESIAN_POINT ( 'NONE',  ( 9.709696787963999043, 4.219671260427300119, -6.239790126677999815 ) ) ;
#19301=CARTESIAN_POINT ( 'NONE',  ( 10.45672469555900008, 4.433465011431599656, -6.750062220519700062 ) ) ;
#19303=CARTESIAN_POINT ( 'NONE',  ( 10.61257802013489737, 3.108115747127599970, -7.479237407015119743 ) ) ;
#19304=CARTESIAN_POINT ( 'NONE',  ( 8.974088727410999056, 2.862182806015999947, -7.595427884080399927 ) ) ;
#19313=CARTESIAN_POINT ( 'NONE',  ( 8.872292071306626227, 4.874163933583397501, -7.462990653670714458 ) ) ;
#19362=EDGE_LOOP ( 'NONE', ( #11122, #39121, #32429, #63780, #68616, #63906, #46292 ) ) ;
#19422=CARTESIAN_POINT ( 'NONE',  ( 10.73213259636989925, 3.092475607087700418, -7.994504989494399361 ) ) ;
#19432=CARTESIAN_POINT ( 'NONE',  ( 10.08521345716899908, 4.924890298941200228, -8.340879262988799780 ) ) ;
#19470=DIRECTION ( 'NONE',  ( 1.000000000000000000, 0.000000000000000000, -0.000000000000000000 ) ) ;
#19474=CARTESIAN_POINT ( 'NONE',  ( 10.55103166480599874, 2.999015536536000504, -7.570575893572789816 ) ) ;
#19476=CARTESIAN_POINT ( 'NONE',  ( 9.427051052051998781, 4.985712601322500603, -7.692906630067099627 ) ) ;
#19484=VERTEX_POINT ( 'NONE', #23013 ) ;
#19518=CARTESIAN_POINT ( 'NONE',  ( 11.22056920625029974, 4.047312782235129802, -6.184582852561999466 ) ) ;
#19548=CARTESIAN_POINT ( 'NONE',  ( 9.143927823787141307, 5.249988444743199700, -7.499999844943244121 ) ) ;
#19562=CARTESIAN_POINT ( 'NONE',  ( 10.29657053952199952, 3.497746311184500190, -6.324815923923999605 ) ) ;
#19583=CARTESIAN_POINT ( 'NONE',  ( 9.099999931440999390, 4.000000000000000000, -7.500000000000000000 ) ) ;
#19598=ORIENTED_EDGE ( 'NONE', *, *, #60611, .F. ) ;
#19628=ORIENTED_EDGE ( 'NONE', *, *, #15854, .F. ) ;
#19635=CARTESIAN_POINT ( 'NONE',  ( 9.507063610504999929, 4.524705472883399970, -8.666648427848999248 ) ) ;
#19654=CARTESIAN_POINT ( 'NONE',  ( 10.52641638348499953, 3.025038519517300184, -7.262511127784999410 ) ) ;
#19659=CARTESIAN_POINT ( 'NONE',  ( 9.050076168957998490, 3.420574098817999786, -8.483869947211399420 ) ) ;
#19762=DIRECTION ( 'NONE',  ( -1.000000000000000000, 0.000000000000000000, 0.000000000000000000 ) ) ;
#19769=CARTESIAN_POINT ( 'NONE',  ( 11.39189666366029918, 3.947847673382490541, -8.673729056199000809 ) ) ;
#19820=CARTESIAN_POINT ( 'NONE',  ( 11.70379573085659786, 5.106255642043000087, -7.691418046581699919 ) ) ;
#19825=CARTESIAN_POINT ( 'NONE',  ( 9.680342523874998051, 3.007153757386999526, -7.348017636355000270 ) ) ;
#19860=CARTESIAN_POINT ( 'NONE',  ( 10.85679632507500081, 4.490665650747399873, -8.409605917786398877 ) ) ;
#19867=CARTESIAN_POINT ( 'NONE',  ( 9.489763540183334456, 4.327184855449099921, -8.717465845835395299 ) ) ;
#19883=EDGE_CURVE ( 'NONE', #20133, #509, #7535, .T. ) ;
#19953=VECTOR ( 'NONE', #29975, 1000.000000000000000 ) ;
#19993=CARTESIAN_POINT ( 'NONE',  ( 10.08351354018237345, 5.250000000000000888, -7.663624617374468428 ) ) ;
#19998=CARTESIAN_POINT ( 'NONE',  ( 10.64949279009019989, 3.739015461786900030, -8.468936491037499792 ) ) ;
#20001=CARTESIAN_POINT ( 'NONE',  ( 9.833267173155999075, 3.026371913119300316, -6.670281532133299329 ) ) ;
#20005=ORIENTED_EDGE ( 'NONE', *, *, #36051, .T. ) ;
#20009=CARTESIAN_POINT ( 'NONE',  ( 9.277558426223626142, 4.358884483112399622, -8.297956262399157623 ) ) ;
#20064=CARTESIAN_POINT ( 'NONE',  ( 8.599999952505998024, 3.250000006358199744, -7.500000000000000000 ) ) ;
#20077=CARTESIAN_POINT ( 'NONE',  ( 10.09259632033899834, 3.197262364844699611, -7.172402329663099430 ) ) ;
#20110=CARTESIAN_POINT ( 'NONE',  ( 11.06456920625009843, 4.037149028919880145, -6.467161360063999886 ) ) ;
#20128=DIRECTION ( 'NONE',  ( 0.000000000000000000, -1.000000000000000000, 0.000000000000000000 ) ) ;
#20133=VERTEX_POINT ( 'NONE', #10131 ) ;
#20160=CARTESIAN_POINT ( 'NONE',  ( 11.50687348028854906, 2.996540789803000315, -8.042549288197099244 ) ) ;
#20162=CARTESIAN_POINT ( 'NONE',  ( 9.247734463322998977, 4.090312251411040378, -8.362294405496898619 ) ) ;
#20198=CARTESIAN_POINT ( 'NONE',  ( 11.05946005378019947, 5.036385109519999403, -6.946587256304699309 ) ) ;
#20256=CARTESIAN_POINT ( 'NONE',  ( 10.09393020684899867, 5.250000000000000000, -7.500000000000000000 ) ) ;
#20267=DIRECTION ( 'NONE',  ( -1.000000000000000000, 0.000000000000000000, 0.000000000000000000 ) ) ;
#20289=CARTESIAN_POINT ( 'NONE',  ( 11.28627509987130040, 3.727547057523676433, -6.250000000000000000 ) ) ;
#20294=ORIENTED_EDGE ( 'NONE', *, *, #44885, .T. ) ;
#20312=CARTESIAN_POINT ( 'NONE',  ( 10.14393020684899938, 5.250000000000000000, -7.500000000000000000 ) ) ;
#20332=CARTESIAN_POINT ( 'NONE',  ( 11.09256785386839894, 3.167490253789400523, -8.060248494254899754 ) ) ;
#20335=CARTESIAN_POINT ( 'NONE',  ( 9.022734463322999332, 4.133249246727800141, -8.772253522581999974 ) ) ;
#20341=FACE_OUTER_BOUND ( 'NONE', #5858, .T. ) ;
#20342=DIRECTION ( 'NONE',  ( 0.000000000000000000, 0.000000000000000000, 1.000000000000000000 ) ) ;
#20346=CARTESIAN_POINT ( 'NONE',  ( 8.948279512853625661, 4.474797027487648293, -6.765085003841553757 ) ) ;
#20416=CARTESIAN_POINT ( 'NONE',  ( 10.68035971519489813, 4.678140486081599825, -6.371865185335000348 ) ) ;
#20417=CARTESIAN_POINT ( 'NONE',  ( 9.282063610504998508, 4.355629271815800507, -8.290718512198798962 ) ) ;
#20451=CARTESIAN_POINT ( 'NONE',  ( 11.35034208742529849, 3.369365911179700301, -8.491292290686200062 ) ) ;
#20504=CARTESIAN_POINT ( 'NONE',  ( 11.06379841651039797, 3.598362324325699912, -8.567697191971999970 ) ) ;
#20506=CARTESIAN_POINT ( 'NONE',  ( 10.05826717315599872, 3.340104753140699767, -6.937642277832399174 ) ) ;
#20546=CARTESIAN_POINT ( 'NONE',  ( 11.59966954483535773, 4.638989336656000440, -6.514072057539499916 ) ) ;
#20588=CARTESIAN_POINT ( 'NONE',  ( 10.09964828895399869, 5.121614868497999851, -8.112615456209400833 ) ) ;
#20680=CARTESIAN_POINT ( 'NONE',  ( 11.21564426047340035, 4.539962866738299851, -8.345807871442598724 ) ) ;
#20684=CARTESIAN_POINT ( 'NONE',  ( 10.01057120343299900, 3.937990586507050139, -8.777708647662999297 ) ) ;
#20692=VECTOR ( 'NONE', #42069, 1000.000000000000000 ) ;
#20742=CARTESIAN_POINT ( 'NONE',  ( 10.14393020684899938, 5.250000000000000000, -7.500000000000000000 ) ) ;
#20762=CARTESIAN_POINT ( 'NONE',  ( 10.52799293566599914, 4.806678152079100208, -8.489570425681801424 ) ) ;
#20763=CARTESIAN_POINT ( 'NONE',  ( 9.307392757686999474, 4.585219941293200208, -8.139707405630899117 ) ) ;
#20789=CYLINDRICAL_SURFACE ( 'NONE', #13379, 1.250000000000000222 ) ;
#20798=CARTESIAN_POINT ( 'NONE',  ( 11.36056039236529891, 4.891071240644300211, -7.543366519014379712 ) ) ;
#20851=CARTESIAN_POINT ( 'NONE',  ( 10.27610941423800028, 4.844410192686099847, -6.733017893878099791 ) ) ;
#20853=CARTESIAN_POINT ( 'NONE',  ( 9.019772138681998896, 3.677371150249499898, -6.695252480703800302 ) ) ;
#20868=CARTESIAN_POINT ( 'NONE',  ( 9.196006702408606515, 4.999605512837395516, -6.731788826750698007 ) ) ;
#20869=CARTESIAN_POINT ( 'NONE',  ( 10.12435795695566476, 5.250000000000000000, -7.807440182398264206 ) ) ;
#20871=EDGE_CURVE ( 'NONE', #37649, #59938, #5790, .T. ) ;
#20891=CARTESIAN_POINT ( 'NONE',  ( 11.14767835872009982, 3.125658946326500320, -6.948943352864199952 ) ) ;
#20898=CARTESIAN_POINT ( 'NONE',  ( 9.593930206849998754, 5.250000000000000000, -7.500000000000000000 ) ) ;
#20938=CARTESIAN_POINT ( 'NONE',  ( 10.19810941423799910, 4.946022705791000007, -6.640722727400100389 ) ) ;
#20973=CARTESIAN_POINT ( 'NONE',  ( 9.633513540182331525, 5.250000000000001776, -7.663624617374467540 ) ) ;
#20978=ORIENTED_EDGE ( 'NONE', *, *, #34974, .F. ) ;
#21025=CARTESIAN_POINT ( 'NONE',  ( 9.000480666858997836, 4.426512626096299918, -8.706015266875999359 ) ) ;
#21026=CARTESIAN_POINT ( 'NONE',  ( 11.04333729122639873, 2.996877626170000308, -7.473611442402849470 ) ) ;
#21029=CARTESIAN_POINT ( 'NONE',  ( 9.478659112603999404, 3.444147913214900214, -8.652134039551000910 ) ) ;
#21030=CARTESIAN_POINT ( 'NONE',  ( 11.07299956498199833, 5.207010770456999893, -7.825000000000000178 ) ) ;
#21062=ORIENTED_EDGE ( 'NONE', *, *, #27217, .F. ) ;
#21109=CARTESIAN_POINT ( 'NONE',  ( 9.484696787962999309, 4.148886440911999429, -6.645868410478299459 ) ) ;
#21115=CARTESIAN_POINT ( 'NONE',  ( 9.789763540182331525, 3.672815144550904076, -6.282534154164603812 ) ) ;
#21118=CARTESIAN_POINT ( 'NONE',  ( 8.807788144226000426, 4.090932644426789722, -8.453461841935100196 ) ) ;
#21134=CARTESIAN_POINT ( 'NONE',  ( 11.83518044953559922, 4.768048975940600620, -7.900497508315099893 ) ) ;
#21145=CARTESIAN_POINT ( 'NONE',  ( 10.69568717260499824, 3.533932086969799879, -8.260703168378098482 ) ) ;
#21153=ORIENTED_EDGE ( 'NONE', *, *, #8914, .T. ) ;
#21167=CARTESIAN_POINT ( 'NONE',  ( 11.39043504475232815, 2.929202812228125730, -8.202738646980327175 ) ) ;
#21191=CARTESIAN_POINT ( 'NONE',  ( 11.15810538575740019, 5.242981041160000188, -7.202822423614300362 ) ) ;
#21194=CARTESIAN_POINT ( 'NONE',  ( 9.880963142879998884, 4.848366390061300102, -7.321163726496699553 ) ) ;
#21212=CARTESIAN_POINT ( 'NONE',  ( 10.08521345716899908, 4.924890298941200228, -8.340879262988799780 ) ) ;
#21232=CARTESIAN_POINT ( 'NONE',  ( 11.02301463001509774, 4.547357026650399980, -6.623338154204899908 ) ) ;
#21240=CARTESIAN_POINT ( 'NONE',  ( 9.458513540183334456, 3.836375382625530239, -8.749999999999998224 ) ) ;
#21252=FACE_OUTER_BOUND ( 'NONE', #69094, .T. ) ;
#21274=CARTESIAN_POINT ( 'NONE',  ( 11.34287482311539996, 4.803125295093300551, -7.824481664695199790 ) ) ;
#21305=CARTESIAN_POINT ( 'NONE',  ( 10.82145113417867677, 4.723115832319042084, -7.991114136793449951 ) ) ;
#21356=CARTESIAN_POINT ( 'NONE',  ( 10.30487885159599770, 4.996404279947399552, -7.381132626649399064 ) ) ;
#21361=CARTESIAN_POINT ( 'NONE',  ( 10.21426717315699939, 3.130949526459800403, -6.759401780699699103 ) ) ;
#21363=CARTESIAN_POINT ( 'NONE',  ( 11.62994988689359843, 4.518136976474400157, -8.516279404258998653 ) ) ;
#21366=CARTESIAN_POINT ( 'NONE',  ( 9.757279731608999640, 4.114789684104199985, -6.225948307210999566 ) ) ;
#21388=DIRECTION ( 'NONE',  ( -1.000000000000000000, 0.000000000000000000, 0.000000000000000000 ) ) ;
#21402=ORIENTED_EDGE ( 'NONE', *, *, #14492, .T. ) ;
#21434=VERTEX_POINT ( 'NONE', #54113 ) ;
#21441=CARTESIAN_POINT ( 'NONE',  ( 11.26212378248529866, 3.384904051819500381, -6.336291382830999908 ) ) ;
#21442=CARTESIAN_POINT ( 'NONE',  ( 8.733265421555000074, 3.837285628664199866, -8.341695632489900092 ) ) ;
#21463=CARTESIAN_POINT ( 'NONE',  ( 8.798455008774128672, 4.948455060776569603, -7.736326407956449103 ) ) ;
#21466=CARTESIAN_POINT ( 'NONE',  ( 11.21979841651039855, 3.695024856201900132, -8.310733465454200442 ) ) ;
#21477=CARTESIAN_POINT ( 'NONE',  ( 10.86190547754509872, 4.891676932241900033, -7.528299448264639260 ) ) ;
#21481=ORIENTED_EDGE ( 'NONE', *, *, #9945, .T. ) ;
#21497=CARTESIAN_POINT ( 'NONE',  ( 8.978248830702483474, 4.955089878105851220, -8.117373328463406423 ) ) ;
#21504=CARTESIAN_POINT ( 'NONE',  ( 11.59999999999999964, 3.850275034462830259, -6.485689145701417857 ) ) ;
#21532=CARTESIAN_POINT ( 'NONE',  ( 10.44841638348500013, 2.891666689023999925, -7.230023356477299323 ) ) ;
#21534=CARTESIAN_POINT ( 'NONE',  ( 8.895138961223999274, 4.832207374954999857, -8.062381800110799190 ) ) ;
#21570=CARTESIAN_POINT ( 'NONE',  ( 10.32169598648999909, 4.766524664146899681, -7.956401575444799867 ) ) ;
#21613=CARTESIAN_POINT ( 'NONE',  ( 11.09672200990539892, 3.182132064022000328, -7.214709569664399247 ) ) ;
#21640=CARTESIAN_POINT ( 'NONE',  ( 10.33103907547007694, 4.774162136902415199, -7.899515915943056577 ) ) ;
#21693=CARTESIAN_POINT ( 'NONE',  ( 11.16225954179439839, 4.877394611789299894, -8.229019074832200076 ) ) ;
#21698=CARTESIAN_POINT ( 'NONE',  ( 9.834329965421998665, 3.206942993865000258, -8.321459087847200564 ) ) ;
#21700=CARTESIAN_POINT ( 'NONE',  ( 11.55610404293055993, 3.497163090439000310, -8.523936114709998790 ) ) ;
#21739=ORIENTED_EDGE ( 'NONE', *, *, #20871, .T. ) ;
#21756=SURFACE_STYLE_FILL_AREA ( #5679 ) ;
#21784=CARTESIAN_POINT ( 'NONE',  ( 11.22056920625029974, 4.047312782235129802, -6.184582852561999466 ) ) ;
#21786=CARTESIAN_POINT ( 'NONE',  ( 9.786633995697998856, 4.998281561686200192, -7.610798122400000310 ) ) ;
#21809=CARTESIAN_POINT ( 'NONE',  ( 10.99826088462129903, 4.001843064679911244, -6.633804182961699603 ) ) ;
#21819=CARTESIAN_POINT ( 'NONE',  ( 10.93210843320491676, 2.862311695598936723, -8.098394516494938244 ) ) ;
#21820=CARTESIAN_POINT ( 'NONE',  ( 11.56833327354034857, 3.253412192327699959, -7.011667014989399149 ) ) ;
#21838=CARTESIAN_POINT ( 'NONE',  ( 11.11486084871780022, 5.207010770456999893, -7.174999999999999822 ) ) ;
#21842=ORIENTED_EDGE ( 'NONE', *, *, #56665, .F. ) ;
#21851=EDGE_CURVE ( 'NONE', #41213, #46101, #2334, .T. ) ;
#21852=CARTESIAN_POINT ( 'NONE',  ( 8.698396402458998367, 3.630894432589700127, -8.298253663472900499 ) ) ;
#21872=CARTESIAN_POINT ( 'NONE',  ( 11.42887348028849992, 2.875789035466000065, -8.107837221875000111 ) ) ;
#21880=B_SPLINE_CURVE_WITH_KNOTS ( 'NONE', 3,
 ( #56416, #8519, #23222, #44569 ),
 .UNSPECIFIED., .F., .F.,
 ( 4, 4 ),
 ( 0.8163836489557121379, 1.000000000000000000 ),
 .UNSPECIFIED. ) ;
#21914=CARTESIAN_POINT ( 'NONE',  ( 11.27745123989519982, 4.410212499603100689, -8.292221125039500151 ) ) ;
#21937=ORIENTED_EDGE ( 'NONE', *, *, #40479, .F. ) ;
#22008=COLOUR_RGB ( '', 0.31764706, 0.68627451, 0.89019608) ;
#22035=CARTESIAN_POINT ( 'NONE',  ( 10.32949413291699869, 4.912929163218899831, -7.083453279150199400 ) ) ;
#22043=CARTESIAN_POINT ( 'NONE',  ( 10.79303032197930001, 4.663532080728800544, -6.572090902022299730 ) ) ;
#22081=CARTESIAN_POINT ( 'NONE',  ( 11.00000000000000000, 3.031410575668799900, -7.174999999999999822 ) ) ;
#22103=CARTESIAN_POINT ( 'NONE',  ( 10.87309687351627652, 2.782534154164606921, -7.172815144550898303 ) ) ;
#22132=CARTESIAN_POINT ( 'NONE',  ( 11.85979573085659844, 4.840012015667699785, -7.645349278262099979 ) ) ;
#22134=CARTESIAN_POINT ( 'NONE',  ( 11.06456920625009843, 4.037149028919880145, -6.467161360063999886 ) ) ;
#22135=CARTESIAN_POINT ( 'NONE',  ( 10.01459632033899894, 3.070047649444500149, -7.120485934352199564 ) ) ;
#22145=B_SPLINE_CURVE_WITH_KNOTS ( 'NONE', 3,
 ( #27195, #68103, #53418, #32101, #68792, #69144, #41547, #52376, #4472, #62857 ),
 .UNSPECIFIED., .F., .F.,
 ( 4, 2, 2, 2, 4 ),
 ( 0.000000000000000000, 0.2500000000000000000, 0.5000000000000000000, 0.7500000000000000000, 1.000000000000000000 ),
 .UNSPECIFIED. ) ;
#22154=FACE_OUTER_BOUND ( 'NONE', #23030, .T. ) ;
#22190=CARTESIAN_POINT ( 'NONE',  ( 8.905196823546312146, 4.608202637908532573, -8.372486832488423403 ) ) ;
#22223=CARTESIAN_POINT ( 'NONE',  ( 10.49349279008999858, 3.667611644732699627, -8.734031750754999379 ) ) ;
#22263=CARTESIAN_POINT ( 'NONE',  ( 10.36325056272499978, 4.892034740700499817, -7.513220396995270001 ) ) ;
#22386=CARTESIAN_POINT ( 'NONE',  ( 11.67918044953561996, 5.011483761127000669, -8.027436060358800418 ) ) ;
#22395=CARTESIAN_POINT ( 'NONE',  ( 10.86687616594229944, 3.655053560864600204, -6.412662853391999818 ) ) ;
#22467=ORIENTED_EDGE ( 'NONE', *, *, #35465, .F. ) ;
#22477=CARTESIAN_POINT ( 'NONE',  ( 11.30878751119029957, 2.958974835389999836, -8.044634158732998586 ) ) ;
#22478=CARTESIAN_POINT ( 'NONE',  ( 9.153405316139998860, 3.786750623988900166, -8.481512610189300361 ) ) ;
#22497=CARTESIAN_POINT ( 'NONE',  ( 11.19518313518939934, 3.462699341914400097, -8.179416362154199760 ) ) ;
#22518=CARTESIAN_POINT ( 'NONE',  ( 11.11486084871780022, 5.207010770456999893, -7.174999999999999822 ) ) ;
#22530=CARTESIAN_POINT ( 'NONE',  ( 9.075651506909604649, 5.234436409784954947, -7.567790861611047859 ) ) ;
#22541=CARTESIAN_POINT ( 'NONE',  ( 8.755358248830999557, 4.089987329977850194, -8.350279134800100422 ) ) ;
#22565=CARTESIAN_POINT ( 'NONE',  ( 11.01041369783139956, 3.935522326596939902, -8.776385133971000840 ) ) ;
#22597=DIRECTION ( 'NONE',  ( -1.000000000000000000, 0.000000000000000000, 0.000000000000000000 ) ) ;
#22605=CARTESIAN_POINT ( 'NONE',  ( 11.23589666366019912, 3.960399224793059947, -8.391246537305399045 ) ) ;
#22618=CARTESIAN_POINT ( 'NONE',  ( 10.66684687351590277, 4.768183399968648040, -6.500416447002280051 ) ) ;
#22645=CARTESIAN_POINT ( 'NONE',  ( 11.56025819896753859, 3.013900664291200293, -7.685900384398899554 ) ) ;
#22695=CARTESIAN_POINT ( 'NONE',  ( 10.50851354018319128, 3.836375382625529795, -8.749999999999998224 ) ) ;
#22713=AXIS2_PLACEMENT_3D ( 'NONE', #60332, #65566, #55085 ) ;
#22729=CARTESIAN_POINT ( 'NONE',  ( 10.25564828895399927, 4.880669054351300495, -7.981013126389099099 ) ) ;
#22737=CARTESIAN_POINT ( 'NONE',  ( 11.16225954179439839, 4.877394611789299894, -8.229019074832200076 ) ) ;
#22792=VERTEX_POINT ( 'NONE', #58174 ) ;
#22824=CARTESIAN_POINT ( 'NONE',  ( 10.48280513895999988, 4.903310631086600146, -6.997844089834400094 ) ) ;
#22825=CARTESIAN_POINT ( 'NONE',  ( 9.558671671056998775, 3.009461603020800347, -7.666361006367900188 ) ) ;
#22835=CARTESIAN_POINT ( 'NONE',  ( 9.809470517051625649, 4.641899585206984646, -8.094556297950068924 ) ) ;
#22847=CARTESIAN_POINT ( 'NONE',  ( 11.11718313518939816, 3.377550038693600154, -8.287087605365499599 ) ) ;
#22860=VECTOR ( 'NONE', #54910, 1000.000000000000000 ) ;
#22862=ORIENTED_EDGE ( 'NONE', *, *, #40479, .T. ) ;
#22879=VERTEX_POINT ( 'NONE', #10276 ) ;
#22889=CARTESIAN_POINT ( 'NONE',  ( 8.719734573340000239, 3.777330902948500047, -8.352506367884300786 ) ) ;
#22914=CARTESIAN_POINT ( 'NONE',  ( 8.715822372493999382, 3.750788346126100237, -8.315254653915399530 ) ) ;
#22940=FACE_OUTER_BOUND ( 'NONE', #27798, .T. ) ;
#22954=EDGE_CURVE ( 'NONE', #33345, #64314, #58560, .T. ) ;
#22965=FACE_OUTER_BOUND ( 'NONE', #45531, .T. ) ;
#22991=CARTESIAN_POINT ( 'NONE',  ( 10.40769129028899975, 3.110563525881361535, -8.413289387078531689 ) ) ;
#22993=CARTESIAN_POINT ( 'NONE',  ( 11.28949010443639978, 5.000675062740000065, -7.574834962826040297 ) ) ;
#22995=CARTESIAN_POINT ( 'NONE',  ( 10.46755864497999866, 4.898932057185599653, -8.204026508301600629 ) ) ;
#23013=CARTESIAN_POINT ( 'NONE',  ( 11.58810207955109917, 3.203462856645999945, -7.174999999999999822 ) ) ;
#23030=EDGE_LOOP ( 'NONE', ( #19148, #8961, #35301, #3756 ) ) ;
#23080=CARTESIAN_POINT ( 'NONE',  ( 11.13349010443639919, 5.274453806861999716, -7.595309363461700158 ) ) ;
#23088=CARTESIAN_POINT ( 'NONE',  ( 10.27195525820100031, 3.879327850572200198, -6.227697122196000024 ) ) ;
#23144=CARTESIAN_POINT ( 'NONE',  ( 8.863694533038728451, 4.511314481744639338, -6.614578276768176224 ) ) ;
#23150=CARTESIAN_POINT ( 'NONE',  ( 9.988317406969001055, 4.237919115995800290, -8.756892549790999070 ) ) ;
#23171=CARTESIAN_POINT ( 'NONE',  ( 11.21979841651039855, 3.695024856201900132, -8.310733465454200442 ) ) ;
#23173=CARTESIAN_POINT ( 'NONE',  ( 11.52166954483529793, 4.562096242626500597, -6.632714178206799538 ) ) ;
#23174=CARTESIAN_POINT ( 'NONE',  ( 9.634659112603999986, 3.563556310301200014, -8.404632083253700259 ) ) ;
#23198=CARTESIAN_POINT ( 'NONE',  ( 10.33364828895399867, 4.760196147278000112, -7.915211961479200475 ) ) ;
#23222=CARTESIAN_POINT ( 'NONE',  ( 8.801820635884373800, 4.060146622106553416, -8.450403350428134175 ) ) ;
#23223=CARTESIAN_POINT ( 'NONE',  ( 11.03443712336079940, 5.057168833716702672, -7.175021320887989162 ) ) ;
#23266=CARTESIAN_POINT ( 'NONE',  ( 10.78887616594230003, 3.613544262574699850, -6.281817606595999415 ) ) ;
#23318=ORIENTED_EDGE ( 'NONE', *, *, #34361, .T. ) ;
#23343=CARTESIAN_POINT ( 'NONE',  ( 10.51927318630899855, 4.756452637475340417, -8.526145288591962412 ) ) ;
#23345=CARTESIAN_POINT ( 'NONE',  ( 11.77359063708300013, 4.955772084214699724, -7.768721787835699999 ) ) ;
#23347=CARTESIAN_POINT ( 'NONE',  ( 9.631696787963999640, 4.196076320588900010, -6.375149554610999303 ) ) ;
#23389=CARTESIAN_POINT ( 'NONE',  ( 11.17901463001529905, 4.697110652903200290, -6.383488688482000128 ) ) ;
#23431=CARTESIAN_POINT ( 'NONE',  ( 10.64533863405319991, 4.703785194191100416, -8.397761948794601139 ) ) ;
#23438=CARTESIAN_POINT ( 'NONE',  ( 10.29657053952199952, 3.497746311184500190, -6.324815923923999605 ) ) ;
#23452=LINE ( 'NONE', #28014, #14998 ) ;
#23464=VERTEX_POINT ( 'NONE', #20312 ) ;
#23496=CARTESIAN_POINT ( 'NONE',  ( 10.24160887879199855, 3.710311786319799854, -6.254020414961999563 ) ) ;
#23500=CARTESIAN_POINT ( 'NONE',  ( 11.21022026213526601, 5.045753393512712570, -7.824998325091605977 ) ) ;
#23515=CARTESIAN_POINT ( 'NONE',  ( 10.99826088462129903, 4.001843064679911244, -6.633804182961699603 ) ) ;
#23519=CARTESIAN_POINT ( 'NONE',  ( 11.64633327354034797, 3.135095881599500256, -6.934277916748599502 ) ) ;
#23520=CARTESIAN_POINT ( 'NONE',  ( 9.176721904869998170, 4.995641764568400589, -8.058956102599799109 ) ) ;
#23529=CARTESIAN_POINT ( 'NONE',  ( 9.429533309317625012, 4.633212041316643770, -6.896199718737570095 ) ) ;
#23542=CARTESIAN_POINT ( 'NONE',  ( 11.70794988689359961, 4.455786710255300598, -8.393984925606600811 ) ) ;
#23605=CARTESIAN_POINT ( 'NONE',  ( 10.86272200990529946, 2.793294545435000220, -7.079074440652799893 ) ) ;
#23611=DIRECTION ( 'NONE',  ( -1.000000000000000000, 0.000000000000000000, 0.000000000000000000 ) ) ;
#23637=CARTESIAN_POINT ( 'NONE',  ( 11.71922412107039868, 4.069539071394910223, -6.185573549454999487 ) ) ;
#23678=B_SPLINE_CURVE_WITH_KNOTS ( 'NONE', 3,
 ( #17382, #65613, #64572, #12141, #53752, #22618, #5510, #32779, #17027, #38360, #16343, #27884, #59685, #33471, #54787, #43619, #1649, #11785 ),
 .UNSPECIFIED., .F., .F.,
 ( 4, 2, 2, 2, 2, 2, 2, 2, 4 ),
 ( 0.000000000000000000, 0.1249999999999996669, 0.2499999999999993339, 0.3749999999999990008, 0.4999999999999986677, 0.6249999999999990008, 0.7499999999999993339, 0.8749999999999996669, 1.000000000000000000 ),
 .UNSPECIFIED. ) ;
#23688=CARTESIAN_POINT ( 'NONE',  ( 10.65364694612719809, 3.195501139158400061, -7.821061011719899980 ) ) ;
#23691=CARTESIAN_POINT ( 'NONE',  ( 10.41488779216199845, 4.929030047862200448, -7.835030859477799758 ) ) ;
#23774=CARTESIAN_POINT ( 'NONE',  ( 10.71918447801630059, 5.140463864104999558, -7.474854604063350116 ) ) ;
#23781=CARTESIAN_POINT ( 'NONE',  ( 11.10887482311539998, 5.184953745778000389, -7.978749413531599721 ) ) ;
#23791=EDGE_CURVE ( 'NONE', #43345, #52427, #29188, .T. ) ;
#23825=CARTESIAN_POINT ( 'NONE',  ( 9.791846873516664829, 3.000416447002276943, -6.731816600031355513 ) ) ;
#23863=CARTESIAN_POINT ( 'NONE',  ( 11.56441235500451015, 3.361299021099800388, -6.914884925939399629 ) ) ;
#23865=CARTESIAN_POINT ( 'NONE',  ( 11.06967835872019812, 3.245266201729799960, -7.024326263066900111 ) ) ;
#23866=CARTESIAN_POINT ( 'NONE',  ( 8.847442991499999465, 3.928121959910110483, -6.360452723514999462 ) ) ;
#23879=UNCERTAINTY_MEASURE_WITH_UNIT (LENGTH_MEASURE( 1.000000000000000082E-05 ), #62404, 'distance_accuracy_value', 'NONE');
#23889=CARTESIAN_POINT ( 'NONE',  ( 10.62903166480609940, 3.135947233695900227, -7.560921321260908989 ) ) ;
#23898=CARTESIAN_POINT ( 'NONE',  ( 11.53828694957233481, 4.309606737214646266, -8.735060943529676436 ) ) ;
#23955=CARTESIAN_POINT ( 'NONE',  ( 9.048601287889788125, 4.000000467705929985, -8.698595322193607871 ) ) ;
#23960=CARTESIAN_POINT ( 'NONE',  ( 11.59999999999999964, 4.000000000000000000, -7.500000000000000000 ) ) ;
#23986=ORIENTED_EDGE ( 'NONE', *, *, #4429, .F. ) ;
#24033=CARTESIAN_POINT ( 'NONE',  ( 10.23103300763299828, 4.692441239783899931, -8.226274395107198600 ) ) ;
#24036=CARTESIAN_POINT ( 'NONE',  ( 10.26291290906799958, 3.364470222553300083, -8.277781595084700683 ) ) ;
#24041=EDGE_LOOP ( 'NONE', ( #450, #21402 ) ) ;
#24058=CARTESIAN_POINT ( 'NONE',  ( 8.789886373836322875, 4.000007821194417446, -8.439846342473931173 ) ) ;
#24117=CARTESIAN_POINT ( 'NONE',  ( 10.74379975933729980, 5.078682052940000524, -7.128873141726999485 ) ) ;
#24125=CARTESIAN_POINT ( 'NONE',  ( 10.86272200990529946, 2.793294545435000220, -7.079074440652799893 ) ) ;
#24187=CARTESIAN_POINT ( 'NONE',  ( 9.760355082327999199, 3.427502311996299955, -6.356045986629998978 ) ) ;
#24204=CARTESIAN_POINT ( 'NONE',  ( 11.71210404293059959, 3.618181340822599790, -8.277504409418298792 ) ) ;
#24206=CARTESIAN_POINT ( 'NONE',  ( 10.98656920625009903, 4.032067152264009913, -6.608450613814399688 ) ) ;
#24207=CARTESIAN_POINT ( 'NONE',  ( 9.252709346416999381, 5.031430618794000331, -7.010219103474399915 ) ) ;
#24308=ADVANCED_FACE ( 'NONE', ( #46560 ), #51453, .T. ) ;
#24330=CARTESIAN_POINT ( 'NONE',  ( 11.22567835872029995, 3.006051690924700370, -6.873560442659099046 ) ) ;
#24379=CARTESIAN_POINT ( 'NONE',  ( 10.35410941423799791, 4.742797679580299963, -6.825313060354999628 ) ) ;
#24381=CARTESIAN_POINT ( 'NONE',  ( 9.275076168957998135, 3.490299597736799875, -8.365475476407400635 ) ) ;
#24383=CARTESIAN_POINT ( 'NONE',  ( 11.04752711762115780, 5.162390711389719833, -7.824990536777686856 ) ) ;
#24404=CARTESIAN_POINT ( 'NONE',  ( 8.763353253171903390, 3.867553254011501629, -8.413353309630901222 ) ) ;
#24444=CARTESIAN_POINT ( 'NONE',  ( 11.36486084871759950, 2.792989229543000107, -7.825000000000000178 ) ) ;
#24465=CARTESIAN_POINT ( 'NONE',  ( 11.28118179236249929, 3.732952383914999839, -6.250199235344999771 ) ) ;
#24473=CARTESIAN_POINT ( 'NONE',  ( 10.76426088462129904, 4.002719309691810778, -6.221990224628999755 ) ) ;
#24534=CARTESIAN_POINT ( 'NONE',  ( 9.228442991499999692, 3.919472480837189909, -6.223324745230999433 ) ) ;
#24556=CARTESIAN_POINT ( 'NONE',  ( 10.85056919669530018, 4.830699382454300306, -7.745432529082900253 ) ) ;
#24558=CARTESIAN_POINT ( 'NONE',  ( 10.90346005378009941, 4.786957292481900161, -7.079777642108599167 ) ) ;
#24559=CARTESIAN_POINT ( 'NONE',  ( 9.100734463322998735, 4.118936914955599882, -8.635600483553998785 ) ) ;
#24623=VERTEX_POINT ( 'NONE', #6386 ) ;
#24634=VERTEX_POINT ( 'NONE', #60234 ) ;
#24673=CARTESIAN_POINT ( 'NONE',  ( 11.43856039236529831, 5.032284719763000069, -7.550239075043479353 ) ) ;
#24697=CARTESIAN_POINT ( 'NONE',  ( 10.97755399909358154, 4.133346405062088280, -8.778526265510096849 ) ) ;
#24715=VERTEX_POINT ( 'NONE', #38556 ) ;
#24723=CARTESIAN_POINT ( 'NONE',  ( 10.20641772631199906, 4.431553727090300043, -8.388315195900499788 ) ) ;
#24725=CARTESIAN_POINT ( 'NONE',  ( 9.781659112603998452, 3.563556310301200014, -8.404632083253700259 ) ) ;
#24764=CARTESIAN_POINT ( 'NONE',  ( 11.34523293495530005, 2.684794526488000432, -7.447129085684729866 ) ) ;
#24809=CARTESIAN_POINT ( 'NONE',  ( 10.56733863405299800, 4.788475529394700558, -8.505794571537999005 ) ) ;
#24816=CARTESIAN_POINT ( 'NONE',  ( 10.05862282008599884, 4.666276081381299790, -8.574682153725998290 ) ) ;
#24877=CARTESIAN_POINT ( 'NONE',  ( 9.912329965421998068, 3.111510091554099855, -8.420309768537698858 ) ) ;
#24895=CARTESIAN_POINT ( 'NONE',  ( 10.84641504065830020, 4.804462279649600376, -6.900173947321999179 ) ) ;
#24898=CARTESIAN_POINT ( 'NONE',  ( 9.936596320338999533, 2.942832934044000037, -7.068569539041399175 ) ) ;
#24906=CARTESIAN_POINT ( 'NONE',  ( 9.302887573405627109, 4.590576684156811638, -8.145562893180322561 ) ) ;
#24946=CARTESIAN_POINT ( 'NONE',  ( 8.733215486276282746, 4.027942412209718270, -8.383215533252753815 ) ) ;
#24971=EDGE_LOOP ( 'NONE', ( #2672, #56099, #32024, #13877, #1689 ) ) ;
#25012=CARTESIAN_POINT ( 'NONE',  ( 11.72433327354039889, 3.016779570871600313, -6.856888818507299810 ) ) ;
#25061=CARTESIAN_POINT ( 'NONE',  ( 10.87103032197929942, 4.583685623598699799, -6.683751296690399357 ) ) ;
#25063=CARTESIAN_POINT ( 'NONE',  ( 10.38955864497999926, 4.790758628877400227, -8.119307134446700047 ) ) ;
#25089=EDGE_CURVE ( 'NONE', #20133, #24634, #70, .T. ) ;
#25103=CARTESIAN_POINT ( 'NONE',  ( 10.98146005378009882, 4.911671201000399556, -7.013182449205100255 ) ) ;
#25146=CARTESIAN_POINT ( 'NONE',  ( 10.88733729122639993, 2.722429312291999803, -7.466391690027689876 ) ) ;
#25157=LINE ( 'NONE', #56973, #41829 ) ;
#25158=CARTESIAN_POINT ( 'NONE',  ( 10.33351354018233081, 2.750000000000000000, -7.336375382625529795 ) ) ;
#25167=( NAMED_UNIT ( * ) SI_UNIT ( $, .STERADIAN. ) SOLID_ANGLE_UNIT ( ) );
#25235=CARTESIAN_POINT ( 'NONE',  ( 11.48641235500450009, 3.260080192309100067, -6.822158181405299615 ) ) ;
#25238=CARTESIAN_POINT ( 'NONE',  ( 9.402671671056999969, 2.738456190347000163, -7.711876388024100137 ) ) ;
#25347=PRODUCT_CONTEXT ( 'NONE', #17253, 'mechanical' ) ;
#25351=CARTESIAN_POINT ( 'NONE',  ( 11.02301463001509774, 4.547357026650399980, -6.623338154204899908 ) ) ;
#25403=CARTESIAN_POINT ( 'NONE',  ( 11.35918179236250047, 3.761636028845500412, -6.384440618559000136 ) ) ;
#25408=CARTESIAN_POINT ( 'NONE',  ( 9.323721904869998411, 4.756019688173900306, -7.924431591189499358 ) ) ;
#25445=CARTESIAN_POINT ( 'NONE',  ( 11.75203632436369894, 2.890282938442000127, -7.240848640331599917 ) ) ;
#25448=AXIS2_PLACEMENT_3D ( 'NONE', #33292, #43780, #49018 ) ;
#25493=CARTESIAN_POINT ( 'NONE',  ( 10.71503032197929883, 4.743378537856500543, -6.460430507351999196 ) ) ;
#25495=CARTESIAN_POINT ( 'NONE',  ( 11.60000000000000142, 3.254367469151916659, -8.163463725006291583 ) ) ;
#25523=CARTESIAN_POINT ( 'NONE',  ( 10.50145247700547557, 3.917463882723016599, -6.629783135293719099 ) ) ;
#25584=CARTESIAN_POINT ( 'NONE',  ( 10.30487885159599770, 4.996404279947399552, -7.381132626649399064 ) ) ;
#25587=EDGE_CURVE ( 'NONE', #42619, #14127, #66685, .T. ) ;
#25588=CARTESIAN_POINT ( 'NONE',  ( 8.668126402770999661, 5.196937059091999878, -7.048639765412399782 ) ) ;
#25606=CARTESIAN_POINT ( 'NONE',  ( 11.00000000000000000, 3.031410575668799900, -7.174999999999999822 ) ) ;
#25664=CARTESIAN_POINT ( 'NONE',  ( 9.813975701332999790, 4.636077325177999420, -8.089163458558500608 ) ) ;
#25697=CARTESIAN_POINT ( 'NONE',  ( 11.31389666366019853, 3.954123449088899900, -8.532487796751999198 ) ) ;
#25734=APPLICATION_CONTEXT ( 'automotive_design' ) ;
#25753=CARTESIAN_POINT ( 'NONE',  ( 11.40425819896749893, 2.744109752373000255, -7.736761623643599428 ) ) ;
#25756=CARTESIAN_POINT ( 'NONE',  ( 8.793822372493998785, 3.711294259598199918, -8.444453017408701356 ) ) ;
#25782=ORIENTED_EDGE ( 'NONE', *, *, #31493, .T. ) ;
#25793=CARTESIAN_POINT ( 'NONE',  ( 10.51925056272499859, 5.174767082365999471, -7.517410630436119234 ) ) ;
#25834=CARTESIAN_POINT ( 'NONE',  ( 10.14887885159599890, 5.269014563305000287, -7.348611220446799486 ) ) ;
#25837=CLOSED_SHELL ( 'NONE', ( #30955, #467, #30457, #7658, #53985, #1489, #8836, #60749, #67183, #31126, #24308, #27818, #14913, #35200, #40978, #60839, #35282, #13578, #12231, #16271, #18760, #42859, #66133, #45873, #51022, #58954, #51301, #39579, #53495, #15855, #12872 ) ) ;
#25838=CARTESIAN_POINT ( 'NONE',  ( 11.59999999999999964, 4.109635333090443154, -8.637585274955606351 ) ) ;
#25925=CARTESIAN_POINT ( 'NONE',  ( 10.79718447801629999, 5.003225587801999552, -7.477880487566260115 ) ) ;
#25928=CARTESIAN_POINT ( 'NONE',  ( 8.644809814040998575, 4.698458605182900705, -8.403266072559899769 ) ) ;
#26010=CARTESIAN_POINT ( 'NONE',  ( 11.67766954483535891, 4.715882430684499305, -6.395429936871999566 ) ) ;
#26011=CARTESIAN_POINT ( 'NONE',  ( 8.851468108405999402, 4.834201109053600121, -7.736255015838599647 ) ) ;
#26016=CARTESIAN_POINT ( 'NONE',  ( 9.852263540182327972, 2.907767014557178342, -6.870476274536370553 ) ) ;
#26048=CARTESIAN_POINT ( 'NONE',  ( 11.48522412107029922, 4.047131449166419870, -6.609122077774299164 ) ) ;
#26060=VERTEX_POINT ( 'NONE', #28819 ) ;
#26099=CARTESIAN_POINT ( 'NONE',  ( 10.89149144726329865, 3.340422662105400065, -6.569275630703699242 ) ) ;
#26101=CARTESIAN_POINT ( 'NONE',  ( 9.146417874593998576, 3.202096358337300330, -7.839201596587598964 ) ) ;
#26141=CARTESIAN_POINT ( 'NONE',  ( 11.64633327354034797, 3.135095881599500256, -6.934277916748599502 ) ) ;
#26148=ORIENTED_EDGE ( 'NONE', *, *, #43451, .T. ) ;
#26161=DIRECTION ( 'NONE',  ( -1.000000000000000000, 0.000000000000000000, 0.000000000000000000 ) ) ;
#26170=CARTESIAN_POINT ( 'NONE',  ( 11.11486084871780022, 5.207010770456999893, -7.174999999999999822 ) ) ;
#26173=FACE_OUTER_BOUND ( 'NONE', #2443, .T. ) ;
#26183=CARTESIAN_POINT ( 'NONE',  ( 11.71210404293059959, 3.618181340822599790, -8.277504409418298792 ) ) ;
#26184=CARTESIAN_POINT ( 'NONE',  ( 10.64118447801629941, 5.277702140407999565, -7.471828720557429193 ) ) ;
#26221=CARTESIAN_POINT ( 'NONE',  ( 9.591846873515667227, 4.999583552997727054, -8.268183399968643599 ) ) ;
#26257=CARTESIAN_POINT ( 'NONE',  ( 11.14975833414749928, 3.203462856645999945, -7.825000000000000178 ) ) ;
#26259=CARTESIAN_POINT ( 'NONE',  ( 8.849999778957998942, 4.000000000000000000, -8.499999833805500060 ) ) ;
#26266=B_SPLINE_SURFACE_WITH_KNOTS ( 'NONE', 3, 3, ( 
 ( #53084, #5184, #42594, #63904 ),
 ( #16017, #37346, #58670, #10770 ),
 ( #32115, #53431, #5528, #48182 ),
 ( #12160, #27903, #54459, #65631 ) ),
 .UNSPECIFIED., .F., .F., .F.,
 ( 4, 4 ),
 ( 4, 4 ),
 ( 0.7363163806532000422, 1.013499456067999960 ),
 ( -0.0005287450254680999126, 0.02696599629895000266 ),
 .UNSPECIFIED. ) ;
#26276=CARTESIAN_POINT ( 'NONE',  ( 11.26487482311540056, 4.930401445321599851, -7.875904247640098887 ) ) ;
#26279=CARTESIAN_POINT ( 'NONE',  ( 9.605304848515999083, 5.163382381259999931, -8.031907719862799055 ) ) ;
#26310=VERTEX_POINT ( 'NONE', #67912 ) ;
#26359=CARTESIAN_POINT ( 'NONE',  ( 11.75203632436369894, 2.890282938442000127, -7.240848640331599917 ) ) ;
#26360=CARTESIAN_POINT ( 'NONE',  ( 9.383380199233998908, 4.860242402105300563, -7.391875284387199763 ) ) ;
#26446=CARTESIAN_POINT ( 'NONE',  ( 10.54687750876899877, 3.382085645339300228, -8.458891008702400072 ) ) ;
#26448=CARTESIAN_POINT ( 'NONE',  ( 10.15958376188599921, 3.268856270222099791, -7.965979387614599894 ) ) ;
#26486=CARTESIAN_POINT ( 'NONE',  ( 11.10612378248509913, 3.517039242046199998, -6.586279795136899651 ) ) ;
#26494=CARTESIAN_POINT ( 'NONE',  ( 9.541846873516668381, 4.999583552997725278, -8.268183399968640046 ) ) ;
#26530=CARTESIAN_POINT ( 'NONE',  ( 11.44133594839949986, 4.569506585117100173, -6.847343244997600387 ) ) ;
#26561=CARTESIAN_POINT ( 'NONE',  ( 10.94452754078378121, 4.508448539877488059, -6.788965764111623002 ) ) ;
#26594=AXIS2_PLACEMENT_3D ( 'NONE', #11930, #28371, #12632 ) ;
#26622=CARTESIAN_POINT ( 'NONE',  ( 9.682355082327998019, 3.488994418336600400, -6.478918346312998899 ) ) ;
#26624=CARTESIAN_POINT ( 'NONE',  ( 10.27610941423800028, 4.844410192686099847, -6.733017893878099791 ) ) ;
#26628=CARTESIAN_POINT ( 'NONE',  ( 9.174709346416998201, 5.155548326249999924, -6.951281079990299538 ) ) ;
#26682=CARTESIAN_POINT ( 'NONE',  ( 10.64393020684969926, 5.250000000000000000, -7.500000000000000000 ) ) ;
#26707=CARTESIAN_POINT ( 'NONE',  ( 11.46989666366029859, 3.941571897678119996, -8.814970315645998866 ) ) ;
#26708=CARTESIAN_POINT ( 'NONE',  ( 9.864633995697998259, 4.861719613449499988, -7.595641268826199166 ) ) ;
#26730=CARTESIAN_POINT ( 'NONE',  ( 11.07210672858429845, 3.307795442047700263, -6.979277962544199632 ) ) ;
#26742=CARTESIAN_POINT ( 'NONE',  ( 10.69057802013490033, 2.966773425016000054, -7.475947032624040034 ) ) ;
#26764=CARTESIAN_POINT ( 'NONE',  ( 11.14955063476181962, 4.976598135215293262, -6.673569913327194847 ) ) ;
#26772=CARTESIAN_POINT ( 'NONE',  ( 11.59999999999999964, 5.087332147730433185, -6.982348652072320583 ) ) ;
#26777=CARTESIAN_POINT ( 'NONE',  ( 8.748305582559998683, 4.091272957481129957, -8.362426869835999810 ) ) ;
#26796=CARTESIAN_POINT ( 'NONE',  ( 10.98995257254739855, 2.904643075091000171, -7.818564472783199548 ) ) ;
#26799=CARTESIAN_POINT ( 'NONE',  ( 10.28622949779699880, 4.480999174483200065, -8.221351791991999391 ) ) ;
#26875=CARTESIAN_POINT ( 'NONE',  ( 8.807788144226000426, 4.090932644426789722, -8.453461841935100196 ) ) ;
#26876=CARTESIAN_POINT ( 'NONE',  ( 11.29364426047339975, 4.466097552695299733, -8.230103870496201068 ) ) ;
#26905=CARTESIAN_POINT ( 'NONE',  ( 10.57529832096847677, 3.253995305422127782, -7.044405226132214537 ) ) ;
#26957=CARTESIAN_POINT ( 'NONE',  ( 11.65456516821461008, 4.802916961510000249, -8.310318115935698913 ) ) ;
#26962=CARTESIAN_POINT ( 'NONE',  ( 10.26492546752099955, 2.860918852493000486, -7.421078600323300023 ) ) ;
#26964=CARTESIAN_POINT ( 'NONE',  ( 11.13764426047339917, 4.613828180779599997, -8.461511872390000022 ) ) ;
#27020=SURFACE_SIDE_STYLE ('',( #21756 ) ) ;
#27027=CARTESIAN_POINT ( 'NONE',  ( 10.15434687351570631, 5.250000000000002665, -7.336375382625537789 ) ) ;
#27049=CARTESIAN_POINT ( 'NONE',  ( 9.535355082327999554, 3.611978631017199959, -6.724663065681199647 ) ) ;
#27070=CARTESIAN_POINT ( 'NONE',  ( 11.09672200990539892, 3.182132064022000328, -7.214709569664399247 ) ) ;
#27082=CARTESIAN_POINT ( 'NONE',  ( 10.36325056272499978, 4.892034740700499817, -7.513220396995270001 ) ) ;
#27110=CARTESIAN_POINT ( 'NONE',  ( 11.60000000000000320, 3.905927825748640725, -6.471240206706528220 ) ) ;
#27135=CARTESIAN_POINT ( 'NONE',  ( 10.15303300763299887, 4.787165141710600480, -8.325626572044798834 ) ) ;
#27141=CYLINDRICAL_SURFACE ( 'NONE', #22713, 1.250000000000000222 ) ;
#27154=CARTESIAN_POINT ( 'NONE',  ( 9.373082992855458428, 2.782568642349716459, -7.172827875665085173 ) ) ;
#27175=CARTESIAN_POINT ( 'NONE',  ( 10.57102344389999971, 3.237334151971200225, -7.037150754511299233 ) ) ;
#27182=AXIS2_PLACEMENT_3D ( 'NONE', #51569, #19762, #18741 ) ;
#27195=CARTESIAN_POINT ( 'NONE',  ( 11.58810207955109917, 3.203462856645999945, -7.174999999999999822 ) ) ;
#27217=EDGE_CURVE ( 'NONE', #57302, #19484, #29462, .T. ) ;
#27298=CARTESIAN_POINT ( 'NONE',  ( 10.35410941423799791, 4.742797679580299963, -6.825313060354999628 ) ) ;
#27304=CARTESIAN_POINT ( 'NONE',  ( 10.22687885159599830, 5.132709421626000079, -7.364871923548499844 ) ) ;
#27388=CARTESIAN_POINT ( 'NONE',  ( 11.27234208742519783, 3.445253572379500362, -8.372004648554700168 ) ) ;
#27389=CARTESIAN_POINT ( 'NONE',  ( 10.24255864497999902, 4.790758628877400227, -8.119307134446700047 ) ) ;
#27411=CARTESIAN_POINT ( 'NONE',  ( 11.53979707368350027, 3.569730287184500472, -6.748224392138099326 ) ) ;
#27422=CARTESIAN_POINT ( 'NONE',  ( 11.19434208742519843, 3.521141233577200325, -8.252717006421999457 ) ) ;
#27476=CARTESIAN_POINT ( 'NONE',  ( 10.93656785386839836, 2.939720539848000413, -8.213529149347399638 ) ) ;
#27517=CARTESIAN_POINT ( 'NONE',  ( 10.35814141025499957, 4.483492689244800822, -8.361148840840000318 ) ) ;
#27554=LINE ( 'NONE', #26875, #10484 ) ;
#27555=CARTESIAN_POINT ( 'NONE',  ( 11.85979573085659844, 4.840012015667699785, -7.645349278262099979 ) ) ;
#27645=CARTESIAN_POINT ( 'NONE',  ( 10.84641504065830020, 4.804462279649600376, -6.900173947321999179 ) ) ;
#27653=CARTESIAN_POINT ( 'NONE',  ( 11.43302763632549990, 2.964209339073000216, -7.022058766158599141 ) ) ;
#27656=CARTESIAN_POINT ( 'NONE',  ( 8.499265421555000088, 3.759926620436100375, -8.741861511046000288 ) ) ;
#27686=CARTESIAN_POINT ( 'NONE',  ( 11.33810207955129812, 4.796537143354000499, -7.825000000000000178 ) ) ;
#27743=CARTESIAN_POINT ( 'NONE',  ( 11.14256920625030034, 4.042230905578960254, -6.325872106312999676 ) ) ;
#27744=CARTESIAN_POINT ( 'NONE',  ( 10.16657120343299958, 3.951311476804090006, -8.503230697164999796 ) ) ;
#27766=CARTESIAN_POINT ( 'NONE',  ( 11.61364291764652812, 3.140345330584100036, -7.393734108507599601 ) ) ;
#27798=EDGE_LOOP ( 'NONE', ( #58441, #34239, #46018, #19014 ) ) ;
#27806=CARTESIAN_POINT ( 'NONE',  ( 11.60000000000000320, 3.468809616172332078, -6.694115079111573330 ) ) ;
#27810=CARTESIAN_POINT ( 'NONE',  ( 8.726967411678998587, 3.935557623441470643, -8.391190439313799487 ) ) ;
#27818=ADVANCED_FACE ( 'NONE', ( #16929 ), #11343, .T. ) ;
#27834=CARTESIAN_POINT ( 'NONE',  ( 10.09964828895399869, 5.121614868497999851, -8.112615456209400833 ) ) ;
#27861=CARTESIAN_POINT ( 'NONE',  ( 11.26212378248529866, 3.384904051819500381, -6.336291382830999908 ) ) ;
#27872=CARTESIAN_POINT ( 'NONE',  ( 11.56833327354034857, 3.253412192327699959, -7.011667014989399149 ) ) ;
#27884=CARTESIAN_POINT ( 'NONE',  ( 10.76059687351619765, 3.370476274536378547, -6.407767014557177454 ) ) ;
#27903=CARTESIAN_POINT ( 'NONE',  ( 8.734997988989999129, 3.937347817007940343, -8.366433385397400002 ) ) ;
#27908=CARTESIAN_POINT ( 'NONE',  ( 10.47145237372899906, 4.043732047787757189, -8.774080944853650976 ) ) ;
#27910=CARTESIAN_POINT ( 'NONE',  ( 11.63410404293056999, 3.557672215630899970, -8.400720262063998689 ) ) ;
#27912=CARTESIAN_POINT ( 'NONE',  ( 11.59999999999999964, 5.064318446328999634, -8.155535082817699788 ) ) ;
#27982=DIRECTION ( 'NONE',  ( 1.000000000000000000, 0.000000000000000000, 0.000000000000000000 ) ) ;
#27994=CARTESIAN_POINT ( 'NONE',  ( 10.82179975933729921, 4.948878321068100661, -7.173532873542499466 ) ) ;
#28001=CARTESIAN_POINT ( 'NONE',  ( 10.52226222744799955, 3.119510978356100139, -8.225278704382400718 ) ) ;
#28014=CARTESIAN_POINT ( 'NONE',  ( 11.37299956498129916, 2.792989229543000107, -7.174999999999999822 ) ) ;
#28033=CARTESIAN_POINT ( 'NONE',  ( 11.16544712921906957, 3.267598948716616825, -7.982093405445620959 ) ) ;
#28054=CARTESIAN_POINT ( 'NONE',  ( 8.896714042595457173, 3.863849893574820893, -6.453285899984952501 ) ) ;
#28064=CARTESIAN_POINT ( 'NONE',  ( 11.28192504596561996, 4.908977993420656105, -7.825000185715046186 ) ) ;
#28072=CARTESIAN_POINT ( 'NONE',  ( 9.843930206850000530, 2.750000000000000000, -7.500000000000000000 ) ) ;
#28081=CARTESIAN_POINT ( 'NONE',  ( 10.64902344389989963, 3.116469856398800253, -6.963800219468099684 ) ) ;
#28082=CARTESIAN_POINT ( 'NONE',  ( 10.11591290906799934, 3.364470222553300083, -8.277781595084700683 ) ) ;
#28090=CARTESIAN_POINT ( 'NONE',  ( 9.581508192411627434, 3.220001783077621305, -7.103597363128174358 ) ) ;
#28104=CARTESIAN_POINT ( 'NONE',  ( 11.16641369783139837, 3.949373449607799902, -8.502191501283999031 ) ) ;
#28126=CARTESIAN_POINT ( 'NONE',  ( 11.00000000000000000, 2.941427501403999667, -7.825000000000000178 ) ) ;
#28198=CARTESIAN_POINT ( 'NONE',  ( 11.13746005378019888, 5.161099018038999731, -6.879992063401499713 ) ) ;
#28247=CARTESIAN_POINT ( 'NONE',  ( 11.33872066707849768, 4.858611803369300652, -6.980638253271099103 ) ) ;
#28249=CARTESIAN_POINT ( 'NONE',  ( 9.429063610504998749, 4.468346739194200445, -8.541338455964998744 ) ) ;
#28311=VERTEX_POINT ( 'NONE', #48510 ) ;
#28332=B_SPLINE_CURVE_WITH_KNOTS ( 'NONE', 3,
 ( #68155, #47195, #31127, #53470, #9777, #42303, #58708, #26561, #64282, #47887, #16399, #15721, #21305, #48219, #69191, #63943, #36354, #9427, #52778, #41944, #52082, #5563, #26905, #37047, #4185, #25523, #58362, #325, #31806, #42634, #16055, #30770, #21640, #41601, #37385 ),
 .UNSPECIFIED., .F., .F.,
 ( 4, 1, 1, 1, 1, 1, 1, 1, 1, 1, 1, 1, 1, 1, 1, 1, 1, 1, 1, 1, 1, 1, 1, 1, 1, 1, 1, 1, 1, 1, 1, 1, 4 ),
 ( 0.000000000000000000, 0.02634724210002164710, 0.05799096732718461711, 0.08963469255434758365, 0.1212784177813103353, 0.1529221430084733158, 0.1845658682354360536, 0.2162095934625990201, 0.2478533186897620144, 0.2794970439167247522, 0.3111407691438877188, 0.3427844943710506853, 0.3744282195980134231, 0.4060719448251764452, 0.4377156700521391830, 0.4693593952793021495, 0.5010031205064651161, 0.5326468457334281315, 0.5642905709605910980, 0.5959342961875535583, 0.6275780214147167468, 0.6592217466418797134, 0.6908654718688422847, 0.7225091970960054732, 0.7541529223229680445, 0.7857966475501312331, 0.8174403727772941997, 0.8490840980042566599, 0.8807278232314198485, 0.9123715484585828150, 0.9440152736855453863, 0.9756589989127085749, 1.000000000000000000 ),
 .UNSPECIFIED. ) ;
#28333=CARTESIAN_POINT ( 'NONE',  ( 11.60118044953561878, 5.133201153721000054, -8.090905336380599167 ) ) ;
#28342=CARTESIAN_POINT ( 'NONE',  ( 11.28118179236249929, 3.732952383914999839, -6.250199235344999771 ) ) ;
#28371=DIRECTION ( 'NONE',  ( -1.000000000000000000, 0.000000000000000000, 0.000000000000000000 ) ) ;
#28393=B_SPLINE_CURVE_WITH_KNOTS ( 'NONE', 3,
 ( #57935, #20869, #4778, #21212 ),
 .UNSPECIFIED., .F., .F.,
 ( 4, 4 ),
 ( 0.000000000000000000, 1.000000000000000000 ),
 .UNSPECIFIED. ) ;
#28409=EDGE_CURVE ( 'NONE', #59938, #24623, #46895, .T. ) ;
#28432=CARTESIAN_POINT ( 'NONE',  ( 11.39189666366029918, 3.947847673382490541, -8.673729056199000809 ) ) ;
#28433=CARTESIAN_POINT ( 'NONE',  ( 9.989267173155999657, 3.235527139800300045, -6.848522029265999400 ) ) ;
#28438=EDGE_LOOP ( 'NONE', ( #46647, #45554, #66512, #28469, #34388, #65332, #23318, #38729, #42596, #57027 ) ) ;
#28442=CARTESIAN_POINT ( 'NONE',  ( 9.505520750864626223, 3.872956735472087964, -6.634325535862901191 ) ) ;
#28457=CARTESIAN_POINT ( 'NONE',  ( 11.01872200990539952, 3.052519557825900343, -7.169497859994799605 ) ) ;
#28469=ORIENTED_EDGE ( 'NONE', *, *, #8914, .F. ) ;
#28525=CARTESIAN_POINT ( 'NONE',  ( 9.393930206848999376, 2.750000000000000000, -7.500000000000000000 ) ) ;
#28537=DIRECTION ( 'NONE',  ( 0.000000000000000000, 0.000000000000000000, -1.000000000000000000 ) ) ;
#28553=CARTESIAN_POINT ( 'NONE',  ( 11.30367835872029936, 2.886444435522000251, -6.798177532456199934 ) ) ;
#28602=CARTESIAN_POINT ( 'NONE',  ( 10.53521345716899837, 4.924890298941200228, -8.340879262988799780 ) ) ;
#28604=CARTESIAN_POINT ( 'NONE',  ( 10.67826222744820086, 3.331419131587999960, -8.050725169876500331 ) ) ;
#28606=CARTESIAN_POINT ( 'NONE',  ( 9.783671671056998420, 2.873958896683999953, -7.689118697196099639 ) ) ;
#28630=VERTEX_POINT ( 'NONE', #60608 ) ;
#28690=CARTESIAN_POINT ( 'NONE',  ( 11.52733460557258915, 4.206337284815599986, -8.761245990815998752 ) ) ;
#28697=CARTESIAN_POINT ( 'NONE',  ( 10.81349144726329925, 3.261052100888700345, -6.457276458983999490 ) ) ;
#28762=CARTESIAN_POINT ( 'NONE',  ( 10.01364655415099847, 4.619310611972400338, -8.619302797893999113 ) ) ;
#28776=CARTESIAN_POINT ( 'NONE',  ( 10.01059687351599692, 4.629523725463622341, -8.592232985442825210 ) ) ;
#28784=CARTESIAN_POINT ( 'NONE',  ( 10.55518582084299872, 3.433275964779900047, -6.844925608615599621 ) ) ;
#28786=CARTESIAN_POINT ( 'NONE',  ( 10.85168717260509830, 3.386210853237200169, -8.501809683958001074 ) ) ;
#28787=CARTESIAN_POINT ( 'NONE',  ( 9.938608878791999501, 3.772542739612499751, -6.521682313853199631 ) ) ;
#28796=CARTESIAN_POINT ( 'NONE',  ( 9.961445400145626294, 4.347277725169313989, -6.696924380570436597 ) ) ;
#28811=CARTESIAN_POINT ( 'NONE',  ( 10.28441772631199846, 4.372518460886800185, -8.266796319406900295 ) ) ;
#28819=CARTESIAN_POINT ( 'NONE',  ( 8.599999952505998024, 4.000000000000000000, -8.249999993641800700 ) ) ;
#28820=CARTESIAN_POINT ( 'NONE',  ( 11.52285868696541549, 4.059810388505518119, -8.771870505746530711 ) ) ;
#28858=CARTESIAN_POINT ( 'NONE',  ( 10.59393020684899867, 5.250000000000000000, -7.500000000000000000 ) ) ;
#28910=CARTESIAN_POINT ( 'NONE',  ( 10.63880513895979973, 5.150451045932999961, -6.860457220153399760 ) ) ;
#28958=CARTESIAN_POINT ( 'NONE',  ( 10.77672335273219950, 4.301522290735800169, -8.312023951944400579 ) ) ;
#28960=CARTESIAN_POINT ( 'NONE',  ( 9.581038493598999395, 4.826346105011899645, -6.712036445818600150 ) ) ;
#29039=CARTESIAN_POINT ( 'NONE',  ( 10.96533729122639933, 2.859653469230999612, -7.470001566214039990 ) ) ;
#29046=CARTESIAN_POINT ( 'NONE',  ( 11.62579573085663043, 5.239377455231000624, -7.714452430741599365 ) ) ;
#29068=CARTESIAN_POINT ( 'NONE',  ( 11.59610237318921477, 3.189590050595149773, -7.174950768514437804 ) ) ;
#29101=ORIENTED_EDGE ( 'NONE', *, *, #57767, .F. ) ;
#29126=CARTESIAN_POINT ( 'NONE',  ( 10.50595525820100029, 3.918212119278319694, -6.637672143048099827 ) ) ;
#29128=CARTESIAN_POINT ( 'NONE',  ( 11.40211496860029783, 4.793947479907100018, -7.093139000852099585 ) ) ;
#29129=CARTESIAN_POINT ( 'NONE',  ( 9.632646554151000018, 4.552790318865400643, -8.499078230848398974 ) ) ;
#29138=CARTESIAN_POINT ( 'NONE',  ( 9.885457958598628636, 4.856131813426149968, -7.319526769407151079 ) ) ;
#29142=ORIENTED_EDGE ( 'NONE', *, *, #1965, .F. ) ;
#29151=CARTESIAN_POINT ( 'NONE',  ( 11.46179707368349909, 3.501542828836900156, -6.629085939160999530 ) ) ;
#29188=CIRCLE ( 'NONE', #55976, 1.249999999999999778 ) ;
#29296=CARTESIAN_POINT ( 'NONE',  ( 10.60441638348510018, 3.158410350011299883, -7.294998899090099798 ) ) ;
#29299=CARTESIAN_POINT ( 'NONE',  ( 8.897151519676997466, 4.024693162376980382, -8.641543873690000765 ) ) ;
#29319=CARTESIAN_POINT ( 'NONE',  ( 8.736820887142258130, 3.746718250072767376, -8.358484985884542695 ) ) ;
#29339=CARTESIAN_POINT ( 'NONE',  ( 11.55300581613033906, 5.107584469683000172, -8.211208432468300344 ) ) ;
#29357=CARTESIAN_POINT ( 'NONE',  ( 9.035395982797805203, 3.688926447190845170, -8.654212551762981320 ) ) ;
#29358=DIRECTION ( 'NONE',  ( 0.000000000000000000, 1.000000000000000000, 0.000000000000000000 ) ) ;
#29370=CARTESIAN_POINT ( 'NONE',  ( 11.59999999999999964, 4.000000000000000000, -7.500000000000000000 ) ) ;
#29384=CARTESIAN_POINT ( 'NONE',  ( 10.34995525820099971, 3.892289273474800471, -6.364355462479999836 ) ) ;
#29392=CARTESIAN_POINT ( 'NONE',  ( 11.33041235500449950, 3.057642534728299832, -6.636704692336500067 ) ) ;
#29394=CARTESIAN_POINT ( 'NONE',  ( 9.843930206850000530, 2.750000000000000000, -7.500000000000000000 ) ) ;
#29396=CARTESIAN_POINT ( 'NONE',  ( 11.51961669203094196, 5.030276287827526005, -7.175016092226064401 ) ) ;
#29452=CARTESIAN_POINT ( 'NONE',  ( 8.810863317747999801, 4.960863370448500120, -7.500000000073117512 ) ) ;
#29457=CARTESIAN_POINT ( 'NONE',  ( 9.203113844318000503, 4.323050436788100193, -6.262250912840999106 ) ) ;
#29462=B_SPLINE_CURVE_WITH_KNOTS ( 'NONE', 3,
 ( #38345, #55472, #59325, #6875 ),
 .UNSPECIFIED., .F., .F.,
 ( 4, 4 ),
 ( 0.000000000000000000, 1.000000000000000000 ),
 .UNSPECIFIED. ) ;
#29467=CARTESIAN_POINT ( 'NONE',  ( 11.59999999999999964, 4.000000000000000000, -7.500000000000000000 ) ) ;
#29477=CARTESIAN_POINT ( 'NONE',  ( 11.75718044953559804, 4.889766368533900120, -7.963966784336999005 ) ) ;
#29482=CARTESIAN_POINT ( 'NONE',  ( 8.655265421554998895, 3.811499292588199861, -8.475084258675400051 ) ) ;
#29493=CARTESIAN_POINT ( 'NONE',  ( 9.733483075504627990, 3.885520926571138567, -8.367425391989351979 ) ) ;
#29499=CARTESIAN_POINT ( 'NONE',  ( 10.99999975383417627, 2.937013229513552925, -7.366608021396839234 ) ) ;
#29597=CARTESIAN_POINT ( 'NONE',  ( 10.47769598648999967, 5.009476315410999803, -8.101059042556599366 ) ) ;
#29615=CARTESIAN_POINT ( 'NONE',  ( 10.53976354018315753, 4.327184855449099921, -8.717465845835397076 ) ) ;
#29617=CARTESIAN_POINT ( 'NONE',  ( 11.41486084871699802, 2.792989229543000107, -7.825000000000000178 ) ) ;
#29647=CARTESIAN_POINT ( 'NONE',  ( 10.72333863405319931, 4.619094858989799768, -8.289729326049599223 ) ) ;
#29651=CARTESIAN_POINT ( 'NONE',  ( 10.03495058442699950, 4.398663815465100768, -6.578094656394299911 ) ) ;
#29691=CARTESIAN_POINT ( 'NONE',  ( 10.76346886766499900, 3.365322927604099679, -6.346853961441000003 ) ) ;
#29730=CARTESIAN_POINT ( 'NONE',  ( 11.45348876160960039, 3.114179898019400206, -8.421216112044099589 ) ) ;
#29740=CARTESIAN_POINT ( 'NONE',  ( 11.37964291764649971, 2.731641218595000087, -7.343212302062899433 ) ) ;
#29802=CARTESIAN_POINT ( 'NONE',  ( 9.051138961223999857, 5.059894361919000438, -8.216246114996598848 ) ) ;
#29821=CARTESIAN_POINT ( 'NONE',  ( 11.02287616594229824, 3.738072157442200005, -6.674353346984900348 ) ) ;
#29824=CARTESIAN_POINT ( 'NONE',  ( 9.430013376692999216, 2.982096917914000223, -6.982691809975100306 ) ) ;
#29873=CARTESIAN_POINT ( 'NONE',  ( 8.736413463905998711, 4.084156314540369870, -8.382409559052598880 ) ) ;
#29941=CARTESIAN_POINT ( 'NONE',  ( 10.89324174884020024, 3.967693531726030010, -8.674442868902998427 ) ) ;
#29975=DIRECTION ( 'NONE',  ( -1.000000000000000000, 0.000000000000000000, -3.164702532202999971E-14 ) ) ;
#29987=DIRECTION ( 'NONE',  ( 0.000000000000000000, 0.000000000000000000, 1.000000000000000000 ) ) ;
#29991=CARTESIAN_POINT ( 'NONE',  ( 11.08841369783139896, 3.942447888101379583, -8.639288317626999003 ) ) ;
#29993=CARTESIAN_POINT ( 'NONE',  ( 9.249747021775998945, 3.245052836381700168, -8.162493079567200382 ) ) ;
#30032=CARTESIAN_POINT ( 'NONE',  ( 11.63611496860034933, 5.171412538012999605, -6.899705789500199415 ) ) ;
#30048=CARTESIAN_POINT ( 'NONE',  ( 9.343930206849998754, 2.750000000000000000, -7.500000000000000000 ) ) ;
#30071=CARTESIAN_POINT ( 'NONE',  ( 10.32118582084299874, 3.163839350524900063, -6.533484739457099622 ) ) ;
#30124=CARTESIAN_POINT ( 'NONE',  ( 9.708513540183332680, 4.163624617374472869, -6.250000000000001776 ) ) ;
#30139=CARTESIAN_POINT ( 'NONE',  ( 9.532392757686999119, 4.863450031739999346, -8.443842375698499936 ) ) ;
#30159=EDGE_CURVE ( 'NONE', #43855, #41213, #7819, .T. ) ;
#30160=CARTESIAN_POINT ( 'NONE',  ( 11.36749010443639918, 4.863785690678500195, -7.564597762509089662 ) ) ;
#30163=CARTESIAN_POINT ( 'NONE',  ( 9.075405316139999456, 3.757578743663700038, -8.615780615741000403 ) ) ;
#30193=ORIENTED_EDGE ( 'NONE', *, *, #32606, .F. ) ;
#30196=ORIENTED_EDGE ( 'NONE', *, *, #1173, .T. ) ;
#30208=CARTESIAN_POINT ( 'NONE',  ( 8.731616107288068918, 4.000002263255227675, -8.381579007094499545 ) ) ;
#30264=ORIENTED_EDGE ( 'NONE', *, *, #5537, .T. ) ;
#30270=CARTESIAN_POINT ( 'NONE',  ( 10.76857802013509868, 2.825431102905000103, -7.472656658230009796 ) ) ;
#30291=CARTESIAN_POINT ( 'NONE',  ( 11.16486084871730000, 5.207010770456999893, -7.174999999999999822 ) ) ;
#30320=CARTESIAN_POINT ( 'NONE',  ( 11.04333729122639873, 2.996877626170000308, -7.473611442402849470 ) ) ;
#30322=CARTESIAN_POINT ( 'NONE',  ( 9.047113844317999920, 4.253652595614200393, -6.528144732449299603 ) ) ;
#30361=CARTESIAN_POINT ( 'NONE',  ( 11.48011496860029901, 4.919769165942200040, -7.028661263734299780 ) ) ;
#30414=CARTESIAN_POINT ( 'NONE',  ( 10.30226354018233437, 2.907767014557178786, -6.870476274536374994 ) ) ;
#30420=CARTESIAN_POINT ( 'NONE',  ( 11.59999999999999964, 3.182579051151299687, -7.174999999999999822 ) ) ;
#30445=CARTESIAN_POINT ( 'NONE',  ( 11.33830977893730108, 3.023401864784708515, -6.673569913327193959 ) ) ;
#30457=ADVANCED_FACE ( 'NONE', ( #22965 ), #376, .T. ) ;
#30489=CARTESIAN_POINT ( 'NONE',  ( 11.19102897915239936, 4.256858847510399890, -8.470038342183499935 ) ) ;
#30491=CARTESIAN_POINT ( 'NONE',  ( 10.40480513895999870, 4.779740423663599636, -7.066537524675499782 ) ) ;
#30492=CARTESIAN_POINT ( 'NONE',  ( 9.073392757686999488, 4.863450031739999346, -8.443842375698499936 ) ) ;
#30542=CARTESIAN_POINT ( 'NONE',  ( 9.909870477708999204, 2.749999999999999556, -7.750389189149368363 ) ) ;
#30575=CARTESIAN_POINT ( 'NONE',  ( 9.779346873515665450, 3.836375382625536012, -6.249999999999999112 ) ) ;
#30596=CYLINDRICAL_SURFACE ( 'NONE', #27182, 1.250000000000000222 ) ;
#30603=CARTESIAN_POINT ( 'NONE',  ( 11.56322412107030928, 4.054600656575539475, -6.467939235001000320 ) ) ;
#30652=CARTESIAN_POINT ( 'NONE',  ( 11.00000000000000000, 4.000000000000000000, -7.500000000000000000 ) ) ;
#30656=CARTESIAN_POINT ( 'NONE',  ( 11.43302763632549990, 2.964209339073000216, -7.022058766158599141 ) ) ;
#30659=CARTESIAN_POINT ( 'NONE',  ( 9.528367640780999182, 4.473477001189199775, -6.614188603779100006 ) ) ;
#30681=CARTESIAN_POINT ( 'NONE',  ( 8.710288521113000115, 3.647046440108700160, -8.284550957747498501 ) ) ;
#30696=CARTESIAN_POINT ( 'NONE',  ( 10.59725056272499977, 5.316133253199000208, -7.519505747156228992 ) ) ;
#30704=CARTESIAN_POINT ( 'NONE',  ( 9.552263540183332680, 5.092232985442822546, -8.129523725463625894 ) ) ;
#30742=CARTESIAN_POINT ( 'NONE',  ( 10.91195257254739914, 2.772832764353999835, -7.856899084262298771 ) ) ;
#30770=CARTESIAN_POINT ( 'NONE',  ( 10.35376078907947495, 4.858294075600578132, -7.665591875800525479 ) ) ;
#30792=CARTESIAN_POINT ( 'NONE',  ( 10.89393020684959978, 2.750000000000000000, -7.500000000000000000 ) ) ;
#30832=CARTESIAN_POINT ( 'NONE',  ( 10.72333863405319931, 4.619094858989799768, -8.289729326049599223 ) ) ;
#30836=CARTESIAN_POINT ( 'NONE',  ( 8.769442991499998286, 3.919472480837189909, -6.223324745230999433 ) ) ;
#30846=CARTESIAN_POINT ( 'NONE',  ( 8.796304629759626792, 4.535214477905362251, -8.192154231972200051 ) ) ;
#30886=ORIENTED_EDGE ( 'NONE', *, *, #4951, .T. ) ;
#30909=ORIENTED_EDGE ( 'NONE', *, *, #16863, .T. ) ;
#30916=CARTESIAN_POINT ( 'NONE',  ( 10.84657802013509986, 2.684088780794000151, -7.469366283838649423 ) ) ;
#30917=CARTESIAN_POINT ( 'NONE',  ( 10.19391290906799874, 3.451408805716100314, -8.171383386399000415 ) ) ;
#30921=ORIENTED_EDGE ( 'NONE', *, *, #67828, .T. ) ;
#30939=ORIENTED_EDGE ( 'NONE', *, *, #36751, .F. ) ;
#30952=CARTESIAN_POINT ( 'NONE',  ( 11.47500581613029880, 4.988618570924500339, -8.134817373646898275 ) ) ;
#30955=ADVANCED_FACE ( 'NONE', ( #67639 ), #30596, .T. ) ;
#30970=DIRECTION ( 'NONE',  ( 0.000000000000000000, 1.000000000000000000, 0.000000000000000000 ) ) ;
#30981=CARTESIAN_POINT ( 'NONE',  ( 11.37077408945316925, 2.816736291912564472, -7.913130250469239790 ) ) ;
#31007=CARTESIAN_POINT ( 'NONE',  ( 11.01872200990539952, 3.052519557825900343, -7.169497859994799605 ) ) ;
#31011=CARTESIAN_POINT ( 'NONE',  ( 9.095759580228998331, 3.156743194445300382, -7.298441312785299395 ) ) ;
#31037=CARTESIAN_POINT ( 'NONE',  ( 11.59999999999999964, 2.500145227336000087, -7.825000000000000178 ) ) ;
#31045=CARTESIAN_POINT ( 'NONE',  ( 11.00008140503725329, 5.084125838812211917, -7.367730262387956586 ) ) ;
#31050=CARTESIAN_POINT ( 'NONE',  ( 11.01790547754519878, 5.174295865741999734, -7.537269019642879542 ) ) ;
#31073=ORIENTED_EDGE ( 'NONE', *, *, #25089, .F. ) ;
#31079=MANIFOLD_SOLID_BREP ( 'Stock-MAS-678-1', #25837 ) ;
#31095=CARTESIAN_POINT ( 'NONE',  ( 10.49349279008999858, 3.667611644732699627, -8.734031750754999379 ) ) ;
#31097=CARTESIAN_POINT ( 'NONE',  ( 11.59999999999999964, 3.707964997157290110, -8.536357045506706598 ) ) ;
#31126=ADVANCED_FACE ( 'NONE', ( #46843 ), #52073, .T. ) ;
#31127=CARTESIAN_POINT ( 'NONE',  ( 11.06623059009866061, 3.312237475846870893, -6.964041498692941090 ) ) ;
#31144=CARTESIAN_POINT ( 'NONE',  ( 11.25158531382730054, 4.272452942476326676, -6.250000000000000000 ) ) ;
#31186=CARTESIAN_POINT ( 'NONE',  ( 10.20641772631199906, 4.431553727090300043, -8.388315195900499788 ) ) ;
#31190=CARTESIAN_POINT ( 'NONE',  ( 9.149380199233998923, 5.269225938816000543, -7.340469740450900282 ) ) ;
#31265=CARTESIAN_POINT ( 'NONE',  ( 9.586013376692998023, 3.227076647348800176, -7.107192877568799361 ) ) ;
#31270=CARTESIAN_POINT ( 'NONE',  ( 9.748096873515667227, 4.327184855449106138, -6.282534154164607365 ) ) ;
#31287=ORIENTED_EDGE ( 'NONE', *, *, #16863, .F. ) ;
#31320=CARTESIAN_POINT ( 'NONE',  ( 11.46550210169813511, 3.941925478257526372, -8.807012707104282967 ) ) ;
#31348=CARTESIAN_POINT ( 'NONE',  ( 10.52226222744799955, 3.119510978356100139, -8.225278704382400718 ) ) ;
#31351=CARTESIAN_POINT ( 'NONE',  ( 9.501025935145998247, 3.874109063559000088, -6.642177514500700042 ) ) ;
#31368=ORIENTED_EDGE ( 'NONE', *, *, #68467, .F. ) ;
#31389=CARTESIAN_POINT ( 'NONE',  ( 10.44999293566599974, 4.720032669050099550, -8.383280442119700027 ) ) ;
#31493=EDGE_CURVE ( 'NONE', #64217, #6549, #17731, .T. ) ;
#31519=CARTESIAN_POINT ( 'NONE',  ( 10.67410807141119911, 4.046361247106100123, -8.502397868920999358 ) ) ;
#31522=CARTESIAN_POINT ( 'NONE',  ( 8.577265421554999492, 3.785712956512099936, -8.608472884860999486 ) ) ;
#31602=CARTESIAN_POINT ( 'NONE',  ( 11.55811496860034815, 5.045590851977999947, -6.964183526617899744 ) ) ;
#31603=CARTESIAN_POINT ( 'NONE',  ( 9.231405316140000039, 3.815922504313999930, -8.347244604637999998 ) ) ;
#31607=EDGE_LOOP ( 'NONE', ( #53320, #33469, #22862, #64448 ) ) ;
#31629=CARTESIAN_POINT ( 'NONE',  ( 8.710288521113000115, 3.647046440108700160, -8.284550957747498501 ) ) ;
#31691=CARTESIAN_POINT ( 'NONE',  ( 11.01456785386839954, 3.053605396817899997, -8.136888821800198457 ) ) ;
#31693=CARTESIAN_POINT ( 'NONE',  ( 10.23557120343299864, 3.957971921952620598, -8.365991721916298474 ) ) ;
#31733=CARTESIAN_POINT ( 'NONE',  ( 11.23078751119019891, 3.084247107206000038, -7.979095341142500075 ) ) ;
#31751=CARTESIAN_POINT ( 'NONE',  ( 8.969356963619999235, 2.880642974985999860, -7.499999999914821025 ) ) ;
#31806=CARTESIAN_POINT ( 'NONE',  ( 10.42760663304247615, 4.647051049978554005, -6.912280214781111098 ) ) ;
#31865=CARTESIAN_POINT ( 'NONE',  ( 9.758342523874999230, 2.871335344632000020, -7.327226901081999699 ) ) ;
#31867=CARTESIAN_POINT ( 'NONE',  ( 10.30072469555899950, 4.570852684939899824, -6.512367818249299667 ) ) ;
#31870=CARTESIAN_POINT ( 'NONE',  ( 9.453329965421998438, 3.111510091554099855, -8.420309768537698858 ) ) ;
#31924=CARTESIAN_POINT ( 'NONE',  ( 10.71684687351633869, 4.768183399968648040, -6.500416447002277387 ) ) ;
#31950=CARTESIAN_POINT ( 'NONE',  ( 11.30367835872029936, 2.886444435522000251, -6.798177532456199934 ) ) ;
#31951=CARTESIAN_POINT ( 'NONE',  ( 9.206076168957999073, 3.560025096655699883, -8.247081005603298820 ) ) ;
#31958=AXIS2_PLACEMENT_3D ( 'NONE', #42926, #26161, #53072 ) ;
#31976=CARTESIAN_POINT ( 'NONE',  ( 8.761230081853241813, 4.521411717137521435, -8.281074114623761417 ) ) ;
#31990=CARTESIAN_POINT ( 'NONE',  ( 10.77879632507499785, 4.423544049216699747, -8.285174533868300273 ) ) ;
#32024=ORIENTED_EDGE ( 'NONE', *, *, #59063, .T. ) ;
#32042=CARTESIAN_POINT ( 'NONE',  ( 11.03918313518939875, 3.292400735470800033, -8.394758848575399668 ) ) ;
#32044=CARTESIAN_POINT ( 'NONE',  ( 9.956950584426998319, 4.344127791340399725, -6.704208565179699875 ) ) ;
#32068=PLANE ( 'NONE',  #43347 ) ;
#32085=CARTESIAN_POINT ( 'NONE',  ( 11.59603632436369125, 3.157359628034400068, -7.303218851299499548 ) ) ;
#32101=CARTESIAN_POINT ( 'NONE',  ( 11.52531641787287597, 3.660964319297691283, -6.691293037684439504 ) ) ;
#32115=CARTESIAN_POINT ( 'NONE',  ( 8.770072224255999416, 4.093776898754200033, -8.386086300777899183 ) ) ;
#32124=CARTESIAN_POINT ( 'NONE',  ( 11.61364291764652812, 3.140345330584100036, -7.393734108507599601 ) ) ;
#32209=CARTESIAN_POINT ( 'NONE',  ( 11.38379707368349969, 3.433355370490100533, -6.509947486183500054 ) ) ;
#32215=CARTESIAN_POINT ( 'NONE',  ( 10.29025461470400060, 2.893436332050999926, -7.781516069110699263 ) ) ;
#32217=CARTESIAN_POINT ( 'NONE',  ( 11.33456651104149948, 4.112542507956200133, -6.364824110469998963 ) ) ;
#32279=CARTESIAN_POINT ( 'NONE',  ( 10.34184687351645771, 3.000416447002276943, -6.731816600031354625 ) ) ;
#32301=CARTESIAN_POINT ( 'NONE',  ( 11.13746005378019888, 5.161099018038999731, -6.879992063401499713 ) ) ;
#32302=CARTESIAN_POINT ( 'NONE',  ( 9.332721904869998752, 4.756019688173900306, -7.924431591189499358 ) ) ;
#32321=CARTESIAN_POINT ( 'NONE',  ( 11.56441235500451015, 3.361299021099800388, -6.914884925939399629 ) ) ;
#32326=VERTEX_POINT ( 'NONE', #17019 ) ;
#32334=CARTESIAN_POINT ( 'NONE',  ( 10.82035090130999855, 4.758726914843000699, -7.969278253227299658 ) ) ;
#32358=CARTESIAN_POINT ( 'NONE',  ( 11.60000000000000142, 4.813860086966098351, -6.684405152318920074 ) ) ;
#32386=CARTESIAN_POINT ( 'NONE',  ( 10.17764828895399809, 5.001141961424000471, -8.046814291299300592 ) ) ;
#32424=CARTESIAN_POINT ( 'NONE',  ( 10.52435971519499880, 4.532462039660099862, -6.614211617270199461 ) ) ;
#32429=ORIENTED_EDGE ( 'NONE', *, *, #32690, .T. ) ;
#32498=CARTESIAN_POINT ( 'NONE',  ( 9.498096873515667227, 3.672815144550898303, -8.717465845835393523 ) ) ;
#32546=CARTESIAN_POINT ( 'NONE',  ( 10.60026222744819790, 3.225465054973100099, -8.138001937130599828 ) ) ;
#32552=CARTESIAN_POINT ( 'NONE',  ( 10.32533997688000049, 4.243109097101799954, -6.385465081946999355 ) ) ;
#32582=CARTESIAN_POINT ( 'NONE',  ( 11.25962254157670905, 4.169672662336058266, -8.360248390549317676 ) ) ;
#32606=EDGE_CURVE ( 'NONE', #35475, #24715, #58442, .T. ) ;
#32636=CARTESIAN_POINT ( 'NONE',  ( 10.52435971519499880, 4.532462039660099862, -6.614211617270199461 ) ) ;
#32637=CARTESIAN_POINT ( 'NONE',  ( 10.21722949779699974, 4.557226039164599563, -8.335668797826500054 ) ) ;
#32659=CARTESIAN_POINT ( 'NONE',  ( 11.51518179236248862, 3.819003318705799899, -6.652923384986699773 ) ) ;
#32670=CARTESIAN_POINT ( 'NONE',  ( 10.32169598648999909, 4.766524664146899681, -7.956401575444799867 ) ) ;
#32690=EDGE_CURVE ( 'NONE', #24715, #57059, #42599, .T. ) ;
#32710=EDGE_CURVE ( 'NONE', #57302, #14855, #23452, .T. ) ;
#32724=CARTESIAN_POINT ( 'NONE',  ( 10.96533729122639933, 2.859653469230999612, -7.470001566214039990 ) ) ;
#32736=CARTESIAN_POINT ( 'NONE',  ( 9.593930206849998754, 5.250000000000000000, -7.500000000000000000 ) ) ;
#32741=CARTESIAN_POINT ( 'NONE',  ( 9.154341692891295068, 5.250000716804955836, -7.336371291557481022 ) ) ;
#32765=CARTESIAN_POINT ( 'NONE',  ( 10.44635971519499940, 4.459622816450200311, -6.735384833238199143 ) ) ;
#32779=CARTESIAN_POINT ( 'NONE',  ( 10.69809687351599869, 4.327184855449106138, -6.282534154164607365 ) ) ;
#32819=AXIS2_PLACEMENT_3D ( 'NONE', #29370, #27982, #60480 ) ;
#32888=CARTESIAN_POINT ( 'NONE',  ( 11.01456785386839954, 3.053605396817899997, -8.136888821800198457 ) ) ;
#32894=CARTESIAN_POINT ( 'NONE',  ( 10.17764828895399809, 5.001141961424000471, -8.046814291299300592 ) ) ;
#32917=FACE_OUTER_BOUND ( 'NONE', #24041, .T. ) ;
#32978=CARTESIAN_POINT ( 'NONE',  ( 11.35034208742529849, 3.369365911179700301, -8.491292290686200062 ) ) ;
#32979=CARTESIAN_POINT ( 'NONE',  ( 9.963938025973998691, 3.477805217445600228, -6.642005297568199573 ) ) ;
#33034=CARTESIAN_POINT ( 'NONE',  ( 9.002599499754321499, 5.050337702473633783, -7.998361244042363261 ) ) ;
#33040=CARTESIAN_POINT ( 'NONE',  ( 11.59999999999999964, 3.182579051151299687, -7.174999999999999822 ) ) ;
#33068=CARTESIAN_POINT ( 'NONE',  ( 10.22272469555899832, 4.639546521693399761, -6.393520617113999549 ) ) ;
#33099=CARTESIAN_POINT ( 'NONE',  ( 11.59456039236534330, 5.314711678001000195, -7.563984187103470092 ) ) ;
#33113=CARTESIAN_POINT ( 'NONE',  ( 10.82035090130999855, 4.758726914843000699, -7.969278253227299658 ) ) ;
#33150=CARTESIAN_POINT ( 'NONE',  ( 10.37581074856900187, 2.827416853083249748, -8.000243450341619322 ) ) ;
#33152=CARTESIAN_POINT ( 'NONE',  ( 10.35826357027499789, 4.850513154668600002, -7.664090691848299386 ) ) ;
#33157=VECTOR ( 'NONE', #33438, 1000.000000000000114 ) ;
#33199=CARTESIAN_POINT ( 'NONE',  ( 10.49809687351654297, 3.672815144550898303, -8.717465845835393523 ) ) ;
#33235=CARTESIAN_POINT ( 'NONE',  ( 10.42795525820099911, 3.905250696375530239, -6.501013802764199490 ) ) ;
#33242=CARTESIAN_POINT ( 'NONE',  ( 10.57149279008999798, 3.703313553258400059, -8.601484120896000007 ) ) ;
#33278=CARTESIAN_POINT ( 'NONE',  ( 11.27531844363630320, 4.339035105373933554, -8.308695084076104465 ) ) ;
#33292=CARTESIAN_POINT ( 'NONE',  ( 8.599999952505998024, 4.000000000000000000, -7.500000000000000000 ) ) ;
#33300=CARTESIAN_POINT ( 'NONE',  ( 8.883506238772763908, 4.136150106583480479, -6.466493704552775945 ) ) ;
#33305=CARTESIAN_POINT ( 'NONE',  ( 10.21627973160999936, 4.114789684104299461, -6.225948307210999566 ) ) ;
#33320=CARTESIAN_POINT ( 'NONE',  ( 9.864763540183249191, 2.782534154164605589, -7.827184855449096368 ) ) ;
#33329=CARTESIAN_POINT ( 'NONE',  ( 10.81013259637009938, 2.968328969579000276, -8.062151801142800167 ) ) ;
#33331=CARTESIAN_POINT ( 'NONE',  ( 8.798797255587999189, 5.003512473869000665, -7.457514444071209780 ) ) ;
#33335=ORIENTED_EDGE ( 'NONE', *, *, #62725, .F. ) ;
#33341=CARTESIAN_POINT ( 'NONE',  ( 9.758812222687625493, 4.162730299909893183, -8.359680823568968577 ) ) ;
#33345=VERTEX_POINT ( 'NONE', #8808 ) ;
#33353=CARTESIAN_POINT ( 'NONE',  ( 10.75210807141120029, 4.040019166404060336, -8.365272822098500427 ) ) ;
#33381=CARTESIAN_POINT ( 'NONE',  ( 11.23627509987185746, 3.727547057523675988, -6.249999999999998224 ) ) ;
#33417=CARTESIAN_POINT ( 'NONE',  ( 10.98579841651039857, 3.550031058388499972, -8.696179055230999211 ) ) ;
#33438=DIRECTION ( 'NONE',  ( -0.5000000000000150990, 0.08222066253632250021, -0.8621135439442261239 ) ) ;
#33446=CARTESIAN_POINT ( 'NONE',  ( 11.17901463001529905, 4.697110652903200290, -6.383488688482000128 ) ) ;
#33460=CARTESIAN_POINT ( 'NONE',  ( 10.52946886766499901, 3.569835351907400423, -6.718432993015899690 ) ) ;
#33469=ORIENTED_EDGE ( 'NONE', *, *, #22954, .T. ) ;
#33471=CARTESIAN_POINT ( 'NONE',  ( 10.79184687351629535, 3.000416447002276943, -6.731816600031355513 ) ) ;
#33499=CARTESIAN_POINT ( 'NONE',  ( 11.38795122972049967, 4.398282450130399646, -6.578956058177199751 ) ) ;
#33502=CARTESIAN_POINT ( 'NONE',  ( 9.555709346417000205, 5.031430618794000331, -7.010219103474399915 ) ) ;
#33571=CARTESIAN_POINT ( 'NONE',  ( 11.00000000000000000, 2.941427501403999667, -7.825000000000000178 ) ) ;
#33581=CARTESIAN_POINT ( 'NONE',  ( 11.53148876160955005, 3.209326035813000022, -8.322268080792200706 ) ) ;
#33590=CARTESIAN_POINT ( 'NONE',  ( 11.52733460557258915, 4.206337284815599986, -8.761245990815998752 ) ) ;
#33648=CARTESIAN_POINT ( 'NONE',  ( 8.923129650240841926, 3.341122914829671497, -6.641242496392400163 ) ) ;
#33653=CARTESIAN_POINT ( 'NONE',  ( 10.06430484851600049, 5.163382381259999931, -8.031907719862799055 ) ) ;
#33676=CARTESIAN_POINT ( 'NONE',  ( 10.60235971519489873, 4.605301262871499546, -6.493038401303000029 ) ) ;
#33677=CARTESIAN_POINT ( 'NONE',  ( 9.735975701333000387, 4.736880367605900588, -8.182531775206799196 ) ) ;
#33686=CARTESIAN_POINT ( 'NONE',  ( 9.708153928322625248, 3.619812067603167538, -8.288028809740389136 ) ) ;
#33698=CARTESIAN_POINT ( 'NONE',  ( 11.73256516821459883, 4.706297556651700020, -8.212808089543500500 ) ) ;
#33724=CARTESIAN_POINT ( 'NONE',  ( 10.39393020684999946, 2.750000000000000000, -7.500000000000000000 ) ) ;
#33765=CARTESIAN_POINT ( 'NONE',  ( 10.88733729122639993, 2.722429312291999803, -7.466391690027689876 ) ) ;
#33796=CARTESIAN_POINT ( 'NONE',  ( 11.34523293495530005, 2.684794526488000432, -7.447129085684729866 ) ) ;
#33816=CARTESIAN_POINT ( 'NONE',  ( 8.849999778957998942, 4.000000000000000000, -7.500000000000000000 ) ) ;
#33844=CARTESIAN_POINT ( 'NONE',  ( 11.14179841651039915, 3.646693590264900031, -8.439215328713499886 ) ) ;
#33848=CARTESIAN_POINT ( 'NONE',  ( 9.859659112603999631, 3.503852111758100296, -8.528383061402999843 ) ) ;
#33926=AXIS2_PLACEMENT_3D ( 'NONE', #46156, #20267, #51056 ) ;
#33927=CARTESIAN_POINT ( 'NONE',  ( 11.42887348028849992, 2.875789035466000065, -8.107837221875000111 ) ) ;
#33935=ORIENTED_EDGE ( 'NONE', *, *, #46455, .F. ) ;
#33937=CARTESIAN_POINT ( 'NONE',  ( 10.51810807141099779, 4.059045408506610109, -8.776647962565998995 ) ) ;
#33998=CARTESIAN_POINT ( 'NONE',  ( 10.34292546752099895, 2.723846966067000164, -7.411581555133209598 ) ) ;
#34024=CARTESIAN_POINT ( 'NONE',  ( 11.58902763632552002, 3.213494089586499847, -7.137085349939700230 ) ) ;
#34026=CARTESIAN_POINT ( 'NONE',  ( 11.60477869730532774, 3.532552483170099844, -6.578238193496799724 ) ) ;
#34027=CARTESIAN_POINT ( 'NONE',  ( 8.697480666858998788, 4.334888990546500231, -8.446938520915798776 ) ) ;
#34037=CARTESIAN_POINT ( 'NONE',  ( 9.404204162135625822, 4.790364090350968773, -7.124690962532754135 ) ) ;
#34048=CARTESIAN_POINT ( 'NONE',  ( 11.28949010443639978, 5.000675062740000065, -7.574834962826040297 ) ) ;
#34111=CARTESIAN_POINT ( 'NONE',  ( 11.03502897915239878, 4.327133900127000388, -8.735435061820998826 ) ) ;
#34132=B_SPLINE_CURVE_WITH_KNOTS ( 'NONE', 3,
 ( #14584, #61101, #24383, #45714 ),
 .UNSPECIFIED., .F., .F.,
 ( 4, 4 ),
 ( 0.000000000000000000, 1.000000000000000000 ),
 .UNSPECIFIED. ) ;
#34180=DIRECTION ( 'NONE',  ( 0.000000000000000000, 1.000000000000000000, 0.000000000000000000 ) ) ;
#34192=CARTESIAN_POINT ( 'NONE',  ( 11.68333460557258796, 4.162011815820000571, -8.490304555719900392 ) ) ;
#34194=CARTESIAN_POINT ( 'NONE',  ( 9.251759580228998914, 2.889471124893000287, -7.234556850645999404 ) ) ;
#34208=VECTOR ( 'NONE', #68770, 1000.000000000000000 ) ;
#34234=CARTESIAN_POINT ( 'NONE',  ( 10.68035971519489813, 4.678140486081599825, -6.371865185335000348 ) ) ;
#34239=ORIENTED_EDGE ( 'NONE', *, *, #35465, .T. ) ;
#34257=AXIS2_PLACEMENT_3D ( 'NONE', #65165, #12043, #59586 ) ;
#34277=CARTESIAN_POINT ( 'NONE',  ( 10.49764694612699856, 2.940513484064000149, -7.922821994243300914 ) ) ;
#34284=CARTESIAN_POINT ( 'NONE',  ( 11.03502897915239878, 4.327133900127000388, -8.735435061820998826 ) ) ;
#34324=AXIS2_PLACEMENT_3D ( 'NONE', #19583, #63242, #14343 ) ;
#34331=CARTESIAN_POINT ( 'NONE',  ( 9.823096873516664829, 2.782534154164606921, -7.172815144550894750 ) ) ;
#34349=CARTESIAN_POINT ( 'NONE',  ( 10.56244474310100045, 5.137935629024000583, -8.052229793103100164 ) ) ;
#34361=EDGE_CURVE ( 'NONE', #8973, #14855, #50845, .T. ) ;
#34363=CARTESIAN_POINT ( 'NONE',  ( 10.04184687351587613, 4.999583552997725278, -8.268183399968640046 ) ) ;
#34370=CARTESIAN_POINT ( 'NONE',  ( 10.92441504065829960, 4.694414232677499577, -6.982228367137699898 ) ) ;
#34373=CARTESIAN_POINT ( 'NONE',  ( 9.835279731608999043, 4.102460098134500299, -6.362794488108000301 ) ) ;
#34383=CARTESIAN_POINT ( 'NONE',  ( 10.03743284169262573, 3.545113930219122800, -6.752597208702827203 ) ) ;
#34388=ORIENTED_EDGE ( 'NONE', *, *, #36387, .T. ) ;
#34396=CARTESIAN_POINT ( 'NONE',  ( 10.29262282008599882, 4.451581486939200083, -8.228386593078399258 ) ) ;
#34406=B_SPLINE_CURVE_WITH_KNOTS ( 'NONE', 3,
 ( #39206, #18918, #60530, #67140, #49692, #44470 ),
 .UNSPECIFIED., .F., .F.,
 ( 4, 1, 1, 4 ),
 ( 0.000000000000000000, 0.3333333333333000081, 0.6666666666667000474, 1.000000000000000000 ),
 .UNSPECIFIED. ) ;
#34486=DIRECTION ( 'NONE',  ( 0.7071067486699967874, -0.7071068137030968037, 9.022793105466955192E-11 ) ) ;
#34493=CARTESIAN_POINT ( 'NONE',  ( 11.00000000000000000, 4.991767524623399233, -7.174999999999999822 ) ) ;
#34519=CARTESIAN_POINT ( 'NONE',  ( 10.88210843320517007, 2.862311695598936723, -8.098394516494941797 ) ) ;
#34542=CARTESIAN_POINT ( 'NONE',  ( 10.57980110216399972, 3.260758259645400337, -7.048535450274799885 ) ) ;
#34545=CARTESIAN_POINT ( 'NONE',  ( 9.655013376692998861, 3.104586782631499897, -7.044942343771899651 ) ) ;
#34557=EDGE_LOOP ( 'NONE', ( #21937, #3433, #48155, #12094 ) ) ;
#34583=CARTESIAN_POINT ( 'NONE',  ( 10.84657802013509986, 2.684088780794000151, -7.469366283838649423 ) ) ;
#34626=CARTESIAN_POINT ( 'NONE',  ( 10.17764828895399809, 5.001141961424000471, -8.046814291299300592 ) ) ;
#34634=CARTESIAN_POINT ( 'NONE',  ( 10.49349279008999858, 3.667611644732699627, -8.734031750754999379 ) ) ;
#34677=CARTESIAN_POINT ( 'NONE',  ( 9.698096873516668381, 4.327184855449106138, -6.282534154164607365 ) ) ;
#34712=CARTESIAN_POINT ( 'NONE',  ( 11.77359063708300013, 4.955772084214699724, -7.768721787835699999 ) ) ;
#34716=CARTESIAN_POINT ( 'NONE',  ( 9.556659112603998807, 3.503852111758100296, -8.528383061402999843 ) ) ;
#34735=CARTESIAN_POINT ( 'NONE',  ( 11.24025954179439957, 4.771812902496799680, -8.141292208271599051 ) ) ;
#34739=ORIENTED_EDGE ( 'NONE', *, *, #42251, .F. ) ;
#34829=CARTESIAN_POINT ( 'NONE',  ( 11.64122412107036908, 4.062069863985690255, -6.326756392227999015 ) ) ;
#34852=CARTESIAN_POINT ( 'NONE',  ( 11.05391045180431675, 5.129049487418005704, -8.114538794791121390 ) ) ;
#34876=CARTESIAN_POINT ( 'NONE',  ( 11.67918044953561996, 5.011483761127000669, -8.027436060358800418 ) ) ;
#34879=CARTESIAN_POINT ( 'NONE',  ( 9.832317406968998696, 4.186809223719299311, -8.486886322867700727 ) ) ;
#34913=EDGE_LOOP ( 'NONE', ( #30909, #5759, #30921, #34739, #19598, #14988, #58575, #46243, #21739, #46198, #38143, #61891 ) ) ;
#34922=CARTESIAN_POINT ( 'NONE',  ( 11.38678751119029897, 2.833702563575000166, -8.110172976325500827 ) ) ;
#34965=CARTESIAN_POINT ( 'NONE',  ( 10.32533997688000049, 4.243109097101799954, -6.385465081946999355 ) ) ;
#34973=CARTESIAN_POINT ( 'NONE',  ( 11.25656651104150008, 4.126085365637900182, -6.228222165170999247 ) ) ;
#34974=EDGE_CURVE ( 'NONE', #2862, #48127, #34132, .T. ) ;
#35038=CARTESIAN_POINT ( 'NONE',  ( 9.101797255588000013, 5.278067516796999925, -7.445890648716809501 ) ) ;
#35045=DIRECTION ( 'NONE',  ( -1.000000000000000000, 0.000000000000000000, 0.000000000000000000 ) ) ;
#35055=CARTESIAN_POINT ( 'NONE',  ( 11.17056785386839834, 3.281375110759499947, -7.983608166707499620 ) ) ;
#35060=CARTESIAN_POINT ( 'NONE',  ( 11.19434208742519843, 3.521141233577200325, -8.252717006421999457 ) ) ;
#35061=CARTESIAN_POINT ( 'NONE',  ( 9.126063610504999701, 4.468346739194200445, -8.541338455964998744 ) ) ;
#35070=CARTESIAN_POINT ( 'NONE',  ( 8.821633776942626071, 4.724939341952408611, -7.989893149673591211 ) ) ;
#35173=CARTESIAN_POINT ( 'NONE',  ( 11.52166954483529793, 4.562096242626500597, -6.632714178206799538 ) ) ;
#35200=ADVANCED_FACE ( 'NONE', ( #44269 ), #27141, .T. ) ;
#35224=CARTESIAN_POINT ( 'NONE',  ( 11.53148876160955005, 3.209326035813000022, -8.322268080792200706 ) ) ;
#35227=CARTESIAN_POINT ( 'NONE',  ( 9.579025935145997650, 3.854158361175799907, -6.506233167833100239 ) ) ;
#35282=ADVANCED_FACE ( 'NONE', ( #20341 ), #68568, .T. ) ;
#35301=ORIENTED_EDGE ( 'NONE', *, *, #14194, .F. ) ;
#35307=CARTESIAN_POINT ( 'NONE',  ( 11.20733594839949809, 4.840266102192999575, -6.537051788466999191 ) ) ;
#35378=CARTESIAN_POINT ( 'NONE',  ( 9.304430433046999127, 2.911395389258000233, -6.828193190755800224 ) ) ;
#35395=CARTESIAN_POINT ( 'NONE',  ( 11.51518179236248862, 3.819003318705799899, -6.652923384986699773 ) ) ;
#35397=CARTESIAN_POINT ( 'NONE',  ( 11.02812378248509795, 3.583106837161099900, -6.711274001288999536 ) ) ;
#35398=CARTESIAN_POINT ( 'NONE',  ( 9.506000818238998562, 2.989704013253000614, -8.032011717116800398 ) ) ;
#35465=EDGE_CURVE ( 'NONE', #28630, #18146, #49978, .T. ) ;
#35475=VERTEX_POINT ( 'NONE', #36690 ) ;
#35514=CARTESIAN_POINT ( 'NONE',  ( 11.59966954483535773, 4.638989336656000440, -6.514072057539499916 ) ) ;
#35566=CARTESIAN_POINT ( 'NONE',  ( 10.47718582084299932, 3.343463760027599818, -6.741111985563299491 ) ) ;
#35568=CARTESIAN_POINT ( 'NONE',  ( 10.33890035061499901, 4.267716286314199969, -8.468075389605498771 ) ) ;
#35609=CARTESIAN_POINT ( 'NONE',  ( 11.22567835872029995, 3.006051690924700370, -6.873560442659099046 ) ) ;
#35650=CARTESIAN_POINT ( 'NONE',  ( 10.07503300763299947, 4.881889043637199777, -8.424978748982498544 ) ) ;
#35734=CARTESIAN_POINT ( 'NONE',  ( 11.65871932425156920, 3.852858594438699935, -8.492622906483498824 ) ) ;
#35736=CARTESIAN_POINT ( 'NONE',  ( 10.69568717260499824, 3.533932086969799879, -8.260703168378098482 ) ) ;
#35737=CARTESIAN_POINT ( 'NONE',  ( 8.999417874593998334, 2.949199072237000063, -7.946712276748498560 ) ) ;
#35785=CARTESIAN_POINT ( 'NONE',  ( 10.05333291544899943, 4.531093146757585011, -8.658936933361781385 ) ) ;
#35821=CARTESIAN_POINT ( 'NONE',  ( 9.893930206848997599, 2.750000000000000000, -7.500000000000000000 ) ) ;
#35848=CARTESIAN_POINT ( 'NONE',  ( 10.43614141025499897, 4.549633050978300730, -8.478951440767898973 ) ) ;
#35871=ORIENTED_EDGE ( 'NONE', *, *, #32690, .F. ) ;
#35897=CARTESIAN_POINT ( 'NONE',  ( 11.45764291764649911, 2.867875922590999771, -7.360052904210999891 ) ) ;
#35899=CARTESIAN_POINT ( 'NONE',  ( 10.40644474310099810, 4.893483781708200198, -7.933599538786499039 ) ) ;
#35939=CARTESIAN_POINT ( 'NONE',  ( 10.77368717260499942, 3.460071470104900015, -8.381256426168800289 ) ) ;
#35965=CARTESIAN_POINT ( 'NONE',  ( 10.64393020684969926, 5.250000000000000000, -7.500000000000000000 ) ) ;
#36051=EDGE_CURVE ( 'NONE', #20133, #60155, #60396, .T. ) ;
#36070=CARTESIAN_POINT ( 'NONE',  ( 10.57564694612699974, 3.068007311611700150, -7.871941502982999772 ) ) ;
#36074=CARTESIAN_POINT ( 'NONE',  ( 8.794772138681999252, 3.523984281974800403, -6.312652778810999621 ) ) ;
#36084=CARTESIAN_POINT ( 'NONE',  ( 9.226900131858625898, 3.814237572305042345, -8.354999759870066711 ) ) ;
#36155=CARTESIAN_POINT ( 'NONE',  ( 10.26990035061499817, 4.231093494672100164, -8.335645555860798694 ) ) ;
#36189=CARTESIAN_POINT ( 'NONE',  ( 11.35545123989519922, 4.475221369382300196, -8.417769225118700405 ) ) ;
#36241=CARTESIAN_POINT ( 'NONE',  ( 11.33456651104149948, 4.112542507956200133, -6.364824110469998963 ) ) ;
#36243=CARTESIAN_POINT ( 'NONE',  ( 10.18491290906799840, 3.451408805716100314, -8.171383386399000415 ) ) ;
#36281=CARTESIAN_POINT ( 'NONE',  ( 11.67403632436368888, 3.023821283238099955, -7.272033745815799755 ) ) ;
#36326=CARTESIAN_POINT ( 'NONE',  ( 10.69041504065829962, 5.024558373595999328, -6.736065107693399945 ) ) ;
#36328=CARTESIAN_POINT ( 'NONE',  ( 11.60000000000000320, 3.450002592736673090, -8.379764693824252930 ) ) ;
#36338=CARTESIAN_POINT ( 'NONE',  ( 10.11476354018233081, 5.217465845835394411, -7.172815144550904520 ) ) ;
#36354=CARTESIAN_POINT ( 'NONE',  ( 10.72299000889467635, 3.772656371820692911, -8.344040565988990465 ) ) ;
#36387=EDGE_CURVE ( 'NONE', #32326, #22792, #43141, .T. ) ;
#36416=CARTESIAN_POINT ( 'NONE',  ( 10.37872469555899890, 4.502158848185001006, -6.631215019384099740 ) ) ;
#36419=CARTESIAN_POINT ( 'NONE',  ( 9.807938025973999885, 3.334935831489500124, -6.407263051216999017 ) ) ;
#36468=ORIENTED_EDGE ( 'NONE', *, *, #4512, .T. ) ;
#36470=EDGE_CURVE ( 'NONE', #63258, #50154, #67684, .T. ) ;
#36496=CARTESIAN_POINT ( 'NONE',  ( 11.09590547754519996, 5.315605332491999846, -7.541753805330609239 ) ) ;
#36497=CARTESIAN_POINT ( 'NONE',  ( 10.06726717315599906, 3.340104753140699767, -6.937642277832399174 ) ) ;
#36503=CARTESIAN_POINT ( 'NONE',  ( 9.643930206848999376, 5.250000000000000000, -7.500000000000000000 ) ) ;
#36524=FACE_OUTER_BOUND ( 'NONE', #64476, .T. ) ;
#36586=CARTESIAN_POINT ( 'NONE',  ( 11.23195122972050086, 4.507250159094099651, -6.326963915009999440 ) ) ;
#36590=CARTESIAN_POINT ( 'NONE',  ( 9.906292290062998163, 4.749786674456300872, -7.064651992867799990 ) ) ;
#36631=CARTESIAN_POINT ( 'NONE',  ( 10.68546886766499959, 3.433493735705800187, -6.470713638631999665 ) ) ;
#36638=CARTESIAN_POINT ( 'NONE',  ( 9.583513540183334456, 5.250000000000000888, -7.663624617374468428 ) ) ;
#36646=CARTESIAN_POINT ( 'NONE',  ( 8.975960865537832234, 2.874039072694928088, -7.646523491995670163 ) ) ;
#36656=VECTOR ( 'NONE', #68589, 1000.000000000000000 ) ;
#36676=B_SPLINE_CURVE_WITH_KNOTS ( 'NONE', 3,
 ( #21838, #37574, #26764, #65172, #58558, #33381, #6795, #53666, #48074, #178 ),
 .UNSPECIFIED., .F., .F.,
 ( 4, 2, 2, 2, 4 ),
 ( 0.000000000000000000, 0.2499999999999997780, 0.4999999999999995559, 0.7499999999999997780, 1.000000000000000000 ),
 .UNSPECIFIED. ) ;
#36677=CARTESIAN_POINT ( 'NONE',  ( 10.22272469555899832, 4.639546521693399761, -6.393520617113999549 ) ) ;
#36687=CARTESIAN_POINT ( 'NONE',  ( 10.10434687351566474, 5.250000000000001776, -7.336375382625535124 ) ) ;
#36690=CARTESIAN_POINT ( 'NONE',  ( 8.736413463905998711, 4.084156314540369870, -8.382409559052598880 ) ) ;
#36723=CARTESIAN_POINT ( 'NONE',  ( 11.37299956498129916, 2.792989229543000107, -7.174999999999999822 ) ) ;
#36751=EDGE_CURVE ( 'NONE', #4423, #3413, #27554, .T. ) ;
#36765=CARTESIAN_POINT ( 'NONE',  ( 11.11718313518939816, 3.377550038693600154, -8.287087605365499599 ) ) ;
#36768=CARTESIAN_POINT ( 'NONE',  ( 8.619480666858999385, 4.380700808321400075, -8.576476893896000320 ) ) ;
#36848=CARTESIAN_POINT ( 'NONE',  ( 11.64122412107036908, 4.062069863985690255, -6.326756392227999015 ) ) ;
#36849=CARTESIAN_POINT ( 'NONE',  ( 8.775480666858998191, 4.289077172771600388, -8.317400147935998689 ) ) ;
#36884=CARTESIAN_POINT ( 'NONE',  ( 11.02755399909320566, 4.133346405062087392, -8.778526265510098625 ) ) ;
#36885=CARTESIAN_POINT ( 'NONE',  ( 11.23589666366019912, 3.960399224793059947, -8.391246537305399045 ) ) ;
#36900=ORIENTED_EDGE ( 'NONE', *, *, #11426, .F. ) ;
#36917=B_SPLINE_CURVE_WITH_KNOTS ( 'NONE', 3,
 ( #5685, #6369, #54270, #58829, #32279, #10590, #38187, #10938, #11615, #53590, #42755, #68975, #15835, #16862, #43453, #64058, #27027, #16180 ),
 .UNSPECIFIED., .F., .F.,
 ( 4, 2, 2, 2, 2, 2, 2, 2, 4 ),
 ( 0.000000000000000000, 0.1250000000000000000, 0.2500000000000000000, 0.3750000000000000000, 0.5000000000000000000, 0.6250000000000000000, 0.7500000000000000000, 0.8750000000000000000, 1.000000000000000000 ),
 .UNSPECIFIED. ) ;
#36938=CARTESIAN_POINT ( 'NONE',  ( 11.57656516821460890, 4.899536366368299589, -8.407828142327998577 ) ) ;
#36940=CARTESIAN_POINT ( 'NONE',  ( 9.171747021775997766, 3.348327362764200288, -8.071865996877098937 ) ) ;
#36957=CARTESIAN_POINT ( 'NONE',  ( 9.227255459545911975, 4.629538885478623023, -6.407745725917160406 ) ) ;
#36973=CARTESIAN_POINT ( 'NONE',  ( 11.00000000000000000, 4.991767524623399233, -7.174999999999999822 ) ) ;
#36979=CARTESIAN_POINT ( 'NONE',  ( 11.47500581613029880, 4.988618570924500339, -8.134817373646898275 ) ) ;
#36993=CARTESIAN_POINT ( 'NONE',  ( 8.982564767455606614, 2.896581991245595233, -7.795647801703331936 ) ) ;
#37020=CARTESIAN_POINT ( 'NONE',  ( 11.58902763632552002, 3.213494089586499847, -7.137085349939700230 ) ) ;
#37047=CARTESIAN_POINT ( 'NONE',  ( 10.55068303964747578, 3.428091289053144308, -6.838932659516637536 ) ) ;
#37053=VECTOR ( 'NONE', #66898, 1000.000000000000000 ) ;
#37106=CARTESIAN_POINT ( 'NONE',  ( 9.175772138681999479, 3.575113238066399912, -6.440186012775000357 ) ) ;
#37107=CARTESIAN_POINT ( 'NONE',  ( 11.01872200990539952, 3.052519557825900343, -7.169497859994799605 ) ) ;
#37111=CARTESIAN_POINT ( 'NONE',  ( 9.200038493598999167, 4.925784867300699865, -6.617216466537199970 ) ) ;
#37185=CARTESIAN_POINT ( 'NONE',  ( 11.83003632436370012, 2.756744593645999775, -7.209663534847899236 ) ) ;
#37187=CARTESIAN_POINT ( 'NONE',  ( 9.965950584426998660, 4.344127791340399725, -6.704208565179699875 ) ) ;
#37194=CARTESIAN_POINT ( 'NONE',  ( 9.716846873515667227, 4.768183399968648040, -6.500416447002277387 ) ) ;
#37220=CARTESIAN_POINT ( 'NONE',  ( 11.10391045180383962, 5.129049487418003928, -8.114538794791117837 ) ) ;
#37221=CARTESIAN_POINT ( 'NONE',  ( 11.40211496860029783, 4.793947479907100018, -7.093139000852099585 ) ) ;
#37248=CARTESIAN_POINT ( 'NONE',  ( 11.59999999999999964, 4.935123867447916979, -6.791171049664775694 ) ) ;
#37250=CARTESIAN_POINT ( 'NONE',  ( 11.59999999999999964, 5.207010770456999893, -7.825000000000000178 ) ) ;
#37273=CARTESIAN_POINT ( 'NONE',  ( 10.39918582084299992, 3.253651555277099927, -6.637298362509499228 ) ) ;
#37277=CARTESIAN_POINT ( 'NONE',  ( 9.779646554150998483, 4.419749732651400365, -8.258629096756299859 ) ) ;
#37293=CARTESIAN_POINT ( 'NONE',  ( 9.352250488097009651, 2.907725329094806188, -6.870455438679060833 ) ) ;
#37346=CARTESIAN_POINT ( 'NONE',  ( 8.776575450301999481, 3.932070968445029902, -8.439408300974900357 ) ) ;
#37354=CARTESIAN_POINT ( 'NONE',  ( 11.41672066707849886, 4.741156262620799922, -7.051685395375099752 ) ) ;
#37385=CARTESIAN_POINT ( 'NONE',  ( 10.31021345716899873, 4.636538040886300394, -8.078719053813800954 ) ) ;
#37391=CARTESIAN_POINT ( 'NONE',  ( 9.643930206848999376, 5.250000000000000000, -7.500000000000000000 ) ) ;
#37394=PRODUCT_DEFINITION_FORMATION_WITH_SPECIFIED_SOURCE ( 'ANY', '', #3134, .NOT_KNOWN. ) ;
#37427=DIRECTION ( 'NONE',  ( 0.7071067617951957152, 0.000000000000000000, -0.7071068005778986532 ) ) ;
#37428=VECTOR ( 'NONE', #38634, 1000.000000000000000 ) ;
#37436=CARTESIAN_POINT ( 'NONE',  ( 10.20641772631199906, 4.431553727090300043, -8.388315195900499788 ) ) ;
#37443=CARTESIAN_POINT ( 'NONE',  ( 9.074455549952999078, 4.888629236328500660, -6.783011486330899231 ) ) ;
#37445=CARTESIAN_POINT ( 'NONE',  ( 11.69559063708295987, 5.086518862378000883, -7.805482129094999166 ) ) ;
#37448=CARTESIAN_POINT ( 'NONE',  ( 10.06122949779699915, 4.709679768527199606, -8.564302809495998758 ) ) ;
#37526=CARTESIAN_POINT ( 'NONE',  ( 9.763317406968999634, 4.161254277581000416, -8.351883209406098629 ) ) ;
#37558=CARTESIAN_POINT ( 'NONE',  ( 10.40480513895999870, 4.779740423663599636, -7.066537524675499782 ) ) ;
#37574=CARTESIAN_POINT ( 'NONE',  ( 11.13220574173981170, 5.136173005413450454, -6.911917091190552753 ) ) ;
#37578=CARTESIAN_POINT ( 'NONE',  ( 8.929547492598356229, 4.733899445644309978, -8.304419251562590532 ) ) ;
#37585=CARTESIAN_POINT ( 'NONE',  ( 11.60000000000000320, 5.139199170149531426, -7.074412716661199418 ) ) ;
#37592=CARTESIAN_POINT ( 'NONE',  ( 8.734020077949999461, 3.936452720224709712, -8.378811912355599745 ) ) ;
#37612=CARTESIAN_POINT ( 'NONE',  ( 10.62072335273219892, 4.397090433355999473, -8.569396700949999612 ) ) ;
#37614=CARTESIAN_POINT ( 'NONE',  ( 9.475696787962998968, 4.148886440911999429, -6.645868410478299459 ) ) ;
#37633=LINE ( 'NONE', #58967, #15288 ) ;
#37649=VERTEX_POINT ( 'NONE', #61278 ) ;
#37656=VECTOR ( 'NONE', #30970, 1000.000000000000000 ) ;
#37657=CARTESIAN_POINT ( 'NONE',  ( 10.64902344389989963, 3.116469856398800253, -6.963800219468099684 ) ) ;
#37662=ORIENTED_EDGE ( 'NONE', *, *, #59063, .F. ) ;
#37780=CARTESIAN_POINT ( 'NONE',  ( 11.48225819896749833, 2.879005208331999910, -7.711331004020999913 ) ) ;
#37789=CARTESIAN_POINT ( 'NONE',  ( 10.64533863405319991, 4.703785194191100416, -8.397761948794601139 ) ) ;
#37876=CARTESIAN_POINT ( 'NONE',  ( 9.356038493598999750, 4.726907342723099426, -6.806856425099999441 ) ) ;
#37895=CARTESIAN_POINT ( 'NONE',  ( 10.77672335273219950, 4.301522290735800169, -8.312023951944400579 ) ) ;
#37905=CARTESIAN_POINT ( 'NONE',  ( 10.97028665956023197, 3.257584962274628904, -8.549395343567624650 ) ) ;
#37906=CARTESIAN_POINT ( 'NONE',  ( 10.28014141025500017, 4.417352327511700594, -8.243346240911998635 ) ) ;
#37918=EDGE_CURVE ( 'NONE', #59647, #60944, #38131, .T. ) ;
#37926=CARTESIAN_POINT ( 'NONE',  ( 8.832144816391009456, 4.216552416542988624, -8.465905425056138967 ) ) ;
#37932=CARTESIAN_POINT ( 'NONE',  ( 11.59999999999999964, 4.590480015894798704, -6.540686298265705467 ) ) ;
#37960=CARTESIAN_POINT ( 'NONE',  ( 10.12841772631199966, 4.490588993294299947, -8.509834072393999804 ) ) ;
#37970=EDGE_CURVE ( 'NONE', #33345, #41213, #25157, .T. ) ;
#37997=CARTESIAN_POINT ( 'NONE',  ( 10.69568717260499824, 3.533932086969799879, -8.260703168378098482 ) ) ;
#38048=EDGE_CURVE ( 'NONE', #22879, #21434, #56270, .T. ) ;
#38104=CARTESIAN_POINT ( 'NONE',  ( 9.143927823787141307, 5.249988444743199700, -7.499999844943244121 ) ) ;
#38120=CARTESIAN_POINT ( 'NONE',  ( 10.50180110216399854, 3.143606124884799957, -6.976989117212499814 ) ) ;
#38126=CARTESIAN_POINT ( 'NONE',  ( 11.40841235500449891, 3.158861363519000154, -6.729431436870699557 ) ) ;
#38131=LINE ( 'NONE', #1773, #22860 ) ;
#38143=ORIENTED_EDGE ( 'NONE', *, *, #8748, .T. ) ;
#38152=CONICAL_SURFACE ( 'NONE', #52678, 0.9999998338055000602, 0.7853981908209605178 ) ;
#38187=CARTESIAN_POINT ( 'NONE',  ( 10.31059687351633158, 3.370476274536378103, -6.407767014557176566 ) ) ;
#38211=CARTESIAN_POINT ( 'NONE',  ( 11.81056516821459823, 4.609678151793300316, -8.115298063151199059 ) ) ;
#38212=CARTESIAN_POINT ( 'NONE',  ( 8.751496707488000126, 4.081676005979390176, -8.356402621895700378 ) ) ;
#38213=CARTESIAN_POINT ( 'NONE',  ( 11.18923293495519822, 2.967327562101000016, -7.458486839450950256 ) ) ;
#38214=CARTESIAN_POINT ( 'NONE',  ( 9.254721904869999349, 4.875830726371099821, -7.991693846894699860 ) ) ;
#38235=CARTESIAN_POINT ( 'NONE',  ( 11.41672066707849886, 4.741156262620799922, -7.051685395375099752 ) ) ;
#38242=B_SPLINE_CURVE_WITH_KNOTS ( 'NONE', 3,
 ( #8019, #13617, #29357, #8363, #45767, #67075, #19188, #36993, #36646, #31751 ),
 .UNSPECIFIED., .F., .F.,
 ( 4, 2, 2, 2, 4 ),
 ( 0.3934091950370091628, 0.5450568962777566639, 0.6967045975185042206, 0.8483522987592517772, 1.000000000000000000 ),
 .UNSPECIFIED. ) ;
#38275=CARTESIAN_POINT ( 'NONE',  ( 11.60000000000000142, 4.187315255316414131, -6.446733142248666226 ) ) ;
#38284=CARTESIAN_POINT ( 'NONE',  ( 10.64393020684969926, 5.250000000000000000, -7.500000000000000000 ) ) ;
#38303=CARTESIAN_POINT ( 'NONE',  ( 10.29657053952199952, 3.497746311184500190, -6.324815923923999605 ) ) ;
#38345=CARTESIAN_POINT ( 'NONE',  ( 11.37299956498129916, 2.792989229543000107, -7.174999999999999822 ) ) ;
#38360=CARTESIAN_POINT ( 'NONE',  ( 10.72934687351609639, 3.836375382625535124, -6.249999999999999112 ) ) ;
#38386=CARTESIAN_POINT ( 'NONE',  ( 10.30903300763299946, 4.597717337857299746, -8.126922218169600143 ) ) ;
#38399=( GEOMETRIC_REPRESENTATION_CONTEXT ( 3 ) GLOBAL_UNCERTAINTY_ASSIGNED_CONTEXT ( ( #23879 ) ) GLOBAL_UNIT_ASSIGNED_CONTEXT ( ( #62404, #66619, #25167 ) ) REPRESENTATION_CONTEXT ( 'NONE', 'WORKASPACE' ) );
#38446=CARTESIAN_POINT ( 'NONE',  ( 9.232128830620874638, 3.792804146276640864, -6.256996123608767668 ) ) ;
#38472=CARTESIAN_POINT ( 'NONE',  ( 11.60533460557258323, 4.184174550317700358, -8.625775273268001087 ) ) ;
#38479=CARTESIAN_POINT ( 'NONE',  ( 10.76841504065829902, 4.914510326623699576, -6.818119527508899935 ) ) ;
#38514=EDGE_CURVE ( 'NONE', #19484, #53681, #59605, .T. ) ;
#38556=CARTESIAN_POINT ( 'NONE',  ( 8.731616107288068918, 4.000002263255227675, -8.381579007094499545 ) ) ;
#38561=CARTESIAN_POINT ( 'NONE',  ( 11.43856039236529831, 5.032284719763000069, -7.550239075043479353 ) ) ;
#38562=CARTESIAN_POINT ( 'NONE',  ( 9.508013376692998619, 3.104586782631499897, -7.044942343771899651 ) ) ;
#38572=CARTESIAN_POINT ( 'NONE',  ( 9.682824781140627834, 3.392296711160748490, -8.129467220476902511 ) ) ;
#38585=CARTESIAN_POINT ( 'NONE',  ( 11.39210538575740017, 4.842454415653899780, -7.298582155985900322 ) ) ;
#38634=DIRECTION ( 'NONE',  ( -1.000000000000000000, 0.000000000000000000, -1.275169027325000072E-14 ) ) ;
#38657=CARTESIAN_POINT ( 'NONE',  ( 8.766480666858997850, 4.289077172771600388, -8.317400147935998689 ) ) ;
#38685=CARTESIAN_POINT ( 'NONE',  ( 11.55300581613033906, 5.107584469683000172, -8.211208432468300344 ) ) ;
#38698=CARTESIAN_POINT ( 'NONE',  ( 11.06967835872019812, 3.245266201729799960, -7.024326263066900111 ) ) ;
#38726=CARTESIAN_POINT ( 'NONE',  ( 11.59999999999999964, 3.116215992411100366, -7.825000000000000178 ) ) ;
#38729=ORIENTED_EDGE ( 'NONE', *, *, #7911, .F. ) ;
#38735=CARTESIAN_POINT ( 'NONE',  ( 11.53564291764652872, 3.004110626587600308, -7.376893506359599506 ) ) ;
#38737=CARTESIAN_POINT ( 'NONE',  ( 10.01163399569799850, 5.134843509922999871, -7.625954975973699312 ) ) ;
#38821=CARTESIAN_POINT ( 'NONE',  ( 11.33456651104149948, 4.112542507956200133, -6.364824110469998963 ) ) ;
#38829=CARTESIAN_POINT ( 'NONE',  ( 10.42380110216399913, 3.026453990125600235, -6.905442784147899360 ) ) ;
#38896=CARTESIAN_POINT ( 'NONE',  ( 10.08963399569799790, 5.271405458160000279, -7.641111829547599932 ) ) ;
#38920=CARTESIAN_POINT ( 'NONE',  ( 11.60988784977536348, 3.148894096305599799, -7.451365240271489832 ) ) ;
#38921=CARTESIAN_POINT ( 'NONE',  ( 9.811963142879999822, 4.982812171771600518, -7.292822454528599785 ) ) ;
#38945=CARTESIAN_POINT ( 'NONE',  ( 11.65871932425156920, 3.852858594438699935, -8.492622906483498824 ) ) ;
#39005=CARTESIAN_POINT ( 'NONE',  ( 8.710288521113000115, 3.647046440108700160, -8.284550957747498501 ) ) ;
#39008=CARTESIAN_POINT ( 'NONE',  ( 10.05041772631199848, 4.549624259497900169, -8.631352948887998977 ) ) ;
#39038=CARTESIAN_POINT ( 'NONE',  ( 10.92968717260509948, 3.312350236372100021, -8.622362941748999532 ) ) ;
#39084=CARTESIAN_POINT ( 'NONE',  ( 10.43210941423799909, 4.641185166475500168, -6.917608226833099394 ) ) ;
#39087=CARTESIAN_POINT ( 'NONE',  ( 9.935646554150999066, 4.552790318865400643, -8.499078230848398974 ) ) ;
#39121=ORIENTED_EDGE ( 'NONE', *, *, #1965, .T. ) ;
#39151=CARTESIAN_POINT ( 'NONE',  ( 9.099999931440999390, 5.064317881551000156, -8.155535999783198875 ) ) ;
#39167=CARTESIAN_POINT ( 'NONE',  ( 10.94072200990529886, 2.922907051630999842, -7.124286150322599376 ) ) ;
#39174=CARTESIAN_POINT ( 'NONE',  ( 11.15810538575740019, 5.242981041160000188, -7.202822423614300362 ) ) ;
#39206=CARTESIAN_POINT ( 'NONE',  ( 11.00000000000000000, 3.031410575668799900, -7.174999999999999822 ) ) ;
#39223=EDGE_CURVE ( 'NONE', #24634, #509, #63673, .T. ) ;
#39257=CARTESIAN_POINT ( 'NONE',  ( 10.87518447801629939, 4.865987311498500389, -7.480906371072489236 ) ) ;
#39261=CARTESIAN_POINT ( 'NONE',  ( 10.68546886766499959, 3.433493735705800187, -6.470713638631999665 ) ) ;
#39262=CARTESIAN_POINT ( 'NONE',  ( 8.849455549952999434, 4.781695603001899997, -6.869290649434700136 ) ) ;
#39284=CARTESIAN_POINT ( 'NONE',  ( 11.14179841651039915, 3.646693590264900031, -8.439215328713499886 ) ) ;
#39292=CARTESIAN_POINT ( 'NONE',  ( 11.41486084871699802, 2.792989229543000107, -7.825000000000000178 ) ) ;
#39347=CARTESIAN_POINT ( 'NONE',  ( 10.69041504065829962, 5.024558373595999328, -6.736065107693399945 ) ) ;
#39351=CARTESIAN_POINT ( 'NONE',  ( 8.791809814040998816, 4.530359890157599878, -8.185876144228299012 ) ) ;
#39377=CARTESIAN_POINT ( 'NONE',  ( 11.83003632436370012, 2.756744593645999775, -7.209663534847899236 ) ) ;
#39419=B_SPLINE_CURVE_WITH_KNOTS ( 'NONE', 3,
 ( #11379, #17324, #49136, #39005 ),
 .UNSPECIFIED., .F., .F.,
 ( 4, 4 ),
 ( 0.000000000000000000, 1.000000000000000000 ),
 .UNSPECIFIED. ) ;
#39420=CARTESIAN_POINT ( 'NONE',  ( 10.59393020684899867, 5.250000000000000000, -7.500000000000000000 ) ) ;
#39426=CARTESIAN_POINT ( 'NONE',  ( 10.34393020684899867, 2.750000000000000000, -7.500000000000000000 ) ) ;
#39428=CARTESIAN_POINT ( 'NONE',  ( 11.07210672858429845, 3.307795442047700263, -6.979277962544199632 ) ) ;
#39430=CARTESIAN_POINT ( 'NONE',  ( 9.454392757686999715, 4.770706668257700400, -8.342464052342599246 ) ) ;
#39471=CARTESIAN_POINT ( 'NONE',  ( 10.80502344389999791, 2.874741265256000489, -6.817099149379099110 ) ) ;
#39489=CARTESIAN_POINT ( 'NONE',  ( 11.00000000000000000, 4.991767524623399233, -7.174999999999999822 ) ) ;
#39512=CARTESIAN_POINT ( 'NONE',  ( 10.81764560330029923, 4.349570499512200428, -6.414140625063999401 ) ) ;
#39520=CARTESIAN_POINT ( 'NONE',  ( 10.19810941423799910, 4.946022705791000007, -6.640722727400100389 ) ) ;
#39535=CARTESIAN_POINT ( 'NONE',  ( 8.710288521113000115, 3.647046440108700160, -8.284550957747498501 ) ) ;
#39576=CARTESIAN_POINT ( 'NONE',  ( 8.824071121570657539, 4.974071175014780799, -7.248446557932072487 ) ) ;
#39579=ADVANCED_FACE ( 'NONE', ( #49957 ), #59636, .F. ) ;
#39596=CARTESIAN_POINT ( 'NONE',  ( 10.05226354018249779, 5.092232985442822546, -8.129523725463625894 ) ) ;
#39602=CARTESIAN_POINT ( 'NONE',  ( 10.38287885159599888, 4.860099138268600072, -7.397393329751199786 ) ) ;
#39604=CARTESIAN_POINT ( 'NONE',  ( 10.44635971519499940, 4.459622816450200311, -6.735384833238199143 ) ) ;
#39605=CARTESIAN_POINT ( 'NONE',  ( 10.03791290906799993, 3.277531639390499851, -8.384179803770500428 ) ) ;
#39630=CARTESIAN_POINT ( 'NONE',  ( 11.58487348028854846, 3.117292544139400157, -7.977261354519500358 ) ) ;
#39695=CARTESIAN_POINT ( 'NONE',  ( 10.66579975933730040, 5.208485784810999775, -7.084213409908699965 ) ) ;
#39729=CARTESIAN_POINT ( 'NONE',  ( 11.67766954483535891, 4.715882430684499305, -6.395429936871999566 ) ) ;
#39751=CARTESIAN_POINT ( 'NONE',  ( 10.86301932002748138, 2.749999999999999112, -7.799851088612627770 ) ) ;
#39755=B_SPLINE_CURVE_WITH_KNOTS ( 'NONE', 3,
 ( #55775, #40715, #2967, #3310, #50524, #23955 ),
 .UNSPECIFIED., .F., .F.,
 ( 4, 2, 4 ),
 ( 0.000000000000000000, 0.1967045975185045814, 0.3934091950370091628 ),
 .UNSPECIFIED. ) ;
#39776=CARTESIAN_POINT ( 'NONE',  ( 10.29262282008599882, 4.451581486939200083, -8.228386593078399258 ) ) ;
#39778=CARTESIAN_POINT ( 'NONE',  ( 10.18692546752099837, 2.997990738918999920, -7.430575645513339822 ) ) ;
#39815=EDGE_CURVE ( 'NONE', #42619, #2862, #66207, .T. ) ;
#39821=CARTESIAN_POINT ( 'NONE',  ( 10.88813259637009878, 2.844182332072999753, -8.129798612793599943 ) ) ;
#39864=CARTESIAN_POINT ( 'NONE',  ( 10.62072335273219892, 4.397090433355999473, -8.569396700949999612 ) ) ;
#39870=ORIENTED_EDGE ( 'NONE', *, *, #11700, .T. ) ;
#39872=CARTESIAN_POINT ( 'NONE',  ( 10.59195391537400077, 5.057233422790000432, -8.218034727798299244 ) ) ;
#39956=CARTESIAN_POINT ( 'NONE',  ( 10.72749279009019929, 3.774717370312400178, -8.336388861178200216 ) ) ;
#39959=CARTESIAN_POINT ( 'NONE',  ( 9.227380199234000102, 5.132898093246000215, -7.357604921762999517 ) ) ;
#39969=CARTESIAN_POINT ( 'NONE',  ( 10.13874943042162613, 3.152062997842154157, -7.715719979441764131 ) ) ;
#39978=PRODUCT_DEFINITION_SHAPE ( 'NONE', 'NONE',  #57742 ) ;
#39983=CARTESIAN_POINT ( 'NONE',  ( 11.41256651104150066, 4.098999650273559503, -6.501426055769400136 ) ) ;
#39991=CARTESIAN_POINT ( 'NONE',  ( 11.43028911132391556, 2.855999340945334808, -8.059011948032956951 ) ) ;
#40044=CARTESIAN_POINT ( 'NONE',  ( 10.32055864497999842, 4.682585200569199912, -8.034587760591801242 ) ) ;
#40054=VECTOR ( 'NONE', #3323, 1000.000000000000114 ) ;
#40127=CARTESIAN_POINT ( 'NONE',  ( 11.26072066707849828, 4.976067344118500380, -6.909591111168198907 ) ) ;
#40129=CARTESIAN_POINT ( 'NONE',  ( 10.28824205624999877, 3.639798001706899822, -8.437601616732200327 ) ) ;
#40208=CARTESIAN_POINT ( 'NONE',  ( 10.86687616594229944, 3.655053560864600204, -6.412662853391999818 ) ) ;
#40215=CARTESIAN_POINT ( 'NONE',  ( 10.12841772631199966, 4.490588993294299947, -8.509834072393999804 ) ) ;
#40227=CARTESIAN_POINT ( 'NONE',  ( 8.731616107288068918, 4.000002263255227675, -8.381579007094499545 ) ) ;
#40255=CARTESIAN_POINT ( 'NONE',  ( 9.666846873516668381, 4.768183399968648040, -6.500416447002280051 ) ) ;
#40275=CARTESIAN_POINT ( 'NONE',  ( 9.152455549953000258, 4.995562869655000071, -6.696732323226999739 ) ) ;
#40282=DIRECTION ( 'NONE',  ( 0.000000000000000000, 1.000000000000000000, 0.000000000000000000 ) ) ;
#40286=EDGE_CURVE ( 'NONE', #24623, #28630, #8577, .T. ) ;
#40292=CARTESIAN_POINT ( 'NONE',  ( 10.77672335273219950, 4.301522290735800169, -8.312023951944400579 ) ) ;
#40293=CARTESIAN_POINT ( 'NONE',  ( 11.56833327354034857, 3.253412192327699959, -7.011667014989399149 ) ) ;
#40294=CARTESIAN_POINT ( 'NONE',  ( 10.18988779216199880, 5.056118594996999782, -7.880862084500499520 ) ) ;
#40303=CARTESIAN_POINT ( 'NONE',  ( 9.049596101582626062, 3.436622489763541122, -6.830568860986387492 ) ) ;
#40339=CARTESIAN_POINT ( 'NONE',  ( 9.893930206848997599, 2.750000000000000000, -7.500000000000000000 ) ) ;
#40345=CARTESIAN_POINT ( 'NONE',  ( 0.000000000000000000, 0.000000000000000000, 0.000000000000000000 ) ) ;
#40402=CARTESIAN_POINT ( 'NONE',  ( 10.51925056272499859, 5.174767082365999471, -7.517410630436119234 ) ) ;
#40424=CARTESIAN_POINT ( 'NONE',  ( 10.92028665956053324, 3.257584962274628460, -8.549395343567624650 ) ) ;
#40434=LINE ( 'NONE', #46032, #19953 ) ;
#40446=CARTESIAN_POINT ( 'NONE',  ( 11.00000000000000000, 5.079754677601000523, -7.825000000000000178 ) ) ;
#40451=CARTESIAN_POINT ( 'NONE',  ( 10.42795525820099911, 3.905250696375530239, -6.501013802764199490 ) ) ;
#40453=CARTESIAN_POINT ( 'NONE',  ( 8.871822372493998188, 3.671800173070400408, -8.573651380901999630 ) ) ;
#40479=EDGE_CURVE ( 'NONE', #64314, #43855, #59130, .T. ) ;
#40494=CARTESIAN_POINT ( 'NONE',  ( 11.80233327354039830, 2.898463260143000042, -6.779499720266399798 ) ) ;
#40537=CARTESIAN_POINT ( 'NONE',  ( 11.25656651104150008, 4.126085365637900182, -6.228222165170999247 ) ) ;
#40545=CARTESIAN_POINT ( 'NONE',  ( 10.37041638348499895, 2.758294858530000226, -7.197535585171899619 ) ) ;
#40549=CARTESIAN_POINT ( 'NONE',  ( 10.23976354018233259, 3.672815144550903632, -6.282534154164605589 ) ) ;
#40582=CARTESIAN_POINT ( 'NONE',  ( 11.16486084871730000, 5.207010770456999893, -7.174999999999999822 ) ) ;
#40594=CARTESIAN_POINT ( 'NONE',  ( 9.771013540183334456, 3.231816600031359066, -6.500416447002272058 ) ) ;
#40609=CARTESIAN_POINT ( 'NONE',  ( 9.887000818240000655, 2.868129552070000088, -8.096031607030200306 ) ) ;
#40625=CARTESIAN_POINT ( 'NONE',  ( 11.73671932425159881, 3.872987101045399783, -8.356835045446798560 ) ) ;
#40628=CARTESIAN_POINT ( 'NONE',  ( 9.683304848515998486, 5.038423216181000086, -7.974775391194199869 ) ) ;
#40695=CYLINDRICAL_SURFACE ( 'NONE', #605, 1.250000000000000222 ) ;
#40698=B_SPLINE_CURVE_WITH_KNOTS ( 'NONE', 3,
 ( #20256, #36687, #36338, #52413, #57652, #67114, #58010, #62218, #4505, #57308, #40549, #10109, #56974, #61877, #30414, #51725, #25158, #67797 ),
 .UNSPECIFIED., .F., .F.,
 ( 4, 2, 2, 2, 2, 2, 2, 2, 4 ),
 ( 0.000000000000000000, 0.1249999999999996669, 0.2499999999999993339, 0.3749999999999990008, 0.4999999999999986677, 0.6249999999999990008, 0.7499999999999993339, 0.8749999999999996669, 1.000000000000000000 ),
 .UNSPECIFIED. ) ;
#40715=CARTESIAN_POINT ( 'NONE',  ( 9.091433907306445406, 4.945719512329345591, -8.331756427597948544 ) ) ;
#40734=ORIENTED_EDGE ( 'NONE', *, *, #10251, .F. ) ;
#40739=FILL_AREA_STYLE ('',( #14178 ) ) ;
#40746=CARTESIAN_POINT ( 'NONE',  ( 10.59725056272499977, 5.316133253199000208, -7.519505747156228992 ) ) ;
#40764=CARTESIAN_POINT ( 'NONE',  ( 11.33570505509991655, 4.908984911270270146, -7.175001305235313431 ) ) ;
#40786=EDGE_CURVE ( 'NONE', #3413, #57059, #39419, .T. ) ;
#40796=CARTESIAN_POINT ( 'NONE',  ( 10.62487750876920067, 3.456442671114800191, -8.343502390669698343 ) ) ;
#40799=CARTESIAN_POINT ( 'NONE',  ( 9.882975701332998852, 4.736880367605800224, -8.182531775206799196 ) ) ;
#40884=CARTESIAN_POINT ( 'NONE',  ( 10.24733997687999931, 4.272363749081500295, -6.251346978035999591 ) ) ;
#40956=CARTESIAN_POINT ( 'NONE',  ( 9.405747021775999528, 3.038503783616799847, -8.343747244947598674 ) ) ;
#40972=CARTESIAN_POINT ( 'NONE',  ( 11.08810207955139937, 3.203462856645999945, -7.174999999999999822 ) ) ;
#40975=CARTESIAN_POINT ( 'NONE',  ( 10.94487616594229884, 3.696562859151900415, -6.543508100188799581 ) ) ;
#40978=ADVANCED_FACE ( 'NONE', ( #56454 ), #44032, .F. ) ;
#40979=CARTESIAN_POINT ( 'NONE',  ( 8.746126402770999064, 5.068373778467000434, -7.097120470443400109 ) ) ;
#40988=CARTESIAN_POINT ( 'NONE',  ( 9.024266954400625096, 3.674418004489155010, -6.687886317613946474 ) ) ;
#41095=CARTESIAN_POINT ( 'NONE',  ( 10.97635090131019986, 4.999207052587699707, -8.118017011233499503 ) ) ;
#41142=B_SPLINE_CURVE_WITH_KNOTS ( 'NONE', 3,
 ( #39151, #1397, #60474, #38104 ),
 .UNSPECIFIED., .F., .F.,
 ( 4, 4 ),
 ( 0.000000000000000000, 0.1494581667962512628 ),
 .UNSPECIFIED. ) ;
#41151=CARTESIAN_POINT ( 'NONE',  ( 10.52641638348499953, 3.025038519517300184, -7.262511127784999410 ) ) ;
#41154=CARTESIAN_POINT ( 'NONE',  ( 9.933633995697999097, 4.998281561686200192, -7.610798122400000310 ) ) ;
#41192=CARTESIAN_POINT ( 'NONE',  ( 10.93479632507519916, 4.557787252275099732, -8.534037301706000278 ) ) ;
#41198=CARTESIAN_POINT ( 'NONE',  ( 9.510596873516666605, 4.629523725463622341, -8.592232985442825210 ) ) ;
#41213=VERTEX_POINT ( 'NONE', #29394 ) ;
#41231=CARTESIAN_POINT ( 'NONE',  ( 10.96118313518939935, 3.207251432249800249, -8.502430091786999711 ) ) ;
#41322=CARTESIAN_POINT ( 'NONE',  ( 10.55103166480599874, 2.999015536536000504, -7.570575893572789816 ) ) ;
#41325=CARTESIAN_POINT ( 'NONE',  ( 8.845430433046999497, 2.911395389258000233, -6.828193190755800224 ) ) ;
#41334=CARTESIAN_POINT ( 'NONE',  ( 9.125583543129625497, 3.128114063008116563, -7.573124426811684629 ) ) ;
#41390=DIRECTION ( 'NONE',  ( -1.000000000000000000, 0.000000000000000000, 0.000000000000000000 ) ) ;
#41406=CARTESIAN_POINT ( 'NONE',  ( 9.054101285863998427, 3.441732526340400167, -6.836640842107200022 ) ) ;
#41439=CARTESIAN_POINT ( 'NONE',  ( 10.98146005378009882, 4.911671201000399556, -7.013182449205100255 ) ) ;
#41464=CARTESIAN_POINT ( 'NONE',  ( 11.42394752546313441, 3.297753801639562443, -8.603859202887296220 ) ) ;
#41472=ORIENTED_EDGE ( 'NONE', *, *, #13109, .F. ) ;
#41478=CARTESIAN_POINT ( 'NONE',  ( 10.53521345716899837, 4.924890298941200228, -8.340879262988799780 ) ) ;
#41487=CARTESIAN_POINT ( 'NONE',  ( 10.84641504065830020, 4.804462279649600376, -6.900173947321999179 ) ) ;
#41489=CARTESIAN_POINT ( 'NONE',  ( 9.830304848515998728, 4.788504886021700102, -7.860510733857099197 ) ) ;
#41525=CARTESIAN_POINT ( 'NONE',  ( 11.68788784977535933, 3.014014167207800465, -7.443657794094239222 ) ) ;
#41531=CARTESIAN_POINT ( 'NONE',  ( 9.354346873516664829, 2.749999999999999112, -7.663624617374463099 ) ) ;
#41547=CARTESIAN_POINT ( 'NONE',  ( 11.46253286130405691, 4.338994305312701805, -6.691343801417681370 ) ) ;
#41601=CARTESIAN_POINT ( 'NONE',  ( 10.31652245563454073, 4.682420780414363826, -8.028218637173727856 ) ) ;
#41661=CARTESIAN_POINT ( 'NONE',  ( 11.14179841651039915, 3.646693590264900031, -8.439215328713499886 ) ) ;
#41664=CARTESIAN_POINT ( 'NONE',  ( 8.820101285864000218, 3.176316400316700150, -6.521261160937499746 ) ) ;
#41677=ORIENTED_EDGE ( 'NONE', *, *, #4774, .T. ) ;
#41745=CARTESIAN_POINT ( 'NONE',  ( 10.14325461470300027, 3.159754091322399816, -7.713763321667399531 ) ) ;
#41777=CARTESIAN_POINT ( 'NONE',  ( 11.30878751119029957, 2.958974835389999836, -8.044634158732998586 ) ) ;
#41829=VECTOR ( 'NONE', #13993, 1000.000000000000000 ) ;
#41830=CARTESIAN_POINT ( 'NONE',  ( 11.28118179236249929, 3.732952383914999839, -6.250199235344999771 ) ) ;
#41832=CARTESIAN_POINT ( 'NONE',  ( 9.982279731608999285, 4.077800926195140008, -6.636486849903699969 ) ) ;
#41849=CARTESIAN_POINT ( 'NONE',  ( 9.164757945270768147, 5.217425660116048469, -7.172825509854747317 ) ) ;
#41870=CARTESIAN_POINT ( 'NONE',  ( 11.55811496860034815, 5.045590851977999947, -6.964183526617899744 ) ) ;
#41877=CARTESIAN_POINT ( 'NONE',  ( 9.385596873516666605, 2.907767014557175678, -8.129523725463620565 ) ) ;
#41914=CARTESIAN_POINT ( 'NONE',  ( 10.86272200990529946, 2.793294545435000220, -7.079074440652799893 ) ) ;
#41944=CARTESIAN_POINT ( 'NONE',  ( 10.64914416493166449, 3.188141180065802160, -7.823998238890133905 ) ) ;
#41968=ORIENTED_EDGE ( 'NONE', *, *, #9375, .T. ) ;
#42011=CARTESIAN_POINT ( 'NONE',  ( 10.62487750876920067, 3.456442671114800191, -8.343502390669698343 ) ) ;
#42014=CARTESIAN_POINT ( 'NONE',  ( 9.529317406968999649, 4.237919115995800290, -8.756892549790999070 ) ) ;
#42035=CARTESIAN_POINT ( 'NONE',  ( 8.599999952505998024, 4.000000000000000000, -7.500000000000000000 ) ) ;
#42069=DIRECTION ( 'NONE',  ( -1.000000000000000000, 0.000000000000000000, -2.609704304917999919E-14 ) ) ;
#42092=CARTESIAN_POINT ( 'NONE',  ( 11.76588784977539781, 2.879134238109999799, -7.435950347916509884 ) ) ;
#42093=CARTESIAN_POINT ( 'NONE',  ( 9.180747021775998107, 3.348327362764200288, -8.071865996877098937 ) ) ;
#42129=CARTESIAN_POINT ( 'NONE',  ( 10.90346005378009941, 4.786957292481900161, -7.079777642108599167 ) ) ;
#42184=CARTESIAN_POINT ( 'NONE',  ( 10.25149413291699929, 5.037815157227999663, -7.026470926762800495 ) ) ;
#42189=CARTESIAN_POINT ( 'NONE',  ( 10.32844474310100047, 4.771257858050099721, -7.874284411628199365 ) ) ;
#42195=ORIENTED_EDGE ( 'NONE', *, *, #14194, .T. ) ;
#42206=CARTESIAN_POINT ( 'NONE',  ( 9.310585478579783469, 3.370455731697034718, -6.407725666907083450 ) ) ;
#42227=CARTESIAN_POINT ( 'NONE',  ( 11.10101463001529964, 4.622233839778099984, -6.503413421344399481 ) ) ;
#42251=EDGE_CURVE ( 'NONE', #23464, #68105, #28393, .T. ) ;
#42270=CARTESIAN_POINT ( 'NONE',  ( 11.63825819896753977, 3.148796120250299868, -7.660469764776300039 ) ) ;
#42271=CARTESIAN_POINT ( 'NONE',  ( 10.17349413291699811, 5.162701151235999930, -6.969488574374499201 ) ) ;
#42303=CARTESIAN_POINT ( 'NONE',  ( 10.99375810342578141, 4.001859925960030928, -6.625879789168364731 ) ) ;
#42349=VERTEX_POINT ( 'NONE', #57578 ) ;
#42359=CARTESIAN_POINT ( 'NONE',  ( 8.949822372493999367, 3.632306086542600010, -8.702849744394999476 ) ) ;
#42360=CARTESIAN_POINT ( 'NONE',  ( 11.51102763632551884, 3.088851714329700293, -7.079572058049399708 ) ) ;
#42363=CARTESIAN_POINT ( 'NONE',  ( 9.985242056249999720, 3.541248877825399877, -8.694123841252999085 ) ) ;
#42407=ORIENTED_EDGE ( 'NONE', *, *, #8748, .F. ) ;
#42411=CARTESIAN_POINT ( 'NONE',  ( 10.84184687351628540, 3.000416447002276943, -6.731816600031354625 ) ) ;
#42433=CARTESIAN_POINT ( 'NONE',  ( 11.59456039236534330, 5.314711678001000195, -7.563984187103470092 ) ) ;
#42434=CARTESIAN_POINT ( 'NONE',  ( 9.636671671056999955, 3.144964309357700216, -7.643603315539799326 ) ) ;
#42444=LINE ( 'NONE', #48030, #50375 ) ;
#42485=ORIENTED_EDGE ( 'NONE', *, *, #1093, .T. ) ;
#42498=CARTESIAN_POINT ( 'NONE',  ( 11.60000000000000320, 3.359735910920770063, -6.808168915892151674 ) ) ;
#42521=CARTESIAN_POINT ( 'NONE',  ( 11.13349010443639919, 5.274453806861999716, -7.595309363461700158 ) ) ;
#42523=CARTESIAN_POINT ( 'NONE',  ( 9.728988259786000015, 3.886559292927400211, -8.359557531806398600 ) ) ;
#42546=EDGE_LOOP ( 'NONE', ( #42195, #48354, #53383, #57572 ) ) ;
#42563=CARTESIAN_POINT ( 'NONE',  ( 11.18412378248529926, 3.450971646934100079, -6.461285588983000316 ) ) ;
#42594=CARTESIAN_POINT ( 'NONE',  ( 8.783078676347997771, 3.752732269140699906, -8.446684196061099215 ) ) ;
#42596=ORIENTED_EDGE ( 'NONE', *, *, #9101, .T. ) ;
#42599=B_SPLINE_CURVE_WITH_KNOTS ( 'NONE', 3,
 ( #40227, #1436, #55271, #39535 ),
 .UNSPECIFIED., .F., .F.,
 ( 4, 4 ),
 ( 0.1836163425310814723, 1.000000000000000000 ),
 .UNSPECIFIED. ) ;
#42619=VERTEX_POINT ( 'NONE', #61380 ) ;
#42620=CARTESIAN_POINT ( 'NONE',  ( 11.20596535229475776, 3.091087823720314987, -7.824984935920127782 ) ) ;
#42634=CARTESIAN_POINT ( 'NONE',  ( 10.40299135172147693, 4.795252583382552558, -7.137146156348714854 ) ) ;
#42685=CARTESIAN_POINT ( 'NONE',  ( 11.70379573085659786, 5.106255642043000087, -7.691418046581699919 ) ) ;
#42691=CARTESIAN_POINT ( 'NONE',  ( 9.606367640780998585, 4.538247246588100303, -6.493012239633999982 ) ) ;
#42693=CARTESIAN_POINT ( 'NONE',  ( 10.89149144726329865, 3.340422662105400065, -6.569275630703699242 ) ) ;
#42698=CARTESIAN_POINT ( 'NONE',  ( 8.896088727410999653, 2.725263018055000153, -7.606911245136100064 ) ) ;
#42724=CARTESIAN_POINT ( 'NONE',  ( 11.14975833414749928, 3.203462856645999945, -7.825000000000000178 ) ) ;
#42749=CARTESIAN_POINT ( 'NONE',  ( 10.85226354018294792, 2.907767014557178342, -6.870476274536370553 ) ) ;
#42755=CARTESIAN_POINT ( 'NONE',  ( 10.24809687351608289, 4.327184855449106138, -6.282534154164607365 ) ) ;
#42776=CARTESIAN_POINT ( 'NONE',  ( 10.92968717260509948, 3.312350236372100021, -8.622362941748999532 ) ) ;
#42777=CARTESIAN_POINT ( 'NONE',  ( 9.510025935145998588, 3.874109063559000088, -6.642177514500700042 ) ) ;
#42802=CARTESIAN_POINT ( 'NONE',  ( 11.58902763632552002, 3.213494089586499847, -7.137085349939700230 ) ) ;
#42812=CARTESIAN_POINT ( 'NONE',  ( 10.65413259636999932, 3.216622244594500302, -7.926858177843299380 ) ) ;
#42831=CARTESIAN_POINT ( 'NONE',  ( 8.856495485442710702, 4.349453410998743941, -8.453238005838597857 ) ) ;
#42837=CARTESIAN_POINT ( 'NONE',  ( 11.59999999999999964, 4.072982449166801189, -6.447388989144585913 ) ) ;
#42859=ADVANCED_FACE ( 'NONE', ( #22154 ), #6610, .F. ) ;
#42864=CARTESIAN_POINT ( 'NONE',  ( 10.42380110216399913, 3.026453990125600235, -6.905442784147899360 ) ) ;
#42868=CARTESIAN_POINT ( 'NONE',  ( 9.931621437244999129, 4.575883738927100097, -6.851875117168399143 ) ) ;
#42885=CARTESIAN_POINT ( 'NONE',  ( 9.216839207166820813, 4.768179003839034813, -6.500433908363888236 ) ) ;
#42926=CARTESIAN_POINT ( 'NONE',  ( 11.59999999999999964, 4.000000000000000000, -7.500000000000000000 ) ) ;
#42933=CARTESIAN_POINT ( 'NONE',  ( 9.643930206848999376, 5.250000000000000000, -7.500000000000000000 ) ) ;
#43029=CARTESIAN_POINT ( 'NONE',  ( 10.74795391537419853, 4.830118059977199785, -8.063786182297898009 ) ) ;
#43034=CARTESIAN_POINT ( 'NONE',  ( 9.707684229509998985, 3.195116560491999991, -6.690125258578699885 ) ) ;
#43036=CARTESIAN_POINT ( 'NONE',  ( 10.71918447801630059, 5.140463864104999558, -7.474854604063350116 ) ) ;
#43092=CARTESIAN_POINT ( 'NONE',  ( 10.69601354018300832, 4.999583552997727054, -6.731816600031361730 ) ) ;
#43093=PRESENTATION_STYLE_ASSIGNMENT (( #59858 ) ) ;
#43119=CARTESIAN_POINT ( 'NONE',  ( 11.05435090131019926, 5.119447121461000449, -8.192386390235398608 ) ) ;
#43120=CARTESIAN_POINT ( 'NONE',  ( 9.659988259785999176, 3.868581654116200141, -8.495776841814999258 ) ) ;
#43141=B_SPLINE_CURVE_WITH_KNOTS ( 'NONE', 3,
 ( #41478, #9998, #8970, #51281 ),
 .UNSPECIFIED., .F., .F.,
 ( 4, 4 ),
 ( 0.000000000000000000, 1.000000000000000000 ),
 .UNSPECIFIED. ) ;
#43143=CARTESIAN_POINT ( 'NONE',  ( 10.80133863405319872, 4.534404523786000674, -8.181696703306599261 ) ) ;
#43152=CARTESIAN_POINT ( 'NONE',  ( 10.91301932002725650, 2.749999999999998224, -7.799851088612626882 ) ) ;
#43153=CARTESIAN_POINT ( 'NONE',  ( 11.27745123989519982, 4.410212499603100689, -8.292221125039500151 ) ) ;
#43187=CARTESIAN_POINT ( 'NONE',  ( 8.741252916288999586, 4.092558584984410608, -8.374574604871998673 ) ) ;
#43192=LINE ( 'NONE', #38284, #37428 ) ;
#43209=CARTESIAN_POINT ( 'NONE',  ( 10.94072200990529886, 2.922907051630999842, -7.124286150322599376 ) ) ;
#43211=LINE ( 'NONE', #28525, #55287 ) ;
#43345=VERTEX_POINT ( 'NONE', #54660 ) ;
#43347=AXIS2_PLACEMENT_3D ( 'NONE', #31037, #58277, #69111 ) ;
#43382=CARTESIAN_POINT ( 'NONE',  ( 11.08841369783139896, 3.942447888101379583, -8.639288317626999003 ) ) ;
#43390=CARTESIAN_POINT ( 'NONE',  ( 10.94072200990529886, 2.922907051630999842, -7.124286150322599376 ) ) ;
#43447=( NAMED_UNIT ( * ) PLANE_ANGLE_UNIT ( ) SI_UNIT ( $, .RADIAN. ) );
#43451=EDGE_CURVE ( 'NONE', #52427, #28311, #7504, .T. ) ;
#43453=CARTESIAN_POINT ( 'NONE',  ( 10.18559687351583243, 5.092232985442825210, -6.870476274536379435 ) ) ;
#43475=CARTESIAN_POINT ( 'NONE',  ( 11.22567835872029995, 3.006051690924700370, -6.873560442659099046 ) ) ;
#43476=CARTESIAN_POINT ( 'NONE',  ( 9.229392757687000071, 4.677963304775400566, -8.241085728986799808 ) ) ;
#43494=DIRECTION ( 'NONE',  ( 0.000000000000000000, 1.000000000000000000, 0.000000000000000000 ) ) ;
#43496=CARTESIAN_POINT ( 'NONE',  ( 11.85159063708299954, 4.825025306051200502, -7.731961446576300467 ) ) ;
#43509=CARTESIAN_POINT ( 'NONE',  ( 11.41486084871699802, 2.792989229543000107, -7.825000000000000178 ) ) ;
#43560=CARTESIAN_POINT ( 'NONE',  ( 10.44426222744799837, 3.013556901740999994, -8.312555471636301263 ) ) ;
#43603=CARTESIAN_POINT ( 'NONE',  ( 10.40480513895999870, 4.779740423663599636, -7.066537524675499782 ) ) ;
#43619=CARTESIAN_POINT ( 'NONE',  ( 10.82309687351639660, 2.782534154164606921, -7.172815144550894750 ) ) ;
#43620=CARTESIAN_POINT ( 'NONE',  ( 11.40221299665285670, 4.908904393308908709, -7.824988380119695996 ) ) ;
#43642=CARTESIAN_POINT ( 'NONE',  ( 10.45672469555900008, 4.433465011431599656, -6.750062220519700062 ) ) ;
#43701=CARTESIAN_POINT ( 'NONE',  ( 9.171146261768624797, 4.712741083356099203, -6.460774852777244170 ) ) ;
#43725=CARTESIAN_POINT ( 'NONE',  ( 11.28533594839949750, 4.750012929834699804, -6.640482273977399430 ) ) ;
#43732=CARTESIAN_POINT ( 'NONE',  ( 11.03918313518939875, 3.292400735470800033, -8.394758848575399668 ) ) ;
#43780=DIRECTION ( 'NONE',  ( -1.000000000000000000, 0.000000000000000000, 0.000000000000000000 ) ) ;
#43788=CARTESIAN_POINT ( 'NONE',  ( 10.82101354018296391, 3.231816600031359510, -6.500416447002272946 ) ) ;
#43819=CARTESIAN_POINT ( 'NONE',  ( 10.89324174884020024, 3.967693531726030010, -8.674442868902998427 ) ) ;
#43820=CARTESIAN_POINT ( 'NONE',  ( 9.432025935145999185, 3.854158361175799907, -6.506233167833100239 ) ) ;
#43840=CARTESIAN_POINT ( 'NONE',  ( 11.85979573085659844, 4.840012015667699785, -7.645349278262099979 ) ) ;
#43855=VERTEX_POINT ( 'NONE', #32736 ) ;
#43875=CARTESIAN_POINT ( 'NONE',  ( 11.60000000000000320, 4.866008700487510552, -6.727195615969563391 ) ) ;
#43950=CARTESIAN_POINT ( 'NONE',  ( 10.90346005378009941, 4.786957292481900161, -7.079777642108599167 ) ) ;
#43990=CARTESIAN_POINT ( 'NONE',  ( 10.82595391537419971, 4.716560378569699452, -7.986661909549199301 ) ) ;
#44032=B_SPLINE_SURFACE_WITH_KNOTS ( 'NONE', 3, 3, ( 
 ( #8559, #66591, #40044, #61355, #36155, #9575, #53268, #30917, #57818, #41745, #5370, #20077, #36497, #68997, #68298, #52230, #37187, #4330, #57467, #5708, #26708, #9927, #25664, #58506, #37526, #48362, #14835, #58852, #10611, #42434, #10962, #31265, #68645, #27049, #42777, #21109, #58169, #63401, #46996, #26360, #10270, #32302, #20763, #20417, #53610, #31603, #31951, #42093, #52575, #52925, #48022, #15857, #41406, #62712, #5021, #63046, #4669, #125, #15522, #15173, #26011, #47340, #47686, #36849, #63745, #21442, #64084 ),
 ( #16202, #54293, #27389, #32637, #469, #27744, #59543, #28082, #12344, #7436, #11638, #22135, #28433, #32979, #28787, #16546, #6395, #64773, #17594, #38921, #21786, #6742, #33677, #49057, #16887, #43120, #23174, #59885, #1856, #22825, #54995, #38562, #1507, #1163, #43820, #44173, #17942, #37876, #59195, #7096, #11297, #38214, #43476, #49747, #64424, #22478, #49396, #48716, #53947, #60242, #6050, #818, #55340, #44523, #65117, #17240, #65818, #39262, #11994, #33331, #60585, #12690, #65469, #34027, #54648, #29482, #57055 ),
 ( #40294, #61962, #14420, #67192, #14075, #56377, #66167, #39605, #56027, #66508, #67535, #24898, #45550, #8480, #2884, #34373, #45882, #3563, #13394, #61613, #18286, #40628, #51466, #29129, #44861, #2539, #34716, #50789, #35398, #13729, #2207, #29824, #3232, #46228, #8136, #7789, #13044, #50098, #24207, #39959, #51129, #23520, #8820, #35061, #24559, #30163, #19659, #61276, #35737, #19304, #18630, #66855, #60932, #9155, #23866, #50437, #56724, #18969, #40979, #55692, #62302, #45203, #25928, #36768, #47946, #31522, #46 ),
 ( #15095, #52844, #58090, #37448, #16122, #20684, #42363, #64005, #47605, #63664, #10193, #46574, #20001, #36419, #46914, #21366, #5286, #47258, #4941, #52496, #14756, #26279, #53188, #62968, #42014, #67882, #21029, #31870, #9493, #25238, #52146, #57733, #9844, #15781, #63315, #51805, #68912, #37111, #26628, #31190, #57388, #62631, #30492, #4592, #20335, #58425, #3903, #10530, #15443, #42698, #58769, #41325, #41664, #36074, #30836, #68217, #68562, #4250, #25588, #53868, #59114, #11907, #6310, #12262, #16460, #27656, #5969 ) ),
 .UNSPECIFIED., .F., .F., .F.,
 ( 4, 4 ),
 ( 4, 1, 1, 1, 1, 1, 1, 1, 1, 1, 1, 1, 1, 1, 1, 1, 1, 1, 1, 1, 1, 1, 1, 1, 1, 1, 1, 1, 1, 1, 1, 1, 1, 1, 1, 1, 1, 1, 1, 1, 1, 1, 1, 1, 1, 1, 1, 1, 1, 1, 1, 1, 1, 1, 1, 1, 1, 1, 1, 1, 1, 1, 1, 1, 4 ),
 ( -0.02000000000000000042, 1.020000000000000018 ),
 ( -0.02000000000000000042, -0.003749999999999999861, 0.01250000000000000069, 0.02875000000000000125, 0.04499999999999999833, 0.06124999999999999889, 0.07749999999999999944, 0.09375000000000000000, 0.1100000000000000006, 0.1262500000000000011, 0.1424999999999999878, 0.1587500000000000022, 0.1749999999999999889, 0.1912500000000000033, 0.2074999999999999900, 0.2237500000000000044, 0.2399999999999999911, 0.2562499999999999778, 0.2725000000000000200, 0.2887500000000000067, 0.3049999999999999933, 0.3212499999999999800, 0.3375000000000000222, 0.3537500000000000089, 0.3699999999999999956, 0.3862499999999999822, 0.4025000000000000244, 0.4187500000000000111, 0.4349999999999999978, 0.4512499999999999845, 0.4675000000000000266, 0.4837500000000000133, 0.5000000000000000000, 0.5162499999999999867, 0.5324999999999999734, 0.5487499999999999600, 0.5649999999999999467, 0.5812500000000000444, 0.5975000000000000311, 0.6137500000000000178, 0.6300000000000000044, 0.6462499999999999911, 0.6624999999999999778, 0.6787499999999999645, 0.6949999999999999512, 0.7112500000000000488, 0.7275000000000000355, 0.7437500000000000222, 0.7600000000000000089, 0.7762499999999999956, 0.7924999999999999822, 0.8087499999999999689, 0.8249999999999999556, 0.8412500000000000533, 0.8575000000000000400, 0.8737500000000000266, 0.8900000000000000133, 0.9062500000000000000, 0.9224999999999999867, 0.9387499999999999734, 0.9549999999999999600, 0.9712499999999999467, 0.9875000000000000444, 1.003749999999999920, 1.020000000000000018 ),
 .UNSPECIFIED. ) ;
#44038=CARTESIAN_POINT ( 'NONE',  ( 10.44601354018326944, 3.000416447002273834, -8.268183399968640046 ) ) ;
#44067=CARTESIAN_POINT ( 'NONE',  ( 11.10328610135029948, 3.121939224269600022, -7.825000000000000178 ) ) ;
#44070=ORIENTED_EDGE ( 'NONE', *, *, #36387, .F. ) ;
#44079=CARTESIAN_POINT ( 'NONE',  ( 10.23103300763299828, 4.692441239783899931, -8.226274395107198600 ) ) ;
#44086=CARTESIAN_POINT ( 'NONE',  ( 11.06379841651039797, 3.598362324325699912, -8.567697191971999970 ) ) ;
#44164=CARTESIAN_POINT ( 'NONE',  ( 9.916846873516377059, 3.231816600031355069, -8.499583552997725278 ) ) ;
#44172=CARTESIAN_POINT ( 'NONE',  ( 10.44125056272499918, 5.033400911533000510, -7.515315513715298934 ) ) ;
#44173=CARTESIAN_POINT ( 'NONE',  ( 9.406696787962999906, 4.172481380750499902, -6.510508982544899403 ) ) ;
#44198=CARTESIAN_POINT ( 'NONE',  ( 11.04333729122639873, 2.996877626170000308, -7.473611442402849470 ) ) ;
#44264=CARTESIAN_POINT ( 'NONE',  ( 10.07503300763299947, 4.881889043637199777, -8.424978748982498544 ) ) ;
#44267=CARTESIAN_POINT ( 'NONE',  ( 8.741151519676998660, 4.018750234858180725, -8.366807394121199337 ) ) ;
#44269=FACE_OUTER_BOUND ( 'NONE', #24971, .T. ) ;
#44294=CARTESIAN_POINT ( 'NONE',  ( 11.05435090131019926, 5.119447121461000449, -8.192386390235398608 ) ) ;
#44304=VERTEX_POINT ( 'NONE', #60260 ) ;
#44340=CARTESIAN_POINT ( 'NONE',  ( 10.42363156114900136, 3.315688435009791935, -8.575598637068461372 ) ) ;
#44343=CARTESIAN_POINT ( 'NONE',  ( 11.26487482311540056, 4.930401445321599851, -7.875904247640098887 ) ) ;
#44345=CARTESIAN_POINT ( 'NONE',  ( 10.23959632033899858, 2.942832934044000037, -7.068569539041399175 ) ) ;
#44427=CARTESIAN_POINT ( 'NONE',  ( 11.10887482311539998, 5.184953745778000389, -7.978749413531599721 ) ) ;
#44436=CARTESIAN_POINT ( 'NONE',  ( 10.24733997687999931, 4.272363749081500295, -6.251346978035999591 ) ) ;
#44437=CIRCLE ( 'NONE', #25448, 0.7499999936418002555 ) ;
#44470=CARTESIAN_POINT ( 'NONE',  ( 11.08810207955139937, 3.203462856645999945, -7.174999999999999822 ) ) ;
#44499=CARTESIAN_POINT ( 'NONE',  ( 9.962988259787000089, 3.832626376493700082, -8.768215461831999846 ) ) ;
#44520=CARTESIAN_POINT ( 'NONE',  ( 11.19518313518939934, 3.462699341914400097, -8.179416362154199760 ) ) ;
#44522=CARTESIAN_POINT ( 'NONE',  ( 10.93990547754509812, 5.032986398992000510, -7.532784233952049213 ) ) ;
#44523=CARTESIAN_POINT ( 'NONE',  ( 8.950772138681999834, 3.626242194157900389, -6.567719246739500250 ) ) ;
#44548=CARTESIAN_POINT ( 'NONE',  ( 11.75718044953559804, 4.889766368533900120, -7.963966784336999005 ) ) ;
#44557=CARTESIAN_POINT ( 'NONE',  ( 11.59999999999999964, 5.064318446328999634, -8.155535082817699788 ) ) ;
#44569=CARTESIAN_POINT ( 'NONE',  ( 8.807788144226000426, 4.090932644426789722, -8.453461841935100196 ) ) ;
#44639=CARTESIAN_POINT ( 'NONE',  ( 11.42834208742529967, 3.293478249981899975, -8.610579932818998472 ) ) ;
#44689=CARTESIAN_POINT ( 'NONE',  ( 11.24025954179439957, 4.771812902496799680, -8.141292208271599051 ) ) ;
#44691=CARTESIAN_POINT ( 'NONE',  ( 10.08762143724499794, 4.758411336345700349, -6.646450532840099790 ) ) ;
#44729=CARTESIAN_POINT ( 'NONE',  ( 11.46989666366029859, 3.941571897678119996, -8.814970315645998866 ) ) ;
#44745=CARTESIAN_POINT ( 'NONE',  ( 9.201637546194751494, 4.272535203994794806, -6.269669426086102781 ) ) ;
#44770=CARTESIAN_POINT ( 'NONE',  ( 10.66995391537419913, 4.943675741382899780, -8.140910455049299443 ) ) ;
#44777=CARTESIAN_POINT ( 'NONE',  ( 10.22272469555899832, 4.639546521693399761, -6.393520617113999549 ) ) ;
#44850=CARTESIAN_POINT ( 'NONE',  ( 9.948096873516250938, 3.672815144550898303, -8.717465845835395299 ) ) ;
#44857=CARTESIAN_POINT ( 'NONE',  ( 10.33364828895399867, 4.760196147278000112, -7.915211961479200475 ) ) ;
#44859=CARTESIAN_POINT ( 'NONE',  ( 11.35545123989519922, 4.475221369382300196, -8.417769225118700405 ) ) ;
#44861=CARTESIAN_POINT ( 'NONE',  ( 9.607317406968999052, 4.212364169857599983, -8.621889436328999068 ) ) ;
#44871=CARTESIAN_POINT ( 'NONE',  ( 10.28877584378239796, 4.466001735846803378, -8.236827240972795394 ) ) ;
#44874=UNCERTAINTY_MEASURE_WITH_UNIT (LENGTH_MEASURE( 1.000000000000000082E-05 ), #66138, 'distance_accuracy_value', 'NONE');
#44881=CARTESIAN_POINT ( 'NONE',  ( 10.65364694612719809, 3.195501139158400061, -7.821061011719899980 ) ) ;
#44885=EDGE_CURVE ( 'NONE', #62603, #14127, #13842, .T. ) ;
#44962=CARTESIAN_POINT ( 'NONE',  ( 8.599999986286999132, 4.750000013710600655, -7.500000000038047787 ) ) ;
#44996=DIRECTION ( 'NONE',  ( 0.000000000000000000, 0.000000000000000000, -1.000000000000000000 ) ) ;
#45023=CARTESIAN_POINT ( 'NONE',  ( 10.53057053952199951, 3.659587858614300249, -6.703496287302799672 ) ) ;
#45026=CARTESIAN_POINT ( 'NONE',  ( 8.880265421554998539, 3.785712956512099936, -8.608472884860999486 ) ) ;
#45033=AXIS2_PLACEMENT_3D ( 'NONE', #14206, #9978, #20128 ) ;
#45085=CARTESIAN_POINT ( 'NONE',  ( 9.262620115046999558, 3.343122245339613663, -6.424592926396654136 ) ) ;
#45107=CARTESIAN_POINT ( 'NONE',  ( 10.42380110216399913, 3.026453990125600235, -6.905442784147899360 ) ) ;
#45117=CARTESIAN_POINT ( 'NONE',  ( 11.18272066707849888, 5.093522884867000222, -6.838543969064300398 ) ) ;
#45162=CARTESIAN_POINT ( 'NONE',  ( 9.604346873516666605, 5.250000000000001776, -7.336375382625535124 ) ) ;
#45179=CARTESIAN_POINT ( 'NONE',  ( 10.46957120343300041, 3.937990586507050139, -8.777708647662999297 ) ) ;
#45200=CARTESIAN_POINT ( 'NONE',  ( 10.67826222744820086, 3.331419131587999960, -8.050725169876500331 ) ) ;
#45203=CARTESIAN_POINT ( 'NONE',  ( 8.670138961223999630, 4.946050868436800307, -8.139313957553699908 ) ) ;
#45214=CARTESIAN_POINT ( 'NONE',  ( 10.26539516633362759, 4.233208782175254647, -8.343294540545050708 ) ) ;
#45224=CARTESIAN_POINT ( 'NONE',  ( 11.63410404293056999, 3.557672215630899970, -8.400720262063998689 ) ) ;
#45251=CARTESIAN_POINT ( 'NONE',  ( 9.957691290288998687, 3.110563525881361535, -8.413289387078533466 ) ) ;
#45311=LINE ( 'NONE', #65924, #33157 ) ;
#45367=CARTESIAN_POINT ( 'NONE',  ( 11.28533594839949750, 4.750012929834699804, -6.640482273977399430 ) ) ;
#45370=CARTESIAN_POINT ( 'NONE',  ( 10.13626717315599990, 3.235527139800300045, -6.848522029265999400 ) ) ;
#45451=CARTESIAN_POINT ( 'NONE',  ( 10.22687885159599830, 5.132709421626000079, -7.364871923548499844 ) ) ;
#45460=CARTESIAN_POINT ( 'NONE',  ( 11.60118044953561878, 5.133201153721000054, -8.090905336380599167 ) ) ;
#45520=CARTESIAN_POINT ( 'NONE',  ( 8.969356963619999235, 2.880642974985999860, -7.499999999914821025 ) ) ;
#45524=CARTESIAN_POINT ( 'NONE',  ( 9.861671671056999600, 2.738456190347000163, -7.711876388024100137 ) ) ;
#45531=EDGE_LOOP ( 'NONE', ( #29142, #6444, #51196, #41677, #11017 ) ) ;
#45547=CARTESIAN_POINT ( 'NONE',  ( 11.31825954179440075, 4.666231193203100425, -8.053565341712399572 ) ) ;
#45549=CARTESIAN_POINT ( 'NONE',  ( 11.36056039236529891, 4.891071240644300211, -7.543366519014379712 ) ) ;
#45550=CARTESIAN_POINT ( 'NONE',  ( 9.911267173156000254, 3.130949526459800403, -6.759401780699699103 ) ) ;
#45554=ORIENTED_EDGE ( 'NONE', *, *, #9945, .F. ) ;
#45575=LINE ( 'NONE', #68245, #36656 ) ;
#45662=CARTESIAN_POINT ( 'NONE',  ( 11.10101463001529964, 4.622233839778099984, -6.503413421344399481 ) ) ;
#45679=CARTESIAN_POINT ( 'NONE',  ( 10.57101354018312023, 4.768183399968643599, -8.499583552997725278 ) ) ;
#45709=CARTESIAN_POINT ( 'NONE',  ( 10.30487885159599770, 4.996404279947399552, -7.381132626649399064 ) ) ;
#45712=CARTESIAN_POINT ( 'NONE',  ( 9.908304848515998131, 4.913464051101100516, -7.917643062525700159 ) ) ;
#45714=CARTESIAN_POINT ( 'NONE',  ( 11.07299956498199833, 5.207010770456999893, -7.825000000000000178 ) ) ;
#45767=CARTESIAN_POINT ( 'NONE',  ( 9.015584277044482064, 3.283082709547154643, -8.431467892494236338 ) ) ;
#45790=CARTESIAN_POINT ( 'NONE',  ( 10.15303300763299887, 4.787165141710600480, -8.325626572044798834 ) ) ;
#45797=CARTESIAN_POINT ( 'NONE',  ( 10.41964694612699915, 2.813019656517000477, -7.973702485506099613 ) ) ;
#45861=CARTESIAN_POINT ( 'NONE',  ( 9.735025935145998233, 3.814256956409300070, -6.234344474498000110 ) ) ;
#45873=ADVANCED_FACE ( 'NONE', ( #63515 ), #32068, .F. ) ;
#45879=CARTESIAN_POINT ( 'NONE',  ( 10.80133863405319872, 4.534404523786000674, -8.181696703306599261 ) ) ;
#45881=CARTESIAN_POINT ( 'NONE',  ( 11.48522412107029922, 4.047131449166419870, -6.609122077774299164 ) ) ;
#45882=CARTESIAN_POINT ( 'NONE',  ( 9.809950584426999853, 4.453199839589800035, -6.451980747609000311 ) ) ;
#45899=CARTESIAN_POINT ( 'NONE',  ( 11.00000000000000000, 2.941427501403999667, -7.825000000000000178 ) ) ;
#45930=CARTESIAN_POINT ( 'NONE',  ( 10.02145237372899800, 4.043732047787757189, -8.774080944853649200 ) ) ;
#45967=B_SPLINE_CURVE_WITH_KNOTS ( 'NONE', 3,
 ( #16071, #50918, #1378, #64985, #11858, #45679, #59758, #29615, #13528, #22695, #33199, #46015, #61742, #44038, #67322, #66984, #19097, #7927 ),
 .UNSPECIFIED., .F., .F.,
 ( 4, 2, 2, 2, 2, 2, 2, 2, 4 ),
 ( 0.000000000000000000, 0.1250000000000000000, 0.2500000000000000000, 0.3750000000000000000, 0.5000000000000000000, 0.6250000000000000000, 0.7500000000000000000, 0.8750000000000000000, 1.000000000000000000 ),
 .UNSPECIFIED. ) ;
#45993=CARTESIAN_POINT ( 'NONE',  ( 10.77368717260499942, 3.460071470104900015, -8.381256426168800289 ) ) ;
#46015=CARTESIAN_POINT ( 'NONE',  ( 10.47726354018323214, 3.370476274536374106, -8.592232985442821658 ) ) ;
#46018=ORIENTED_EDGE ( 'NONE', *, *, #46715, .F. ) ;
#46032=CARTESIAN_POINT ( 'NONE',  ( 10.89393020684959978, 2.750000000000000000, -7.500000000000000000 ) ) ;
#46048=CARTESIAN_POINT ( 'NONE',  ( 11.60533460557258323, 4.184174550317700358, -8.625775273268001087 ) ) ;
#46052=CARTESIAN_POINT ( 'NONE',  ( 10.16159632033899918, 3.070047649444500149, -7.120485934352199564 ) ) ;
#46101=VERTEX_POINT ( 'NONE', #69026 ) ;
#46134=CARTESIAN_POINT ( 'NONE',  ( 10.83810672858429847, 2.978701842912999886, -6.731711997412900494 ) ) ;
#46156=CARTESIAN_POINT ( 'NONE',  ( 11.59999999999999964, 4.000000000000000000, -7.500000000000000000 ) ) ;
#46198=ORIENTED_EDGE ( 'NONE', *, *, #46715, .T. ) ;
#46207=CARTESIAN_POINT ( 'NONE',  ( 9.279101285863998072, 3.176316400316700150, -6.521261160937499746 ) ) ;
#46224=CARTESIAN_POINT ( 'NONE',  ( 10.77256919669529900, 4.962345366016100101, -7.784327714719899483 ) ) ;
#46228=CARTESIAN_POINT ( 'NONE',  ( 9.379355082327998971, 3.488994418336600400, -6.478918346312998899 ) ) ;
#46243=ORIENTED_EDGE ( 'NONE', *, *, #5537, .F. ) ;
#46292=ORIENTED_EDGE ( 'NONE', *, *, #56579, .F. ) ;
#46338=ORIENTED_EDGE ( 'NONE', *, *, #68467, .T. ) ;
#46343=CARTESIAN_POINT ( 'NONE',  ( 10.44999293566599974, 4.720032669050099550, -8.383280442119700027 ) ) ;
#46376=ORIENTED_EDGE ( 'NONE', *, *, #60926, .F. ) ;
#46392=CARTESIAN_POINT ( 'NONE',  ( 10.45257053952200010, 3.605640676136899980, -6.577269499510100204 ) ) ;
#46395=CARTESIAN_POINT ( 'NONE',  ( 10.08560887879199797, 3.772542739612499751, -6.521682313853199631 ) ) ;
#46435=CARTESIAN_POINT ( 'NONE',  ( 10.93990547754509812, 5.032986398992000510, -7.532784233952049213 ) ) ;
#46455=EDGE_CURVE ( 'NONE', #64217, #52427, #45575, .T. ) ;
#46560=FACE_OUTER_BOUND ( 'NONE', #11407, .T. ) ;
#46569=CARTESIAN_POINT ( 'NONE',  ( 11.31410538575739899, 4.975963290822400076, -7.266662245194900116 ) ) ;
#46573=CARTESIAN_POINT ( 'NONE',  ( 10.73724174883999893, 3.975468761016990094, -8.391788556008700439 ) ) ;
#46574=CARTESIAN_POINT ( 'NONE',  ( 9.858596320338998353, 2.815618218644000414, -7.016653143730500197 ) ) ;
#46624=CARTESIAN_POINT ( 'NONE',  ( 10.08521345716899908, 4.924890298941200228, -8.340879262988799780 ) ) ;
#46647=ORIENTED_EDGE ( 'NONE', *, *, #34974, .T. ) ;
#46691=CARTESIAN_POINT ( 'NONE',  ( 11.76588784977539781, 2.879134238109999799, -7.435950347916509884 ) ) ;
#46715=EDGE_CURVE ( 'NONE', #59938, #18146, #8818, .T. ) ;
#46739=CARTESIAN_POINT ( 'NONE',  ( 10.37872469555899890, 4.502158848185001006, -6.631215019384099740 ) ) ;
#46742=CARTESIAN_POINT ( 'NONE',  ( 9.298392757686999133, 4.585219941293100732, -8.139707405630899117 ) ) ;
#46778=CARTESIAN_POINT ( 'NONE',  ( 10.52799293566599914, 4.806678152079100208, -8.489570425681801424 ) ) ;
#46822=CARTESIAN_POINT ( 'NONE',  ( 10.05041772631199848, 4.549624259497900169, -8.631352948887998977 ) ) ;
#46825=CARTESIAN_POINT ( 'NONE',  ( 11.60000000000000142, 3.310169951859694315, -8.238968815098687060 ) ) ;
#46843=FACE_OUTER_BOUND ( 'NONE', #31607, .T. ) ;
#46895=B_SPLINE_CURVE_WITH_KNOTS ( 'NONE', 3,
 ( #59686, #43620, #18081, #17740 ),
 .UNSPECIFIED., .F., .F.,
 ( 4, 4 ),
 ( 0.000000000000000000, 1.000000000000000000 ),
 .UNSPECIFIED. ) ;
#46905=CARTESIAN_POINT ( 'NONE',  ( 10.07309687351575178, 5.217465845835396188, -7.827184855449103473 ) ) ;
#46911=CARTESIAN_POINT ( 'NONE',  ( 10.23103300763299828, 4.692441239783899931, -8.226274395107198600 ) ) ;
#46914=CARTESIAN_POINT ( 'NONE',  ( 9.782608878791998919, 3.710311786319799854, -6.254020414961999563 ) ) ;
#46920=PLANE ( 'NONE',  #3212 ) ;
#46996=CARTESIAN_POINT ( 'NONE',  ( 9.408709346416998187, 4.783195203880800328, -7.128095150442700145 ) ) ;
#47029=CARTESIAN_POINT ( 'NONE',  ( 11.10612378248509913, 3.517039242046199998, -6.586279795136899651 ) ) ;
#47082=CARTESIAN_POINT ( 'NONE',  ( 11.33041235500449950, 3.057642534728299832, -6.636704692336500067 ) ) ;
#47085=CARTESIAN_POINT ( 'NONE',  ( 10.13425461470299993, 3.159754091322399816, -7.713763321667399531 ) ) ;
#47108=EDGE_LOOP ( 'NONE', ( #8181, #30886, #41968 ) ) ;
#47123=CARTESIAN_POINT ( 'NONE',  ( 11.39700581613019992, 4.869652672166700391, -8.058426314824099990 ) ) ;
#47164=CARTESIAN_POINT ( 'NONE',  ( 10.44426222744799837, 3.013556901740999994, -8.312555471636301263 ) ) ;
#47166=CARTESIAN_POINT ( 'NONE',  ( 11.60000000000000142, 4.325863785438847309, -8.622936771936917211 ) ) ;
#47195=CARTESIAN_POINT ( 'NONE',  ( 11.08126742035591228, 3.231380926423223166, -7.106626190113856545 ) ) ;
#47255=CARTESIAN_POINT ( 'NONE',  ( 10.60026222744819790, 3.225465054973100099, -8.138001937130599828 ) ) ;
#47258=CARTESIAN_POINT ( 'NONE',  ( 9.706621437244999484, 4.849675135054999586, -6.543738240676099771 ) ) ;
#47319=B_SPLINE_SURFACE_WITH_KNOTS ( 'NONE', 3, 3, ( 
 ( #10961, #37185, #63045, #63744, #68644, #26010, #468, #42433, #58505, #58851, #26707, #16545, #48021, #9574, #31950, #21441, #21784, #124, #32301, #36496, #43119, #53267, #5369, #42776, #5020, #30916, #52229, #4329, #68297, #20416, #15172, #47685, #9926, #20762, #68996 ),
 ( #42092, #26359, #63400, #15521, #36848, #58168, #31602, #52924, #59542, #54292, #28432, #32978, #22477, #6393, #43475, #11993, #27743, #17940, #60240, #65116, #49056, #12343, #43819, #28786, #33329, #50097, #1162, #39261, #2206, #33676, #60584, #12689, #17239, #17593, #55339 ),
 ( #54647, #11296, #23519, #34026, #7435, #23173, #48714, #38561, #11637, #44859, #6049, #27388, #1506, #38213, #817, #7095, #22134, #64772, #66166, #44522, #59884, #16886, #49746, #18285, #59194, #6741, #28081, #54994, #49395, #32636, #22824, #44172, #53946, #65468, #1855 ),
 ( #38920, #65817, #40293, #2537, #45881, #55691, #29128, #45549, #56026, #57054, #14419, #35060, #67191, #61612, #23865, #35397, #24206, #9154, #24558, #18629, #51804, #60931, #46573, #35736, #8479, #19303, #66854, #3902, #13043, #39604, #30491, #18968, #2883, #7788, #3562 ) ),
 .UNSPECIFIED., .F., .F., .F.,
 ( 4, 4 ),
 ( 4, 1, 1, 1, 1, 1, 1, 1, 1, 1, 1, 1, 1, 1, 1, 1, 1, 1, 1, 1, 1, 1, 1, 1, 1, 1, 1, 1, 1, 1, 1, 1, 4 ),
 ( -0.02000000000000000042, 1.020000000000000018 ),
 ( 0.1633025096610999927, 0.1899619885200000136, 0.2166214673788000034, 0.2432809462376999965, 0.2699404250964999585, 0.2965999039553000038, 0.3232593828141999692, 0.3499188616730000145, 0.3765783405318000043, 0.4032378193906999697, 0.4298972982494999595, 0.4565567771083000048, 0.4832162559671999702, 0.5098757348260000155, 0.5365352136848999809, 0.5631946925437000262, 0.5898541714025000715, 0.6165136502614000369, 0.6431731291201999712, 0.6698326079790000165, 0.6964920868378999819, 0.7231515656967000272, 0.7498110445554999615, 0.7764705234143999268, 0.8031300022731999722, 0.8297894811320000175, 0.8564489599908999828, 0.8831084388497000282, 0.9097679177085999935, 0.9364273965674000388, 0.9630868754261999731, 0.9897463542851000495, 1.016405833144000015 ),
 .UNSPECIFIED. ) ;
#47333=EDGE_LOOP ( 'NONE', ( #2318, #68683, #54062, #36468, #10749, #64560, #13838, #33335, #15957, #60564, #25782, #41472 ) ) ;
#47340=CARTESIAN_POINT ( 'NONE',  ( 8.826138961223998436, 4.718363881473300658, -7.985449642667900250 ) ) ;
#47352=AXIS2_PLACEMENT_3D ( 'NONE', #42035, #21388, #51827 ) ;
#47376=CARTESIAN_POINT ( 'NONE',  ( 11.11123293495519881, 3.108594079907299967, -7.464165716332529676 ) ) ;
#47392=CARTESIAN_POINT ( 'NONE',  ( 9.343930206849998754, 2.750000000000000000, -7.500000000000000000 ) ) ;
#47399=CARTESIAN_POINT ( 'NONE',  ( 11.57299956498156845, 5.207010770456999893, -7.825000000000000178 ) ) ;
#47425=CARTESIAN_POINT ( 'NONE',  ( 10.81764560330029923, 4.349570499512200428, -6.414140625063999401 ) ) ;
#47427=CARTESIAN_POINT ( 'NONE',  ( 9.070430433046999141, 3.262177192690499883, -7.044669955395099770 ) ) ;
#47465=CARTESIAN_POINT ( 'NONE',  ( 10.31021345716899873, 4.636538040886300394, -8.078719053813800954 ) ) ;
#47467=CARTESIAN_POINT ( 'NONE',  ( 11.56322412107030928, 4.054600656575539475, -6.467939235001000320 ) ) ;
#47474=CARTESIAN_POINT ( 'NONE',  ( 9.427263540183332680, 3.370476274536375438, -8.592232985442821658 ) ) ;
#47509=CARTESIAN_POINT ( 'NONE',  ( 11.56441235500451015, 3.361299021099800388, -6.914884925939399629 ) ) ;
#47510=CARTESIAN_POINT ( 'NONE',  ( 10.93656785386839836, 2.939720539848000413, -8.213529149347399638 ) ) ;
#47517=CARTESIAN_POINT ( 'NONE',  ( 10.07503300763299947, 4.881889043637199777, -8.424978748982498544 ) ) ;
#47528=CARTESIAN_POINT ( 'NONE',  ( 11.36486084871759950, 2.792989229543000107, -7.825000000000000178 ) ) ;
#47601=CARTESIAN_POINT ( 'NONE',  ( 10.50180110216399854, 3.143606124884799957, -6.976989117212499814 ) ) ;
#47605=CARTESIAN_POINT ( 'NONE',  ( 9.934583761885999564, 2.921249888908000081, -8.187519150726398465 ) ) ;
#47661=DIRECTION ( 'NONE',  ( 1.000000000000000000, 0.000000000000000000, 0.000000000000000000 ) ) ;
#47685=CARTESIAN_POINT ( 'NONE',  ( 10.59725056272499977, 5.316133253199000208, -7.519505747156228992 ) ) ;
#47686=CARTESIAN_POINT ( 'NONE',  ( 8.800809814040999157, 4.530359890157599878, -8.185876144228299012 ) ) ;
#47777=CARTESIAN_POINT ( 'NONE',  ( 11.55194988689359903, 4.580487242693600081, -8.638573882912000457 ) ) ;
#47780=CARTESIAN_POINT ( 'NONE',  ( 10.08359632033899800, 3.197262364844699611, -7.172402329663099430 ) ) ;
#47792=B_SPLINE_CURVE_WITH_KNOTS ( 'NONE', 3,
 ( #39426, #11809, #33150, #22991, #44340, #61093, #27908, #49217, #23343, #28602 ),
 .UNSPECIFIED., .F., .F.,
 ( 4, 2, 2, 2, 4 ),
 ( 0.000000000000000000, 0.2500000000000000000, 0.5000000000000000000, 0.7500000000000000000, 1.000000000000000000 ),
 .UNSPECIFIED. ) ;
#47818=CARTESIAN_POINT ( 'NONE',  ( 11.06456920625009843, 4.037149028919880145, -6.467161360063999886 ) ) ;
#47857=CARTESIAN_POINT ( 'NONE',  ( 11.39210538575740017, 4.842454415653899780, -7.298582155985900322 ) ) ;
#47874=PRODUCT_DEFINITION_CONTEXT ( 'detailed design', #25734, 'design' ) ;
#47887=CARTESIAN_POINT ( 'NONE',  ( 10.89529697814178100, 4.826567894363762434, -7.215614489968412926 ) ) ;
#47936=CARTESIAN_POINT ( 'NONE',  ( 10.67410807141119911, 4.046361247106100123, -8.502397868920999358 ) ) ;
#47941=CARTESIAN_POINT ( 'NONE',  ( 9.150442991499998513, 3.928121959910110483, -6.360452723514999462 ) ) ;
#47943=CARTESIAN_POINT ( 'NONE',  ( 11.35918179236250047, 3.761636028845500412, -6.384440618559000136 ) ) ;
#47946=CARTESIAN_POINT ( 'NONE',  ( 8.594151519676998419, 4.024693162376980382, -8.641543873690000765 ) ) ;
#47994=EDGE_CURVE ( 'NONE', #60155, #24623, #7437, .T. ) ;
#48021=CARTESIAN_POINT ( 'NONE',  ( 11.38678751119029897, 2.833702563575000166, -8.110172976325500827 ) ) ;
#48022=CARTESIAN_POINT ( 'NONE',  ( 9.104759580228998672, 3.156743194445300382, -7.298441312785299395 ) ) ;
#48030=CARTESIAN_POINT ( 'NONE',  ( 8.849999778957998942, 4.000000000000000000, -8.499999833805500060 ) ) ;
#48041=CARTESIAN_POINT ( 'NONE',  ( 8.810863317747999801, 4.960863370448500120, -7.500000000073117512 ) ) ;
#48046=CARTESIAN_POINT ( 'NONE',  ( 10.94903032197929882, 4.503839166471300004, -6.795411691360399686 ) ) ;
#48057=CARTESIAN_POINT ( 'NONE',  ( 11.12299956498149811, 5.207010770456999893, -7.825000000000000178 ) ) ;
#48058=CARTESIAN_POINT ( 'NONE',  ( 11.06967835872019812, 3.245266201729799960, -7.024326263066900111 ) ) ;
#48074=CARTESIAN_POINT ( 'NONE',  ( 11.30565467195989093, 2.863826994586553099, -6.911917091190549201 ) ) ;
#48084=CARTESIAN_POINT ( 'NONE',  ( 11.59999999999999964, 4.804380105966678194, -6.677026092743739483 ) ) ;
#48111=CARTESIAN_POINT ( 'NONE',  ( 10.57149279008999798, 3.703313553258400059, -8.601484120896000007 ) ) ;
#48113=CARTESIAN_POINT ( 'NONE',  ( 9.602342523874998648, 3.142972170141900001, -7.368808371628100318 ) ) ;
#48127=VERTEX_POINT ( 'NONE', #21030 ) ;
#48152=CARTESIAN_POINT ( 'NONE',  ( 11.52677869730533011, 3.596497913043499750, -6.704332466833498927 ) ) ;
#48155=ORIENTED_EDGE ( 'NONE', *, *, #60926, .T. ) ;
#48182=CARTESIAN_POINT ( 'NONE',  ( 8.727215710425999973, 3.626036035117899736, -8.308760775591800041 ) ) ;
#48191=CARTESIAN_POINT ( 'NONE',  ( 11.17056785386839834, 3.281375110759499947, -7.983608166707499620 ) ) ;
#48219=CARTESIAN_POINT ( 'NONE',  ( 10.79683585285767577, 4.539293524411616154, -8.187933206668011721 ) ) ;
#48271=CARTESIAN_POINT ( 'NONE',  ( 11.26072066707849828, 4.976067344118500380, -6.909591111168198907 ) ) ;
#48276=CARTESIAN_POINT ( 'NONE',  ( 10.48444474310099928, 5.015709705366000470, -7.992914665944799602 ) ) ;
#48278=CARTESIAN_POINT ( 'NONE',  ( 10.96533729122639933, 2.859653469230999612, -7.470001566214039990 ) ) ;
#48309=B_SPLINE_SURFACE_WITH_KNOTS ( 'NONE', 3, 3, ( 
 ( #61389, #39377, #18404, #18748, #23637, #39729, #60007, #33099, #38685, #12118, #6516, #44639, #55458, #33796, #28553, #27861, #1281, #33446, #28198, #61046, #44294, #65591, #17715, #39038, #55111, #49863, #65931, #18059, #60697, #2315, #28910, #40746, #14532, #8934, #62070 ),
 ( #46691, #50900, #25012, #61724, #34829, #35514, #68332, #56141, #30952, #2996, #19769, #20451, #41777, #3671, #24330, #67994, #14185, #45662, #51577, #62746, #41095, #66968, #29941, #52267, #57501, #30270, #62411, #56836, #19074, #9262, #14866, #40402, #29597, #46343, #35848 ),
 ( #67645, #57164, #13510, #4363, #30603, #35173, #51918, #24673, #56486, #36189, #25697, #67306, #4014, #13844, #8590, #47029, #20110, #25351, #41439, #9610, #8249, #51244, #3339, #45993, #19422, #26742, #58201, #63779, #504, #52960, #4702, #64119, #15890, #68680, #58890 ),
 ( #58538, #15558, #21820, #5057, #26048, #16234, #37221, #20798, #10994, #43153, #36885, #27422, #5406, #47376, #48058, #10645, #64458, #160, #42129, #21477, #32334, #31990, #9962, #21145, #42812, #16582, #53644, #48747, #5740, #851, #37558, #27082, #32670, #48398, #37906 ) ),
 .UNSPECIFIED., .F., .F., .F.,
 ( 4, 4 ),
 ( 4, 1, 1, 1, 1, 1, 1, 1, 1, 1, 1, 1, 1, 1, 1, 1, 1, 1, 1, 1, 1, 1, 1, 1, 1, 1, 1, 1, 1, 1, 1, 1, 4 ),
 ( -0.02000000000000000042, 1.020000000000000018 ),
 ( 0.1633025096610999927, 0.1899619885200000136, 0.2166214673788000034, 0.2432809462376999965, 0.2699404250964999585, 0.2965999039553000038, 0.3232593828141999692, 0.3499188616730000145, 0.3765783405318000043, 0.4032378193906999697, 0.4298972982494999595, 0.4565567771083000048, 0.4832162559671999702, 0.5098757348260000155, 0.5365352136848999809, 0.5631946925437000262, 0.5898541714025000715, 0.6165136502614000369, 0.6431731291201999712, 0.6698326079790000165, 0.6964920868378999819, 0.7231515656967000272, 0.7498110445554999615, 0.7764705234143999268, 0.8031300022731999722, 0.8297894811320000175, 0.8564489599908999828, 0.8831084388497000282, 0.9097679177085999935, 0.9364273965674000388, 0.9630868754261999731, 0.9897463542851000495, 1.016405833144000015 ),
 .UNSPECIFIED. ) ;
#48354=ORIENTED_EDGE ( 'NONE', *, *, #36470, .T. ) ;
#48362=CARTESIAN_POINT ( 'NONE',  ( 9.737988259786000356, 3.886559292927400211, -8.359557531806398600 ) ) ;
#48387=CARTESIAN_POINT ( 'NONE',  ( 11.73671932425159881, 3.872987101045399783, -8.356835045446798560 ) ) ;
#48391=ORIENTED_EDGE ( 'NONE', *, *, #25587, .F. ) ;
#48398=CARTESIAN_POINT ( 'NONE',  ( 10.29399293566599916, 4.546741702992100009, -8.170700474995699736 ) ) ;
#48455=CARTESIAN_POINT ( 'NONE',  ( 11.61759063708296047, 5.217265640542000149, -7.842242470354300110 ) ) ;
#48475=CARTESIAN_POINT ( 'NONE',  ( 9.341834235717472623, 3.000408294236256435, -6.731799792051354814 ) ) ;
#48510=CARTESIAN_POINT ( 'NONE',  ( 9.099999931440999390, 5.246365646610000155, -7.404749409716440134 ) ) ;
#48622=CARTESIAN_POINT ( 'NONE',  ( 11.21149010443640037, 5.137564434800999891, -7.585072163144589652 ) ) ;
#48628=CARTESIAN_POINT ( 'NONE',  ( 10.20226357027499908, 5.120085139777000194, -7.716099591766099053 ) ) ;
#48714=CARTESIAN_POINT ( 'NONE',  ( 11.48011496860029901, 4.919769165942200040, -7.028661263734299780 ) ) ;
#48716=CARTESIAN_POINT ( 'NONE',  ( 9.102747021775998704, 3.245052836381700168, -8.162493079567200382 ) ) ;
#48737=CARTESIAN_POINT ( 'NONE',  ( 10.70287750876920008, 3.530799696887600092, -8.228113772635300194 ) ) ;
#48747=CARTESIAN_POINT ( 'NONE',  ( 10.52946886766499901, 3.569835351907400423, -6.718432993015899690 ) ) ;
#48756=CARTESIAN_POINT ( 'NONE',  ( 11.00000000000000000, 4.991767524623399233, -7.174999999999999822 ) ) ;
#48767=CARTESIAN_POINT ( 'NONE',  ( 9.099999931440999390, 5.246365646610000155, -7.404749409716440134 ) ) ;
#48801=CARTESIAN_POINT ( 'NONE',  ( 10.91195257254739914, 2.772832764353999835, -7.856899084262298771 ) ) ;
#48824=AXIS2_PLACEMENT_3D ( 'NONE', #30652, #19470, #29987 ) ;
#48845=CARTESIAN_POINT ( 'NONE',  ( 11.40211496860029783, 4.793947479907100018, -7.093139000852099585 ) ) ;
#48943=CARTESIAN_POINT ( 'NONE',  ( 9.150818738817875442, 4.951062758656399332, -6.673278530809400699 ) ) ;
#48964=CARTESIAN_POINT ( 'NONE',  ( 10.37872469555899890, 4.502158848185001006, -6.631215019384099740 ) ) ;
#48974=CARTESIAN_POINT ( 'NONE',  ( 11.26072066707849828, 4.976067344118500380, -6.909591111168198907 ) ) ;
#49000=CARTESIAN_POINT ( 'NONE',  ( 11.32240614981507854, 4.732436490098000270, -7.982093918858203629 ) ) ;
#49018=DIRECTION ( 'NONE',  ( 0.000000000000000000, 1.000000000000000000, 0.000000000000000000 ) ) ;
#49033=CARTESIAN_POINT ( 'NONE',  ( 10.36825461470400001, 2.760277452415999644, -7.815392442832299835 ) ) ;
#49046=CARTESIAN_POINT ( 'NONE',  ( 9.885596873516499627, 2.907767014557175678, -8.129523725463620565 ) ) ;
#49054=CARTESIAN_POINT ( 'NONE',  ( 11.76133460557259980, 4.139849081322200419, -8.354833838171700222 ) ) ;
#49056=CARTESIAN_POINT ( 'NONE',  ( 10.97635090131019986, 4.999207052587699707, -8.118017011233499503 ) ) ;
#49057=CARTESIAN_POINT ( 'NONE',  ( 9.710646554150999421, 4.486270025758400060, -8.378853663802400931 ) ) ;
#49073=CARTESIAN_POINT ( 'NONE',  ( 8.599999952505998024, 4.000000000000000000, -7.500000000000000000 ) ) ;
#49075=CARTESIAN_POINT ( 'NONE',  ( 11.17056785386839834, 3.281375110759499947, -7.983608166707499620 ) ) ;
#49106=CARTESIAN_POINT ( 'NONE',  ( 8.807788144226000426, 4.090932644426789722, -8.453461841935100196 ) ) ;
#49136=CARTESIAN_POINT ( 'NONE',  ( 8.724024145839393896, 3.782477278638352036, -8.345440805164775711 ) ) ;
#49142=CARTESIAN_POINT ( 'NONE',  ( 8.943784697134999462, 4.470490447737899942, -6.771750947090999340 ) ) ;
#49182=CARTESIAN_POINT ( 'NONE',  ( 10.60746886766490071, 3.501664543805500074, -6.594573315824700188 ) ) ;
#49217=CARTESIAN_POINT ( 'NONE',  ( 10.50333291544900050, 4.531093146757585899, -8.658936933361777832 ) ) ;
#49219=CARTESIAN_POINT ( 'NONE',  ( 11.60948876160955479, 3.304472173606900043, -8.223320049540498999 ) ) ;
#49301=CARTESIAN_POINT ( 'NONE',  ( 10.47718582084299932, 3.343463760027599818, -6.741111985563299491 ) ) ;
#49310=CARTESIAN_POINT ( 'NONE',  ( 10.47303166480599934, 2.862083839376000416, -7.580230465881790280 ) ) ;
#49333=PLANE ( 'NONE',  #26594 ) ;
#49364=B_SPLINE_CURVE_WITH_KNOTS ( 'NONE', 3,
 ( #30681, #29319, #24404, #24058 ),
 .UNSPECIFIED., .F., .F.,
 ( 4, 4 ),
 ( 0.000000000000000000, 0.8163836489557121379 ),
 .UNSPECIFIED. ) ;
#49365=CARTESIAN_POINT ( 'NONE',  ( 8.916525748329496182, 3.463676007238745136, -6.567753456898077324 ) ) ;
#49395=CARTESIAN_POINT ( 'NONE',  ( 10.56591429142999949, 4.019686495353769651, -6.466681092390999197 ) ) ;
#49396=CARTESIAN_POINT ( 'NONE',  ( 9.128076168957999670, 3.490299597736799875, -8.365475476407400635 ) ) ;
#49404=CARTESIAN_POINT ( 'NONE',  ( 9.556179045228626379, 3.383234358265068575, -6.879409626165266189 ) ) ;
#49415=DIRECTION ( 'NONE',  ( -1.000000000000000000, 0.000000000000000000, 0.000000000000000000 ) ) ;
#49417=CARTESIAN_POINT ( 'NONE',  ( 10.38287885159599888, 4.860099138268600072, -7.397393329751199786 ) ) ;
#49427=DIRECTION ( 'NONE',  ( -1.000000000000000000, 0.000000000000000000, 1.665334536957000056E-14 ) ) ;
#49487=CARTESIAN_POINT ( 'NONE',  ( 8.867797255587998251, 4.866234952405400271, -7.463326341748410364 ) ) ;
#49502=ORIENTED_EDGE ( 'NONE', *, *, #60714, .T. ) ;
#49515=FACE_OUTER_BOUND ( 'NONE', #34557, .T. ) ;
#49524=CARTESIAN_POINT ( 'NONE',  ( 10.86190547754509872, 4.891676932241900033, -7.528299448264639260 ) ) ;
#49535=CARTESIAN_POINT ( 'NONE',  ( 8.849999778957998942, 4.000000000000000000, -7.500000000000000000 ) ) ;
#49567=CARTESIAN_POINT ( 'NONE',  ( 11.31410538575739899, 4.975963290822400076, -7.266662245194900116 ) ) ;
#49569=CARTESIAN_POINT ( 'NONE',  ( 9.378405316141000370, 3.757578743663700038, -8.615780615741000403 ) ) ;
#49594=CIRCLE ( 'NONE', #11603, 0.7499999936418002555 ) ;
#49603=EDGE_LOOP ( 'NONE', ( #7416, #50894, #8662, #571, #6582, #5424, #8624, #19108, #44070, #66122 ) ) ;
#49653=CARTESIAN_POINT ( 'NONE',  ( 11.18272066707849888, 5.093522884867000222, -6.838543969064300398 ) ) ;
#49661=CARTESIAN_POINT ( 'NONE',  ( 11.35502763632549872, 2.839566963815999934, -6.964545474268299508 ) ) ;
#49692=CARTESIAN_POINT ( 'NONE',  ( 11.07907162307749793, 3.185388239149200107, -7.174999999999999822 ) ) ;
#49723=CARTESIAN_POINT ( 'NONE',  ( 10.54555864497999984, 5.007105485494000696, -8.288745882156399958 ) ) ;
#49746=CARTESIAN_POINT ( 'NONE',  ( 10.81524174883999834, 3.971581146373189597, -8.533115712456000423 ) ) ;
#49747=CARTESIAN_POINT ( 'NONE',  ( 9.204063610504999104, 4.411988005505000032, -8.416028484082099581 ) ) ;
#49771=CARTESIAN_POINT ( 'NONE',  ( 11.26487482311540056, 4.930401445321599851, -7.875904247640098887 ) ) ;
#49814=CARTESIAN_POINT ( 'NONE',  ( 9.099999931440999390, 4.000000000000000000, -7.500000000000000000 ) ) ;
#49834=CARTESIAN_POINT ( 'NONE',  ( 10.96118313518939935, 3.207251432249800249, -8.502430091786999711 ) ) ;
#49863=CARTESIAN_POINT ( 'NONE',  ( 10.84657802013509986, 2.684088780794000151, -7.469366283838649423 ) ) ;
#49914=CARTESIAN_POINT ( 'NONE',  ( 10.28441772631199846, 4.372518460886800185, -8.266796319406900295 ) ) ;
#49918=CARTESIAN_POINT ( 'NONE',  ( 9.733013376692998264, 2.982096917914000223, -6.982691809975100306 ) ) ;
#49957=FACE_OUTER_BOUND ( 'NONE', #28438, .T. ) ;
#49975=CARTESIAN_POINT ( 'NONE',  ( 9.120327454391752298, 5.191173620088457064, -7.088789390544037339 ) ) ;
#49978=B_SPLINE_CURVE_WITH_KNOTS ( 'NONE', 3,
 ( #47528, #68832, #42620, #5209 ),
 .UNSPECIFIED., .F., .F.,
 ( 4, 4 ),
 ( 0.000000000000000000, 1.000000000000000000 ),
 .UNSPECIFIED. ) ;
#50003=CARTESIAN_POINT ( 'NONE',  ( 10.37457053952199892, 3.551693493661699730, -6.451042711717000167 ) ) ;
#50011=CARTESIAN_POINT ( 'NONE',  ( 10.66579975933730040, 5.208485784810999775, -7.084213409908699965 ) ) ;
#50053=B_SPLINE_CURVE_WITH_KNOTS ( 'NONE', 3,
 ( #8950, #40764, #15227, #30291 ),
 .UNSPECIFIED., .F., .F.,
 ( 4, 4 ),
 ( 0.000000000000000000, 1.000000000000000000 ),
 .UNSPECIFIED. ) ;
#50078=VERTEX_POINT ( 'NONE', #35965 ) ;
#50095=CARTESIAN_POINT ( 'NONE',  ( 10.43210941423799909, 4.641185166475500168, -6.917608226833099394 ) ) ;
#50097=CARTESIAN_POINT ( 'NONE',  ( 10.76857802013509868, 2.825431102905000103, -7.472656658230009796 ) ) ;
#50098=CARTESIAN_POINT ( 'NONE',  ( 9.278038493598998571, 4.826346105011899645, -6.712036445818600150 ) ) ;
#50109=CARTESIAN_POINT ( 'NONE',  ( 10.24006601915162484, 3.957587222814286321, -8.373918476712228554 ) ) ;
#50120=CARTESIAN_POINT ( 'NONE',  ( 10.67826222744820086, 3.331419131587999960, -8.050725169876500331 ) ) ;
#50154=VERTEX_POINT ( 'NONE', #26170 ) ;
#50232=FACE_OUTER_BOUND ( 'NONE', #19362, .T. ) ;
#50261=CARTESIAN_POINT ( 'NONE',  ( 11.58487348028854846, 3.117292544139400157, -7.977261354519500358 ) ) ;
#50263=CARTESIAN_POINT ( 'NONE',  ( 9.226430433046999724, 3.028322657068899915, -6.900352112302299723 ) ) ;
#50349=CARTESIAN_POINT ( 'NONE',  ( 10.84226088462129844, 4.002427228022017225, -6.359261544073000039 ) ) ;
#50356=CARTESIAN_POINT ( 'NONE',  ( 11.01041369783139956, 3.935522326596939902, -8.776385133971000840 ) ) ;
#50375=VECTOR ( 'NONE', #136, 1000.000000000000227 ) ;
#50432=CARTESIAN_POINT ( 'NONE',  ( 11.07210672858429845, 3.307795442047700263, -6.979277962544199632 ) ) ;
#50437=CARTESIAN_POINT ( 'NONE',  ( 8.822113844317998499, 4.288351516201100111, -6.395197822644999697 ) ) ;
#50446=CARTESIAN_POINT ( 'NONE',  ( 9.860128811416625894, 4.869607263996035940, -7.596516710088708990 ) ) ;
#50459=CARTESIAN_POINT ( 'NONE',  ( 10.43210941423799909, 4.641185166475500168, -6.917608226833099394 ) ) ;
#50524=CARTESIAN_POINT ( 'NONE',  ( 9.057169810767971896, 4.203513387681364399, -8.707169876682314680 ) ) ;
#50549=SURFACE_STYLE_FILL_AREA ( #40739 ) ;
#50607=CARTESIAN_POINT ( 'NONE',  ( 10.55518582084299872, 3.433275964779900047, -6.844925608615599621 ) ) ;
#50610=CARTESIAN_POINT ( 'NONE',  ( 9.224417874593999755, 3.075647715286899953, -7.892956936667999912 ) ) ;
#50632=CARTESIAN_POINT ( 'NONE',  ( 11.59999999999999964, 4.000000000000000000, -7.500000000000000000 ) ) ;
#50695=CARTESIAN_POINT ( 'NONE',  ( 10.25149413291699929, 5.037815157227999663, -7.026470926762800495 ) ) ;
#50702=CARTESIAN_POINT ( 'NONE',  ( 10.88733729122639993, 2.722429312291999803, -7.466391690027689876 ) ) ;
#50705=CARTESIAN_POINT ( 'NONE',  ( 11.39975833414730033, 4.796537143354000499, -7.174999999999999822 ) ) ;
#50765=CARTESIAN_POINT ( 'NONE',  ( 9.329759580229000093, 2.755835090116000696, -7.202614619576299226 ) ) ;
#50786=CARTESIAN_POINT ( 'NONE',  ( 10.35826357027499789, 4.850513154668600002, -7.664090691848299386 ) ) ;
#50789=CARTESIAN_POINT ( 'NONE',  ( 9.531329965421999617, 3.206942993865000258, -8.321459087847200564 ) ) ;
#50800=CARTESIAN_POINT ( 'NONE',  ( 10.01210369451062654, 3.801861024511436593, -6.647783351891156656 ) ) ;
#50834=EDGE_CURVE ( 'NONE', #60944, #32326, #47792, .T. ) ;
#50845=B_SPLINE_CURVE_WITH_KNOTS ( 'NONE', 3,
 ( #40972, #62961, #67874, #14749 ),
 .UNSPECIFIED., .F., .F.,
 ( 4, 4 ),
 ( 0.000000000000000000, 1.000000000000000000 ),
 .UNSPECIFIED. ) ;
#50894=ORIENTED_EDGE ( 'NONE', *, *, #21851, .F. ) ;
#50900=CARTESIAN_POINT ( 'NONE',  ( 11.75203632436369894, 2.890282938442000127, -7.240848640331599917 ) ) ;
#50918=CARTESIAN_POINT ( 'NONE',  ( 10.63351354018304740, 5.250000000000001776, -7.663624617374467540 ) ) ;
#50950=CARTESIAN_POINT ( 'NONE',  ( 10.74795391537419853, 4.830118059977199785, -8.063786182297898009 ) ) ;
#50952=CARTESIAN_POINT ( 'NONE',  ( 9.958963142879998287, 4.982812171771600518, -7.292822454528599785 ) ) ;
#51011=CARTESIAN_POINT ( 'NONE',  ( 11.50705667793316778, 4.601576474242010661, -8.661791977777625107 ) ) ;
#51022=ADVANCED_FACE ( 'NONE', ( #3384 ), #8977, .T. ) ;
#51035=CARTESIAN_POINT ( 'NONE',  ( 11.33041235500449950, 3.057642534728299832, -6.636704692336500067 ) ) ;
#51043=CARTESIAN_POINT ( 'NONE',  ( 10.96118313518939935, 3.207251432249800249, -8.502430091786999711 ) ) ;
#51056=DIRECTION ( 'NONE',  ( 0.000000000000000000, 1.000000000000000000, 0.000000000000000000 ) ) ;
#51066=CARTESIAN_POINT ( 'NONE',  ( 11.54684497800060150, 3.023157657667436826, -7.824998645711865208 ) ) ;
#51106=CARTESIAN_POINT ( 'NONE',  ( 9.253772138682000659, 3.523984281974800403, -6.312652778810999621 ) ) ;
#51126=CARTESIAN_POINT ( 'NONE',  ( 10.53057053952199951, 3.659587858614300249, -6.703496287302799672 ) ) ;
#51129=CARTESIAN_POINT ( 'NONE',  ( 9.202051052051999136, 5.120555153167999585, -7.719295683256799379 ) ) ;
#51196=ORIENTED_EDGE ( 'NONE', *, *, #53955, .T. ) ;
#51244=CARTESIAN_POINT ( 'NONE',  ( 10.85679632507500081, 4.490665650747399873, -8.409605917786398877 ) ) ;
#51281=CARTESIAN_POINT ( 'NONE',  ( 10.31021345716899873, 4.636538040886300394, -8.078719053813800954 ) ) ;
#51290=CARTESIAN_POINT ( 'NONE',  ( 10.89564560330029863, 4.307504762655200103, -6.544808043482999160 ) ) ;
#51293=CARTESIAN_POINT ( 'NONE',  ( 9.148430433047000321, 3.145249924879699677, -6.972511033848699746 ) ) ;
#51301=ADVANCED_FACE ( 'NONE', ( #64423 ), #47319, .F. ) ;
#51334=CARTESIAN_POINT ( 'NONE',  ( 11.42834208742529967, 3.293478249981899975, -8.610579932818998472 ) ) ;
#51351=CARTESIAN_POINT ( 'NONE',  ( 9.303275160948496492, 2.900329483618105719, -6.884602962369688051 ) ) ;
#51374=CARTESIAN_POINT ( 'NONE',  ( 10.59195391537400077, 5.057233422790000432, -8.218034727798299244 ) ) ;
#51427=CARTESIAN_POINT ( 'NONE',  ( 9.802263540183334456, 2.907767014557178786, -6.870476274536374994 ) ) ;
#51444=CARTESIAN_POINT ( 'NONE',  ( 9.481734463323000739, 4.133249246727800141, -8.772253522581999974 ) ) ;
#51453=CYLINDRICAL_SURFACE ( 'NONE', #63320, 1.250000000000000222 ) ;
#51463=CARTESIAN_POINT ( 'NONE',  ( 10.69872335273220010, 4.349306362047499874, -8.440710326446700051 ) ) ;
#51466=CARTESIAN_POINT ( 'NONE',  ( 9.657975701332999208, 4.837683410033799980, -8.275900091855099561 ) ) ;
#51467=DIRECTION ( 'NONE',  ( -1.000000000000000000, 0.000000000000000000, -1.233561263588000078E-14 ) ) ;
#51531=FACE_OUTER_BOUND ( 'NONE', #8337, .T. ) ;
#51569=CARTESIAN_POINT ( 'NONE',  ( 11.59999999999999964, 4.000000000000000000, -7.500000000000000000 ) ) ;
#51577=CARTESIAN_POINT ( 'NONE',  ( 11.05946005378019947, 5.036385109519999403, -6.946587256304699309 ) ) ;
#51580=EDGE_LOOP ( 'NONE', ( #54013, #61301, #1474 ) ) ;
#51629=CARTESIAN_POINT ( 'NONE',  ( 10.94487616594229884, 3.696562859151900415, -6.543508100188799581 ) ) ;
#51632=CARTESIAN_POINT ( 'NONE',  ( 10.36422949779699820, 4.557226039164599563, -8.335668797826500054 ) ) ;
#51669=CARTESIAN_POINT ( 'NONE',  ( 10.47769598648999967, 5.009476315410999803, -8.101059042556599366 ) ) ;
#51675=CARTESIAN_POINT ( 'NONE',  ( 9.448096873516666605, 3.672815144550898303, -8.717465845835395299 ) ) ;
#51725=CARTESIAN_POINT ( 'NONE',  ( 10.32309687351566652, 2.782534154164606921, -7.172815144550894750 ) ) ;
#51784=CIRCLE ( 'NONE', #32819, 1.250000000000000888 ) ;
#51802=CARTESIAN_POINT ( 'NONE',  ( 11.68333460557258796, 4.162011815820000571, -8.490304555719900392 ) ) ;
#51804=CARTESIAN_POINT ( 'NONE',  ( 10.82035090130999855, 4.758726914843000699, -7.969278253227299658 ) ) ;
#51805=CARTESIAN_POINT ( 'NONE',  ( 9.250696787962999323, 4.219671260427300119, -6.239790126677999815 ) ) ;
#51814=CARTESIAN_POINT ( 'NONE',  ( 9.252229279041625176, 4.091138914130668880, -8.370187317335780364 ) ) ;
#51827=DIRECTION ( 'NONE',  ( 0.000000000000000000, -1.000000000000000000, 0.000000000000000000 ) ) ;
#51853=CARTESIAN_POINT ( 'NONE',  ( 9.925810748568999031, 2.827416853083249304, -8.000243450341617546 ) ) ;
#51890=CARTESIAN_POINT ( 'NONE',  ( 9.727263540182331525, 4.629523725463627670, -6.407767014557179230 ) ) ;
#51918=CARTESIAN_POINT ( 'NONE',  ( 11.48011496860029901, 4.919769165942200040, -7.028661263734299780 ) ) ;
#51966=CARTESIAN_POINT ( 'NONE',  ( 11.40841235500449891, 3.158861363519000154, -6.729431436870699557 ) ) ;
#51968=CARTESIAN_POINT ( 'NONE',  ( 9.399709346416997846, 4.783195203880800328, -7.128095150442700145 ) ) ;
#52006=CARTESIAN_POINT ( 'NONE',  ( 11.30878751119029957, 2.958974835389999836, -8.044634158732998586 ) ) ;
#52013=CARTESIAN_POINT ( 'NONE',  ( 9.479346873516668381, 4.163624617374466652, -8.749999999999998224 ) ) ;
#52050=CARTESIAN_POINT ( 'NONE',  ( 10.73964560330029983, 4.391636236366600166, -6.283473206644000442 ) ) ;
#52052=VECTOR ( 'NONE', #12489, 1000.000000000000000 ) ;
#52073=CYLINDRICAL_SURFACE ( 'NONE', #33926, 1.250000000000000222 ) ;
#52082=CARTESIAN_POINT ( 'NONE',  ( 10.62452888361057113, 3.128042445605609512, -7.561478660064198110 ) ) ;
#52142=CARTESIAN_POINT ( 'NONE',  ( 10.32949413291699869, 4.912929163218899831, -7.083453279150199400 ) ) ;
#52146=CARTESIAN_POINT ( 'NONE',  ( 9.377342523874999003, 2.735516931877000513, -7.306436165809000016 ) ) ;
#52151=B_SPLINE_CURVE_WITH_KNOTS ( 'NONE', 3,
 ( #68971, #52897, #22103, #42749, #42411, #43788, #64743, #65085, #58482, #17207, #16857, #10586, #31924, #43092, #4995, #53237, #5337, #26682 ),
 .UNSPECIFIED., .F., .F.,
 ( 4, 2, 2, 2, 2, 2, 2, 2, 4 ),
 ( 0.000000000000000000, 0.1250000000000000000, 0.2500000000000000000, 0.3750000000000000000, 0.5000000000000000000, 0.6250000000000000000, 0.7500000000000000000, 0.8750000000000000000, 1.000000000000000000 ),
 .UNSPECIFIED. ) ;
#52154=( GEOMETRIC_REPRESENTATION_CONTEXT ( 3 ) GLOBAL_UNCERTAINTY_ASSIGNED_CONTEXT ( ( #66520 ) ) GLOBAL_UNIT_ASSIGNED_CONTEXT ( ( #11964, #43447, #53238 ) ) REPRESENTATION_CONTEXT ( 'NONE', 'WORKASPACE' ) );
#52157=CARTESIAN_POINT ( 'NONE',  ( 9.328216720588626387, 4.762939826712631941, -7.928316576537355331 ) ) ;
#52229=CARTESIAN_POINT ( 'NONE',  ( 10.80502344389999791, 2.874741265256000489, -6.817099149379099110 ) ) ;
#52230=CARTESIAN_POINT ( 'NONE',  ( 9.991279731608999626, 4.077800926195140008, -6.636486849903699969 ) ) ;
#52235=CARTESIAN_POINT ( 'NONE',  ( 9.664763540182335078, 5.217465845835396188, -7.172815144550905408 ) ) ;
#52267=CARTESIAN_POINT ( 'NONE',  ( 10.85168717260509830, 3.386210853237200169, -8.501809683958001074 ) ) ;
#52321=CARTESIAN_POINT ( 'NONE',  ( 11.16225954179439839, 4.877394611789299894, -8.229019074832200076 ) ) ;
#52323=CARTESIAN_POINT ( 'NONE',  ( 9.855633995697999694, 4.861719613449499988, -7.595641268826199166 ) ) ;
#52360=CARTESIAN_POINT ( 'NONE',  ( 10.89324174884020024, 3.967693531726030010, -8.674442868902998427 ) ) ;
#52366=CARTESIAN_POINT ( 'NONE',  ( 9.343930206849998754, 2.750000000000000000, -7.500000000000000000 ) ) ;
#52376=CARTESIAN_POINT ( 'NONE',  ( 11.43114108301961629, 4.620688244309836712, -6.880598518631706462 ) ) ;
#52413=CARTESIAN_POINT ( 'NONE',  ( 10.13559687351566829, 5.092232985442826099, -6.870476274536379435 ) ) ;
#52427=VERTEX_POINT ( 'NONE', #6389 ) ;
#52491=CARTESIAN_POINT ( 'NONE',  ( 10.96949144726329806, 3.419793223320000131, -6.681274802424499448 ) ) ;
#52496=CARTESIAN_POINT ( 'NONE',  ( 9.655963142879999239, 5.251703735191999733, -7.236139910592400248 ) ) ;
#52575=CARTESIAN_POINT ( 'NONE',  ( 9.155417874594000693, 3.202096358337300330, -7.839201596587598964 ) ) ;
#52617=ORIENTED_EDGE ( 'NONE', *, *, #60611, .T. ) ;
#52661=CARTESIAN_POINT ( 'NONE',  ( 11.18272066707849888, 5.093522884867000222, -6.838543969064300398 ) ) ;
#52664=CARTESIAN_POINT ( 'NONE',  ( 9.754317406968999293, 4.161254277581000416, -8.351883209406098629 ) ) ;
#52678=AXIS2_PLACEMENT_3D ( 'NONE', #33816, #56506, #61412 ) ;
#52703=CARTESIAN_POINT ( 'NONE',  ( 10.55569598648999907, 5.130952141044000214, -8.173387776112500447 ) ) ;
#52755=CARTESIAN_POINT ( 'NONE',  ( 10.09964828895399869, 5.121614868497999851, -8.112615456209400833 ) ) ;
#52778=CARTESIAN_POINT ( 'NONE',  ( 10.67375944625267614, 3.325302618462734561, -8.055763479958521600 ) ) ;
#52841=CARTESIAN_POINT ( 'NONE',  ( 10.89564560330029863, 4.307504762655200103, -6.544808043482999160 ) ) ;
#52844=CARTESIAN_POINT ( 'NONE',  ( 10.10344474310099905, 5.137935629024000583, -8.052229793103100164 ) ) ;
#52897=CARTESIAN_POINT ( 'NONE',  ( 10.88351354018293904, 2.750000000000000000, -7.336375382625530683 ) ) ;
#52924=CARTESIAN_POINT ( 'NONE',  ( 11.51656039236534923, 5.173498198882000132, -7.557111631074219460 ) ) ;
#52925=CARTESIAN_POINT ( 'NONE',  ( 9.130088727410999638, 3.136022381937999981, -7.572461161969050281 ) ) ;
#52930=CARTESIAN_POINT ( 'NONE',  ( 9.821013540182335078, 3.231816600031359510, -6.500416447002272946 ) ) ;
#52960=CARTESIAN_POINT ( 'NONE',  ( 10.52435971519499880, 4.532462039660099862, -6.614211617270199461 ) ) ;
#52986=CARTESIAN_POINT ( 'NONE',  ( 11.54292372906209074, 5.032542535543790052, -8.269164421058194492 ) ) ;
#53013=CARTESIAN_POINT ( 'NONE',  ( 10.34995525820099971, 3.892289273474800471, -6.364355462479999836 ) ) ;
#53016=CARTESIAN_POINT ( 'NONE',  ( 8.869809814040998219, 4.614409247670200109, -8.294571108394100278 ) ) ;
#53053=CARTESIAN_POINT ( 'NONE',  ( 10.72702344389999851, 2.995605560827999891, -6.890449684422599752 ) ) ;
#53072=DIRECTION ( 'NONE',  ( 0.000000000000000000, 1.000000000000000000, 0.000000000000000000 ) ) ;
#53084=CARTESIAN_POINT ( 'NONE',  ( 8.811649685568998080, 4.101356036306899711, -8.457700632733599733 ) ) ;
#53092=CARTESIAN_POINT ( 'NONE',  ( 11.73671932425159881, 3.872987101045399783, -8.356835045446798560 ) ) ;
#53182=CARTESIAN_POINT ( 'NONE',  ( 9.530380199233999150, 5.132898093246000215, -7.357604921762999517 ) ) ;
#53185=CARTESIAN_POINT ( 'NONE',  ( 11.65456516821461008, 4.802916961510000249, -8.310318115935698913 ) ) ;
#53188=CARTESIAN_POINT ( 'NONE',  ( 9.579975701332999805, 4.938486452461599896, -8.369268408503399925 ) ) ;
#53194=FACE_OUTER_BOUND ( 'NONE', #14886, .T. ) ;
#53237=CARTESIAN_POINT ( 'NONE',  ( 10.66476354018302608, 5.217465845835396188, -7.172815144550905408 ) ) ;
#53238=( NAMED_UNIT ( * ) SI_UNIT ( $, .STERADIAN. ) SOLID_ANGLE_UNIT ( ) );
#53267=CARTESIAN_POINT ( 'NONE',  ( 11.01279632507519857, 4.624908853805600906, -8.658468685623999406 ) ) ;
#53268=CARTESIAN_POINT ( 'NONE',  ( 10.21924205624999971, 3.689072563647699976, -8.309340504471899536 ) ) ;
#53291=CARTESIAN_POINT ( 'NONE',  ( 11.76133460557259980, 4.139849081322200419, -8.354833838171700222 ) ) ;
#53320=ORIENTED_EDGE ( 'NONE', *, *, #37970, .F. ) ;
#53338=CARTESIAN_POINT ( 'NONE',  ( 8.712681907068999365, 3.774194491866800227, -8.364514367444298770 ) ) ;
#53357=CARTESIAN_POINT ( 'NONE',  ( 10.71918447801630059, 5.140463864104999558, -7.474854604063350116 ) ) ;
#53360=CARTESIAN_POINT ( 'NONE',  ( 9.678329965421998082, 3.397808798486600335, -8.123757726465999696 ) ) ;
#53383=ORIENTED_EDGE ( 'NONE', *, *, #7911, .T. ) ;
#53418=CARTESIAN_POINT ( 'NONE',  ( 11.55670819615736455, 3.379350336066780702, -6.880644002891321165 ) ) ;
#53431=CARTESIAN_POINT ( 'NONE',  ( 8.755786719645998417, 3.934709392726489785, -8.402920843186199917 ) ) ;
#53440=CARTESIAN_POINT ( 'NONE',  ( 11.24441369783139777, 3.956299011112040187, -8.365094684940499903 ) ) ;
#53470=CARTESIAN_POINT ( 'NONE',  ( 11.04298866606778162, 3.494581883632823516, -6.786808489985508785 ) ) ;
#53476=CARTESIAN_POINT ( 'NONE',  ( 9.477263540182331525, 3.370476274536374106, -8.592232985442821658 ) ) ;
#53495=ADVANCED_FACE ( 'NONE', ( #53194 ), #46920, .F. ) ;
#53524=CARTESIAN_POINT ( 'NONE',  ( 11.45764291764649911, 2.867875922590999771, -7.360052904210999891 ) ) ;
#53529=CARTESIAN_POINT ( 'NONE',  ( 9.353076168957999315, 3.420574098817999786, -8.483869947211399420 ) ) ;
#53531=CARTESIAN_POINT ( 'NONE',  ( 11.18687482311539938, 5.057677595549000316, -7.927326830586499007 ) ) ;
#53582=ORIENTED_EDGE ( 'NONE', *, *, #5292, .F. ) ;
#53585=FILL_AREA_STYLE_COLOUR ( '', #22008 ) ;
#53590=CARTESIAN_POINT ( 'NONE',  ( 10.25851354018279160, 4.163624617374472869, -6.250000000000000888 ) ) ;
#53610=CARTESIAN_POINT ( 'NONE',  ( 9.256734463322999318, 4.090312251411050148, -8.362294405496898619 ) ) ;
#53634=CARTESIAN_POINT ( 'NONE',  ( 11.63825819896753977, 3.148796120250299868, -7.660469764776300039 ) ) ;
#53644=CARTESIAN_POINT ( 'NONE',  ( 10.57102344389999971, 3.237334151971200225, -7.037150754511299233 ) ) ;
#53666=CARTESIAN_POINT ( 'NONE',  ( 11.28830977893787768, 3.023401864784706738, -6.673569913327193959 ) ) ;
#53681=VERTEX_POINT ( 'NONE', #30420 ) ;
#53699=CARTESIAN_POINT ( 'NONE',  ( 10.79303032197930001, 4.663532080728800544, -6.572090902022299730 ) ) ;
#53739=CARTESIAN_POINT ( 'NONE',  ( 10.69057802013490033, 2.966773425016000054, -7.475947032624040034 ) ) ;
#53752=CARTESIAN_POINT ( 'NONE',  ( 10.64601354018249957, 4.999583552997728830, -6.731816600031361730 ) ) ;
#53778=CARTESIAN_POINT ( 'NONE',  ( 11.21979841651039855, 3.695024856201900132, -8.310733465454200442 ) ) ;
#53859=CARTESIAN_POINT ( 'NONE',  ( 11.23610538575739959, 5.109472165990999848, -7.234742334405199315 ) ) ;
#53865=CARTESIAN_POINT ( 'NONE',  ( 11.08841369783139896, 3.942447888101379583, -8.639288317626999003 ) ) ;
#53868=CARTESIAN_POINT ( 'NONE',  ( 8.642797255587998606, 5.278067516796999925, -7.445890648716809501 ) ) ;
#53906=ORIENTED_EDGE ( 'NONE', *, *, #31493, .F. ) ;
#53946=CARTESIAN_POINT ( 'NONE',  ( 10.39969598649000027, 4.888000489779200208, -8.028730309000598808 ) ) ;
#53947=CARTESIAN_POINT ( 'NONE',  ( 9.077417874593999514, 3.075647715286899953, -7.892956936667999912 ) ) ;
#53955=EDGE_CURVE ( 'NONE', #42349, #57892, #61710, .T. ) ;
#53969=CARTESIAN_POINT ( 'NONE',  ( 11.31825954179440075, 4.666231193203100425, -8.053565341712399572 ) ) ;
#53985=ADVANCED_FACE ( 'NONE', ( #7202 ), #9895, .T. ) ;
#54009=CARTESIAN_POINT ( 'NONE',  ( 11.59999999999999787, 3.745359844992758092, -6.522131813714044490 ) ) ;
#54012=CARTESIAN_POINT ( 'NONE',  ( 8.741072744221000335, 3.937347817007940343, -8.366433385397499478 ) ) ;
#54013=ORIENTED_EDGE ( 'NONE', *, *, #25089, .T. ) ;
#54035=CARTESIAN_POINT ( 'NONE',  ( 10.71503032197929883, 4.743378537856500543, -6.460430507351999196 ) ) ;
#54037=CARTESIAN_POINT ( 'NONE',  ( 8.994442991499997930, 3.945420918055940085, -6.634708680083400090 ) ) ;
#54057=CARTESIAN_POINT ( 'NONE',  ( 9.321001730958840881, 3.231794228473278352, -6.500403846372135419 ) ) ;
#54062=ORIENTED_EDGE ( 'NONE', *, *, #67828, .F. ) ;
#54079=CARTESIAN_POINT ( 'NONE',  ( 11.19434208742519843, 3.521141233577200325, -8.252717006421999457 ) ) ;
#54113=CARTESIAN_POINT ( 'NONE',  ( 11.39975833414730033, 4.796537143354000499, -7.174999999999999822 ) ) ;
#54154=CARTESIAN_POINT ( 'NONE',  ( 9.539763540182331525, 4.327184855449099921, -8.717465845835397076 ) ) ;
#54177=CYLINDRICAL_SURFACE ( 'NONE', #66698, 1.250000000000000222 ) ;
#54198=CARTESIAN_POINT ( 'NONE',  ( 10.64949279009019989, 3.739015461786900030, -8.468936491037499792 ) ) ;
#54205=CARTESIAN_POINT ( 'NONE',  ( 11.48225819896749833, 2.879005208331999910, -7.711331004020999913 ) ) ;
#54270=CARTESIAN_POINT ( 'NONE',  ( 10.37309687351658383, 2.782534154164606921, -7.172815144550898303 ) ) ;
#54292=CARTESIAN_POINT ( 'NONE',  ( 11.43345123989529810, 4.540230239159599890, -8.543317325199000223 ) ) ;
#54293=CARTESIAN_POINT ( 'NONE',  ( 10.25944474310099785, 4.893483781708200198, -7.933599538786499039 ) ) ;
#54309=EDGE_CURVE ( 'NONE', #8973, #22792, #28332, .T. ) ;
#54341=ORIENTED_EDGE ( 'NONE', *, *, #38048, .F. ) ;
#54384=CARTESIAN_POINT ( 'NONE',  ( 10.17349413291699811, 5.162701151235999930, -6.969488574374499201 ) ) ;
#54404=ORIENTED_EDGE ( 'NONE', *, *, #14492, .F. ) ;
#54428=CARTESIAN_POINT ( 'NONE',  ( 10.29399293566599916, 4.546741702992100009, -8.170700474995699736 ) ) ;
#54459=CARTESIAN_POINT ( 'NONE',  ( 8.720712484379999907, 3.780467314030099946, -8.340498368324299250 ) ) ;
#54468=CARTESIAN_POINT ( 'NONE',  ( 11.65871932425156920, 3.852858594438699935, -8.492622906483498824 ) ) ;
#54555=CARTESIAN_POINT ( 'NONE',  ( 10.21462282008599942, 4.523146351753199568, -8.343818446627699004 ) ) ;
#54563=CARTESIAN_POINT ( 'NONE',  ( 11.01456785386839954, 3.053605396817899997, -8.136888821800198457 ) ) ;
#54647=CARTESIAN_POINT ( 'NONE',  ( 11.68788784977535933, 3.014014167207800465, -7.443657794094239222 ) ) ;
#54648=CARTESIAN_POINT ( 'NONE',  ( 8.672151519676999598, 4.021721698617580110, -8.504175633905001419 ) ) ;
#54656=CARTESIAN_POINT ( 'NONE',  ( 9.632166486775625813, 3.137137839323436594, -7.644917771834661480 ) ) ;
#54660=CARTESIAN_POINT ( 'NONE',  ( 9.099999931440999390, 5.064317881551000156, -8.155535999783198875 ) ) ;
#54668=CARTESIAN_POINT ( 'NONE',  ( 11.21564426047340035, 4.539962866738299851, -8.345807871442598724 ) ) ;
#54710=FACE_OUTER_BOUND ( 'NONE', #5700, .T. ) ;
#54735=CARTESIAN_POINT ( 'NONE',  ( 10.37041638348499895, 2.758294858530000226, -7.197535585171899619 ) ) ;
#54773=CARTESIAN_POINT ( 'NONE',  ( 10.28014141025500017, 4.417352327511700594, -8.243346240911998635 ) ) ;
#54787=CARTESIAN_POINT ( 'NONE',  ( 10.80226354018299872, 2.907767014557178786, -6.870476274536374994 ) ) ;
#54800=EDGE_CURVE ( 'NONE', #46101, #60944, #40698, .T. ) ;
#54813=CARTESIAN_POINT ( 'NONE',  ( 11.36333594839950045, 4.659759757475400832, -6.743912759487099784 ) ) ;
#54817=CARTESIAN_POINT ( 'NONE',  ( 9.884988259786998910, 3.850604015305000072, -8.631996151823999597 ) ) ;
#54899=CARTESIAN_POINT ( 'NONE',  ( 10.94487616594229884, 3.696562859151900415, -6.543508100188799581 ) ) ;
#54907=CARTESIAN_POINT ( 'NONE',  ( 11.05964426047339799, 4.687693494822500639, -8.577215873335999774 ) ) ;
#54910=DIRECTION ( 'NONE',  ( -1.000000000000000000, 0.000000000000000000, 0.000000000000000000 ) ) ;
#54970=CARTESIAN_POINT ( 'NONE',  ( 10.03897570133299944, 4.938486452461599896, -8.369268408503399925 ) ) ;
#54985=CARTESIAN_POINT ( 'NONE',  ( 9.927263540182998725, 3.370476274536375438, -8.592232985442821658 ) ) ;
#54994=CARTESIAN_POINT ( 'NONE',  ( 10.60746886766490071, 3.501664543805500074, -6.594573315824700188 ) ) ;
#54995=CARTESIAN_POINT ( 'NONE',  ( 9.533342523874999586, 3.007153757386999526, -7.348017636355000270 ) ) ;
#55003=CARTESIAN_POINT ( 'NONE',  ( 9.530849898046625412, 3.608426922415753690, -6.717566108970133953 ) ) ;
#55018=CARTESIAN_POINT ( 'NONE',  ( 11.56025819896753859, 3.013900664291200293, -7.685900384398899554 ) ) ;
#55039=CARTESIAN_POINT ( 'NONE',  ( 11.07273594314529142, 5.128905988536224037, -7.175020482857276782 ) ) ;
#55060=DIRECTION ( 'NONE',  ( 0.000000000000000000, 0.8514543052404082157, -0.5244287998266055073 ) ) ;
#55081=CARTESIAN_POINT ( 'NONE',  ( 10.34580110216399973, 2.909301855364999856, -6.833896451085399448 ) ) ;
#55085=DIRECTION ( 'NONE',  ( 0.000000000000000000, 1.000000000000000000, 0.000000000000000000 ) ) ;
#55097=CARTESIAN_POINT ( 'NONE',  ( 8.784678295047998020, 4.000000000000000000, -7.500000000000000000 ) ) ;
#55111=CARTESIAN_POINT ( 'NONE',  ( 10.88813259637009878, 2.844182332072999753, -8.129798612793599943 ) ) ;
#55160=CARTESIAN_POINT ( 'NONE',  ( 10.97364560330029981, 4.265439025801100570, -6.675475461903199736 ) ) ;
#55162=CARTESIAN_POINT ( 'NONE',  ( 8.975151519677000422, 4.027664626136379766, -8.778912113473998247 ) ) ;
#55205=CARTESIAN_POINT ( 'NONE',  ( 10.97124174884019965, 3.963805917081910213, -8.815770025351000072 ) ) ;
#55221=CARTESIAN_POINT ( 'NONE',  ( 9.099999931440999390, 5.246365646610000155, -7.404749409716440134 ) ) ;
#55248=CARTESIAN_POINT ( 'NONE',  ( 10.98579841651039857, 3.550031058388499972, -8.696179055230999211 ) ) ;
#55256=CARTESIAN_POINT ( 'NONE',  ( 11.23195122972050086, 4.507250159094099651, -6.326963915009999440 ) ) ;
#55271=CARTESIAN_POINT ( 'NONE',  ( 8.717397846562217723, 3.754687009553120181, -8.340771899786949106 ) ) ;
#55287=VECTOR ( 'NONE', #11386, 1000.000000000000000 ) ;
#55337=CARTESIAN_POINT ( 'NONE',  ( 11.44133594839949986, 4.569506585117100173, -6.847343244997600387 ) ) ;
#55339=CARTESIAN_POINT ( 'NONE',  ( 10.43614141025499897, 4.549633050978300730, -8.478951440767898973 ) ) ;
#55340=CARTESIAN_POINT ( 'NONE',  ( 8.976101285863999024, 3.353260484332500013, -6.731514281717299930 ) ) ;
#55363=CARTESIAN_POINT ( 'NONE',  ( 10.50595525820100029, 3.918212119278319694, -6.637672143048099827 ) ) ;
#55378=ORIENTED_EDGE ( 'NONE', *, *, #39223, .F. ) ;
#55423=SHAPE_REPRESENTATION ( 'Terminal Screw 3', ( #9676 ), #52154 ) ;
#55430=CARTESIAN_POINT ( 'NONE',  ( 10.51810807141099779, 4.059045408506610109, -8.776647962565998995 ) ) ;
#55447=ORIENTED_EDGE ( 'NONE', *, *, #46455, .T. ) ;
#55457=DIRECTION ( 'NONE',  ( 0.000000000000000000, -1.000000000000000000, 0.000000000000000000 ) ) ;
#55458=CARTESIAN_POINT ( 'NONE',  ( 11.38678751119029897, 2.833702563575000166, -8.110172976325500827 ) ) ;
#55472=CARTESIAN_POINT ( 'NONE',  ( 11.46021572556888657, 2.954248811040025124, -7.175002613693187925 ) ) ;
#55508=CARTESIAN_POINT ( 'NONE',  ( 10.75210807141120029, 4.040019166404060336, -8.365272822098500427 ) ) ;
#55512=CARTESIAN_POINT ( 'NONE',  ( 8.958265421554999719, 3.759926620436100375, -8.741861511046000288 ) ) ;
#55553=CARTESIAN_POINT ( 'NONE',  ( 10.63880513895979973, 5.150451045932999961, -6.860457220153399760 ) ) ;
#55597=CARTESIAN_POINT ( 'NONE',  ( 10.39918582084299992, 3.253651555277099927, -6.637298362509499228 ) ) ;
#55605=CARTESIAN_POINT ( 'NONE',  ( 11.40425819896749893, 2.744109752373000255, -7.736761623643599428 ) ) ;
#55650=CARTESIAN_POINT ( 'NONE',  ( 9.843930206850000530, 2.750000000000000000, -7.500000000000000000 ) ) ;
#55668=CARTESIAN_POINT ( 'NONE',  ( 10.52022949779799887, 4.709679768527199606, -8.564302809495998758 ) ) ;
#55689=CARTESIAN_POINT ( 'NONE',  ( 10.29262282008599882, 4.451581486939200083, -8.228386593078399258 ) ) ;
#55691=CARTESIAN_POINT ( 'NONE',  ( 11.44366954483529852, 4.485203148598100320, -6.751356298874699569 ) ) ;
#55692=CARTESIAN_POINT ( 'NONE',  ( 8.720797255587999786, 5.140789995332999851, -7.451702546394010085 ) ) ;
#55701=CARTESIAN_POINT ( 'NONE',  ( 9.936116252963625328, 4.581155023945095550, -6.845942581217610012 ) ) ;
#55714=CARTESIAN_POINT ( 'NONE',  ( 11.68333460557258796, 4.162011815820000571, -8.490304555719900392 ) ) ;
#55765=ORIENTED_EDGE ( 'NONE', *, *, #32710, .T. ) ;
#55775=CARTESIAN_POINT ( 'NONE',  ( 9.099999931440999390, 5.064317881551000156, -8.155535999783198875 ) ) ;
#55855=CARTESIAN_POINT ( 'NONE',  ( 10.40749413291699987, 4.788043169210699723, -7.140435631538599281 ) ) ;
#55857=CARTESIAN_POINT ( 'NONE',  ( 9.401721904869997815, 4.875830726371099821, -7.991693846894699860 ) ) ;
#55899=CARTESIAN_POINT ( 'NONE',  ( 11.13746005378019888, 5.161099018038999731, -6.879992063401499713 ) ) ;
#55939=CARTESIAN_POINT ( 'NONE',  ( 10.44841638348500013, 2.891666689023999925, -7.230023356477299323 ) ) ;
#55946=CARTESIAN_POINT ( 'NONE',  ( 10.17349413291699811, 5.162701151235999930, -6.969488574374499201 ) ) ;
#55976=AXIS2_PLACEMENT_3D ( 'NONE', #49814, #66229, #55060 ) ;
#56024=CARTESIAN_POINT ( 'NONE',  ( 11.41672066707849886, 4.741156262620799922, -7.051685395375099752 ) ) ;
#56026=CARTESIAN_POINT ( 'NONE',  ( 11.31900581613029821, 4.750686773407899466, -7.982035256002799173 ) ) ;
#56027=CARTESIAN_POINT ( 'NONE',  ( 10.01258376188599897, 3.037118682679400106, -8.113672563022399586 ) ) ;
#56099=ORIENTED_EDGE ( 'NONE', *, *, #39223, .T. ) ;
#56141=CARTESIAN_POINT ( 'NONE',  ( 11.51656039236534923, 5.173498198882000132, -7.557111631074219460 ) ) ;
#56167=CARTESIAN_POINT ( 'NONE',  ( 11.07299956498199833, 5.207010770456999893, -7.825000000000000178 ) ) ;
#56195=CARTESIAN_POINT ( 'NONE',  ( 11.23610538575739959, 5.109472165990999848, -7.234742334405199315 ) ) ;
#56197=CARTESIAN_POINT ( 'NONE',  ( 9.351063610504999346, 4.411988005505000032, -8.416028484082099581 ) ) ;
#56224=AXIS2_PLACEMENT_3D ( 'NONE', #49535, #13531, #44996 ) ;
#56255=CARTESIAN_POINT ( 'NONE',  ( 9.293111399473126255, 2.988705873519680090, -6.748153640515438312 ) ) ;
#56270=B_SPLINE_CURVE_WITH_KNOTS ( 'NONE', 3,
 ( #8054, #29396, #67796, #50705 ),
 .UNSPECIFIED., .F., .F.,
 ( 4, 4 ),
 ( 0.000000000000000000, 1.000000000000000000 ),
 .UNSPECIFIED. ) ;
#56282=CARTESIAN_POINT ( 'NONE',  ( 11.37964291764649971, 2.731641218595000087, -7.343212302062899433 ) ) ;
#56291=CARTESIAN_POINT ( 'NONE',  ( 11.57656516821460890, 4.899536366368299589, -8.407828142327998577 ) ) ;
#56352=CARTESIAN_POINT ( 'NONE',  ( 9.811013376692999444, 2.859607053196999704, -6.920441276178300072 ) ) ;
#56373=CARTESIAN_POINT ( 'NONE',  ( 10.70287750876920008, 3.530799696887600092, -8.228113772635300194 ) ) ;
#56377=CARTESIAN_POINT ( 'NONE',  ( 10.08857120343299840, 3.944651031655580287, -8.640469672413999547 ) ) ;
#56392=CARTESIAN_POINT ( 'NONE',  ( 10.99999970531878013, 2.901368254139102376, -7.597293174631950308 ) ) ;
#56405=CARTESIAN_POINT ( 'NONE',  ( 11.59999999999999964, 4.000000000000000000, -7.500000000000000000 ) ) ;
#56416=CARTESIAN_POINT ( 'NONE',  ( 8.789886373836322875, 4.000007821194417446, -8.439846342473931173 ) ) ;
#56454=FACE_OUTER_BOUND ( 'NONE', #47333, .T. ) ;
#56486=CARTESIAN_POINT ( 'NONE',  ( 11.39700581613019992, 4.869652672166700391, -8.058426314824099990 ) ) ;
#56506=DIRECTION ( 'NONE',  ( 1.000000000000000000, 0.000000000000000000, 0.000000000000000000 ) ) ;
#56536=CARTESIAN_POINT ( 'NONE',  ( 11.21149010443640037, 5.137564434800999891, -7.585072163144589652 ) ) ;
#56539=CARTESIAN_POINT ( 'NONE',  ( 9.553696787962998371, 4.172481380750499902, -6.510508982544899403 ) ) ;
#56579=EDGE_CURVE ( 'NONE', #12138, #26310, #37633, .T. ) ;
#56598=CARTESIAN_POINT ( 'NONE',  ( 9.272783876522375124, 3.210141752053232711, -6.518107589053542483 ) ) ;
#56624=CARTESIAN_POINT ( 'NONE',  ( 11.57656516821460890, 4.899536366368299589, -8.407828142327998577 ) ) ;
#56631=ORIENTED_EDGE ( 'NONE', *, *, #54800, .T. ) ;
#56665=EDGE_CURVE ( 'NONE', #3413, #35475, #45311, .T. ) ;
#56682=CARTESIAN_POINT ( 'NONE',  ( 9.593930206849998754, 5.250000000000000000, -7.500000000000000000 ) ) ;
#56699=CARTESIAN_POINT ( 'NONE',  ( 9.659038493598998798, 4.925784867300699865, -6.617216466537199970 ) ) ;
#56721=CARTESIAN_POINT ( 'NONE',  ( 11.61364291764652812, 3.140345330584100036, -7.393734108507599601 ) ) ;
#56724=CARTESIAN_POINT ( 'NONE',  ( 8.796784697134999220, 4.619613413415000203, -6.540930833646799947 ) ) ;
#56826=SURFACE_SIDE_STYLE ('',( #50549 ) ) ;
#56836=CARTESIAN_POINT ( 'NONE',  ( 10.68546886766499959, 3.433493735705800187, -6.470713638631999665 ) ) ;
#56882=CARTESIAN_POINT ( 'NONE',  ( 10.64949279009019989, 3.739015461786900030, -8.468936491037499792 ) ) ;
#56884=CARTESIAN_POINT ( 'NONE',  ( 9.097772138681998300, 3.626242194157900389, -6.567719246739500250 ) ) ;
#56921=CARTESIAN_POINT ( 'NONE',  ( 11.68277869730536977, 3.468607053297499743, -6.452143920160000157 ) ) ;
#56929=CARTESIAN_POINT ( 'NONE',  ( 9.521013540183334456, 4.768183399968643599, -8.499583552997725278 ) ) ;
#56962=CARTESIAN_POINT ( 'NONE',  ( 10.05862282008599884, 4.666276081381299790, -8.574682153725998290 ) ) ;
#56973=CARTESIAN_POINT ( 'NONE',  ( 9.893930206848997599, 2.750000000000000000, -7.500000000000000000 ) ) ;
#56974=CARTESIAN_POINT ( 'NONE',  ( 10.27101354018233437, 3.231816600031359066, -6.500416447002272058 ) ) ;
#57027=ORIENTED_EDGE ( 'NONE', *, *, #57767, .T. ) ;
#57052=CARTESIAN_POINT ( 'NONE',  ( 11.73256516821459883, 4.706297556651700020, -8.212808089543500500 ) ) ;
#57054=CARTESIAN_POINT ( 'NONE',  ( 11.27745123989519982, 4.410212499603100689, -8.292221125039500151 ) ) ;
#57055=CARTESIAN_POINT ( 'NONE',  ( 8.646822372493998543, 3.711294259598199918, -8.444453017408701356 ) ) ;
#57059=VERTEX_POINT ( 'NONE', #31629 ) ;
#57164=CARTESIAN_POINT ( 'NONE',  ( 11.67403632436368888, 3.023821283238099955, -7.272033745815799755 ) ) ;
#57213=CARTESIAN_POINT ( 'NONE',  ( 11.62994988689359843, 4.518136976474400157, -8.516279404258998653 ) ) ;
#57215=CARTESIAN_POINT ( 'NONE',  ( 10.11093802597399893, 3.477805217445600228, -6.642005297568199573 ) ) ;
#57251=CARTESIAN_POINT ( 'NONE',  ( 10.73213259636989925, 3.092475607087700418, -7.994504989494399361 ) ) ;
#57258=CARTESIAN_POINT ( 'NONE',  ( 9.364763540183330903, 2.782534154164605589, -7.827184855449096368 ) ) ;
#57268=CARTESIAN_POINT ( 'NONE',  ( 9.323602683899247623, 2.780955253993290022, -7.180752970636812726 ) ) ;
#57302=VERTEX_POINT ( 'NONE', #60953 ) ;
#57308=CARTESIAN_POINT ( 'NONE',  ( 10.22934687351566474, 3.836375382625535124, -6.249999999999999112 ) ) ;
#57386=CARTESIAN_POINT ( 'NONE',  ( 10.74795391537419853, 4.830118059977199785, -8.063786182297898009 ) ) ;
#57388=CARTESIAN_POINT ( 'NONE',  ( 9.124051052051999733, 5.255397705012999410, -7.745684736446600382 ) ) ;
#57399=CARTESIAN_POINT ( 'NONE',  ( 9.176241837494625742, 3.342362352854908458, -8.077100505959180055 ) ) ;
#57467=CARTESIAN_POINT ( 'NONE',  ( 9.915292290062998504, 4.749786674456300872, -7.064651992867799990 ) ) ;
#57473=CARTESIAN_POINT ( 'NONE',  ( 9.841846873515665450, 3.000416447002276943, -6.731816600031354625 ) ) ;
#57501=CARTESIAN_POINT ( 'NONE',  ( 10.81013259637009938, 2.968328969579000276, -8.062151801142800167 ) ) ;
#57557=CARTESIAN_POINT ( 'NONE',  ( 11.30995122972050027, 4.452766304612699955, -6.452959986593999275 ) ) ;
#57562=CARTESIAN_POINT ( 'NONE',  ( 9.349051052051999378, 4.850870049477099322, -7.666517576877299511 ) ) ;
#57572=ORIENTED_EDGE ( 'NONE', *, *, #32710, .F. ) ;
#57578=CARTESIAN_POINT ( 'NONE',  ( 8.599999952505998024, 4.749999993641800700, -7.500000000000000000 ) ) ;
#57597=CARTESIAN_POINT ( 'NONE',  ( 11.60477869730532774, 3.532552483170099844, -6.578238193496799724 ) ) ;
#57641=CARTESIAN_POINT ( 'NONE',  ( 10.54272335273199879, 4.444874504667400750, -8.698083075453000745 ) ) ;
#57652=CARTESIAN_POINT ( 'NONE',  ( 10.14601354018233259, 4.999583552997728830, -6.731816600031361730 ) ) ;
#57730=CARTESIAN_POINT ( 'NONE',  ( 11.63410404293056999, 3.557672215630899970, -8.400720262063998689 ) ) ;
#57733=CARTESIAN_POINT ( 'NONE',  ( 9.352013376692999813, 2.859607053196999704, -6.920441276178300072 ) ) ;
#57742=PRODUCT_DEFINITION ( 'UNKNOWN', '', #37394, #47874 ) ;
#57767=EDGE_CURVE ( 'NONE', #62603, #2862, #1181, .T. ) ;
#57776=ORIENTED_EDGE ( 'NONE', *, *, #28409, .F. ) ;
#57818=CARTESIAN_POINT ( 'NONE',  ( 10.16858376188599955, 3.268856270222099791, -7.965979387614599894 ) ) ;
#57892=VERTEX_POINT ( 'NONE', #62833 ) ;
#57912=CARTESIAN_POINT ( 'NONE',  ( 11.20733594839949809, 4.840266102192999575, -6.537051788466999191 ) ) ;
#57914=CARTESIAN_POINT ( 'NONE',  ( 9.273063610504998167, 4.355629271815800507, -8.290718512198798962 ) ) ;
#57935=CARTESIAN_POINT ( 'NONE',  ( 10.14393020684899938, 5.250000000000000000, -7.500000000000000000 ) ) ;
#57955=CARTESIAN_POINT ( 'NONE',  ( 11.35034208742529849, 3.369365911179700301, -8.491292290686200062 ) ) ;
#58010=CARTESIAN_POINT ( 'NONE',  ( 10.17726354018233437, 4.629523725463628558, -6.407767014557180119 ) ) ;
#58086=CARTESIAN_POINT ( 'NONE',  ( 10.82179975933729921, 4.948878321068100661, -7.173532873542499466 ) ) ;
#58090=CARTESIAN_POINT ( 'NONE',  ( 10.08655864497999843, 5.007105485494000696, -8.288745882156399958 ) ) ;
#58152=CARTESIAN_POINT ( 'NONE',  ( 11.59999999999999964, 4.000000000000000000, -7.500000000000000000 ) ) ;
#58168=CARTESIAN_POINT ( 'NONE',  ( 11.59966954483535773, 4.638989336656000440, -6.514072057539499916 ) ) ;
#58169=CARTESIAN_POINT ( 'NONE',  ( 9.459367640780998343, 4.408706755790200660, -6.735364967924099666 ) ) ;
#58174=CARTESIAN_POINT ( 'NONE',  ( 10.31021345716899873, 4.636538040886300394, -8.078719053813800954 ) ) ;
#58201=CARTESIAN_POINT ( 'NONE',  ( 10.64902344389989963, 3.116469856398800253, -6.963800219468099684 ) ) ;
#58224=CARTESIAN_POINT ( 'NONE',  ( 11.56493925477931306, 5.173530340702487962, -7.948835763880663485 ) ) ;
#58251=CARTESIAN_POINT ( 'NONE',  ( 10.74379975933729980, 5.078682052940000524, -7.128873141726999485 ) ) ;
#58255=CARTESIAN_POINT ( 'NONE',  ( 8.819151519676999840, 4.021721698617580110, -8.504175633905001419 ) ) ;
#58271=CARTESIAN_POINT ( 'NONE',  ( 9.185590450029501142, 5.092272840597503070, -6.870462550877411090 ) ) ;
#58277=DIRECTION ( 'NONE',  ( 0.000000000000000000, 0.000000000000000000, -1.000000000000000000 ) ) ;
#58290=CARTESIAN_POINT ( 'NONE',  ( 10.97635090131019986, 4.999207052587699707, -8.118017011233499503 ) ) ;
#58332=CARTESIAN_POINT ( 'NONE',  ( 11.51518179236248862, 3.819003318705799899, -6.652923384986699773 ) ) ;
#58362=CARTESIAN_POINT ( 'NONE',  ( 10.47683719568447636, 4.186288604638629174, -6.645958924689391090 ) ) ;
#58369=CARTESIAN_POINT ( 'NONE',  ( 9.393930206848999376, 2.750000000000000000, -7.500000000000000000 ) ) ;
#58420=CARTESIAN_POINT ( 'NONE',  ( 10.11295058442699890, 4.453199839589800035, -6.451980747609000311 ) ) ;
#58422=CARTESIAN_POINT ( 'NONE',  ( 10.99410672858429905, 3.198097575668700010, -6.896755974168000236 ) ) ;
#58425=CARTESIAN_POINT ( 'NONE',  ( 8.997405316140000053, 3.728406863338599830, -8.750048621292000561 ) ) ;
#58441=ORIENTED_EDGE ( 'NONE', *, *, #40286, .T. ) ;
#58442=B_SPLINE_CURVE_WITH_KNOTS ( 'NONE', 3,
 ( #29873, #19016, #24946, #30208 ),
 .UNSPECIFIED., .F., .F.,
 ( 4, 4 ),
 ( 0.000000000000000000, 0.1836163425310814723 ),
 .UNSPECIFIED. ) ;
#58454=CARTESIAN_POINT ( 'NONE',  ( 11.18114303127866727, 3.379301870158037069, -8.119425260350670470 ) ) ;
#58482=CARTESIAN_POINT ( 'NONE',  ( 10.77934687351631382, 3.836375382625536012, -6.249999999999999112 ) ) ;
#58505=CARTESIAN_POINT ( 'NONE',  ( 11.55300581613033906, 5.107584469683000172, -8.211208432468300344 ) ) ;
#58506=CARTESIAN_POINT ( 'NONE',  ( 9.788646554150998824, 4.419749732651400365, -8.258629096756299859 ) ) ;
#58537=CARTESIAN_POINT ( 'NONE',  ( 10.98937577273788868, 3.538822733277925181, -8.699885912910444219 ) ) ;
#58538=CARTESIAN_POINT ( 'NONE',  ( 11.60988784977536348, 3.148894096305599799, -7.451365240271489832 ) ) ;
#58558=CARTESIAN_POINT ( 'NONE',  ( 11.20158531382784162, 4.272452942476327564, -6.250000000000000000 ) ) ;
#58560=B_SPLINE_CURVE_WITH_KNOTS ( 'NONE', 3,
 ( #35821, #9236, #15862, #26016, #57473, #52930, #69002, #21115, #30575, #14840, #31270, #51890, #37194, #3985, #9580, #52235, #4674, #36503 ),
 .UNSPECIFIED., .F., .F.,
 ( 4, 2, 2, 2, 2, 2, 2, 2, 4 ),
 ( 0.000000000000000000, 0.1250000000000000000, 0.2500000000000000000, 0.3750000000000000000, 0.5000000000000000000, 0.6250000000000000000, 0.7500000000000000000, 0.8750000000000000000, 1.000000000000000000 ),
 .UNSPECIFIED. ) ;
#58575=ORIENTED_EDGE ( 'NONE', *, *, #1093, .F. ) ;
#58595=CARTESIAN_POINT ( 'NONE',  ( 11.08425954179440076, 4.982976321082899673, -8.316745941391600283 ) ) ;
#58597=CARTESIAN_POINT ( 'NONE',  ( 9.653000818238998804, 3.232852935619000334, -7.903971937289999694 ) ) ;
#58613=ORIENTED_EDGE ( 'NONE', *, *, #67342, .F. ) ;
#58635=CARTESIAN_POINT ( 'NONE',  ( 11.15278751119019773, 3.209519379020799867, -7.913556523549700294 ) ) ;
#58670=CARTESIAN_POINT ( 'NONE',  ( 8.762289945692000259, 3.761977284103799946, -8.411288920148800585 ) ) ;
#58708=CARTESIAN_POINT ( 'NONE',  ( 10.96914282210478042, 4.267867395145749754, -6.667932297870764913 ) ) ;
#58759=CARTESIAN_POINT ( 'NONE',  ( 11.62994988689359843, 4.518136976474400157, -8.516279404258998653 ) ) ;
#58764=CARTESIAN_POINT ( 'NONE',  ( 9.049126402770998112, 5.068373778467000434, -7.097120470443400109 ) ) ;
#58766=CARTESIAN_POINT ( 'NONE',  ( 11.38379707368349969, 3.433355370490100533, -6.509947486183500054 ) ) ;
#58769=CARTESIAN_POINT ( 'NONE',  ( 8.870759580228998686, 2.755835090116000696, -7.202614619576299226 ) ) ;
#58824=ORIENTED_EDGE ( 'NONE', *, *, #67102, .F. ) ;
#58829=CARTESIAN_POINT ( 'NONE',  ( 10.35226354018316108, 2.907767014557178342, -6.870476274536370553 ) ) ;
#58851=CARTESIAN_POINT ( 'NONE',  ( 11.51145123989532948, 4.605239108938600445, -8.668865425277999748 ) ) ;
#58852=CARTESIAN_POINT ( 'NONE',  ( 9.687329965421998423, 3.397808798486600335, -8.123757726465999696 ) ) ;
#58890=CARTESIAN_POINT ( 'NONE',  ( 10.35814141025499957, 4.483492689244800822, -8.361148840840000318 ) ) ;
#58943=CARTESIAN_POINT ( 'NONE',  ( 10.30072469555899950, 4.570852684939899824, -6.512367818249299667 ) ) ;
#58946=CARTESIAN_POINT ( 'NONE',  ( 9.450367640780999778, 4.408706755790200660, -6.735364967924099666 ) ) ;
#58954=ADVANCED_FACE ( 'NONE', ( #22940 ), #48309, .F. ) ;
#58964=CARTESIAN_POINT ( 'NONE',  ( 9.393930206848999376, 2.750000000000000000, -7.500000000000000000 ) ) ;
#58967=CARTESIAN_POINT ( 'NONE',  ( 8.599999986286999132, 3.249999986289399789, -7.499999999961952213 ) ) ;
#58994=CARTESIAN_POINT ( 'NONE',  ( 9.393930206848999376, 2.750000000000000000, -7.500000000000000000 ) ) ;
#59061=CARTESIAN_POINT ( 'NONE',  ( 9.529346873515667227, 4.163624617374466652, -8.749999999999998224 ) ) ;
#59063=EDGE_CURVE ( 'NONE', #509, #28630, #65853, .T. ) ;
#59104=CARTESIAN_POINT ( 'NONE',  ( 10.92026088462129962, 4.002135146349410810, -6.496532863517000322 ) ) ;
#59110=CARTESIAN_POINT ( 'NONE',  ( 10.59610807141099897, 4.052703327804870526, -8.639522915742999132 ) ) ;
#59114=CARTESIAN_POINT ( 'NONE',  ( 8.617468108405999416, 5.230803879475000251, -7.848577323721800170 ) ) ;
#59130=LINE ( 'NONE', #1790, #17022 ) ;
#59140=CARTESIAN_POINT ( 'NONE',  ( 11.22823073745748168, 3.830325957789608715, -8.360328963510957223 ) ) ;
#59173=FACE_OUTER_BOUND ( 'NONE', #8941, .T. ) ;
#59194=CARTESIAN_POINT ( 'NONE',  ( 10.73213259636989925, 3.092475607087700418, -7.994504989494399361 ) ) ;
#59195=CARTESIAN_POINT ( 'NONE',  ( 9.330709346416998784, 4.907312911337299965, -7.069157126958599768 ) ) ;
#59216=CARTESIAN_POINT ( 'NONE',  ( 10.72749279009019929, 3.774717370312400178, -8.336388861178200216 ) ) ;
#59251=CARTESIAN_POINT ( 'NONE',  ( 11.60000000000000142, 3.599560744838743886, -6.596661741119738132 ) ) ;
#59280=CARTESIAN_POINT ( 'NONE',  ( 11.52733460557258915, 4.206337284815599986, -8.761245990815998752 ) ) ;
#59324=CARTESIAN_POINT ( 'NONE',  ( 11.44366954483529852, 4.485203148598100320, -6.751356298874699569 ) ) ;
#59325=CARTESIAN_POINT ( 'NONE',  ( 11.53192018828833731, 3.091029700564639437, -7.175001928748123703 ) ) ;
#59363=CARTESIAN_POINT ( 'NONE',  ( 11.66287348028854964, 3.238044298475899918, -7.911973420841600380 ) ) ;
#59421=CARTESIAN_POINT ( 'NONE',  ( 9.211801307670125283, 4.111875952999886508, -6.244821713992729784 ) ) ;
#59447=CARTESIAN_POINT ( 'NONE',  ( 11.11302897915239818, 4.291996373817799970, -8.602736702002999891 ) ) ;
#59453=CARTESIAN_POINT ( 'NONE',  ( 11.28533594839949750, 4.750012929834699804, -6.640482273977399430 ) ) ;
#59482=CARTESIAN_POINT ( 'NONE',  ( 11.21253483539785556, 3.661009989788314822, -8.308639362931231176 ) ) ;
#59542=CARTESIAN_POINT ( 'NONE',  ( 11.47500581613029880, 4.988618570924500339, -8.134817373646898275 ) ) ;
#59543=CARTESIAN_POINT ( 'NONE',  ( 10.14124205625000030, 3.639798001706899822, -8.437601616732200327 ) ) ;
#59564=CARTESIAN_POINT ( 'NONE',  ( 11.34287482311539996, 4.803125295093300551, -7.824481664695199790 ) ) ;
#59586=DIRECTION ( 'NONE',  ( 0.000000000000000000, 1.000000000000000000, 0.000000000000000000 ) ) ;
#59605=B_SPLINE_CURVE_WITH_KNOTS ( 'NONE', 3,
 ( #67129, #12627, #29068, #61551 ),
 .UNSPECIFIED., .F., .F.,
 ( 4, 4 ),
 ( 0.000000000000000000, 1.000000000000000000 ),
 .UNSPECIFIED. ) ;
#59632=CARTESIAN_POINT ( 'NONE',  ( 10.27195525820100031, 3.879327850572200198, -6.227697122196000024 ) ) ;
#59636=B_SPLINE_SURFACE_WITH_KNOTS ( 'NONE', 3, 3, ( 
 ( #3428, #19170, #40494, #8684, #61482, #14282, #30032, #18496, #29339, #13601, #44729, #51334, #34922, #24764, #67397, #66372, #19518, #23389, #55899, #8345, #66026, #8003, #55205, #18150, #39821, #34583, #39471, #29691, #12906, #34234, #55553, #30696, #52703, #46778, #62497 ),
 ( #62838, #25445, #63177, #56921, #63534, #20546, #41870, #15645, #36979, #68082, #69126, #57955, #52006, #14956, #35609, #42563, #4798, #42227, #20198, #31050, #58290, #41192, #52360, #9353, #4452, #15306, #53053, #36631, #5151, #4109, #10053, #25793, #51669, #31389, #9021 ),
 ( #41525, #36281, #26141, #57597, #47467, #3765, #30361, #9704, #47123, #63871, #10395, #68424, #31733, #68772, #20891, #26486, #47818, #21232, #25103, #46435, #67737, #19860, #14620, #35939, #57251, #53739, #37657, #49182, #15985, #32424, #64900, #11089, #65255, #6874, #27517 ),
 ( #11770, #32085, #27872, #48152, #64213, #59324, #48845, #17014, #1293, #21914, #22605, #54079, #58635, #5499, #38698, #5837, #950, #255, #43950, #49524, #33113, #17370, #11424, #37997, #60020, #6175, #27175, #33460, #12130, #32765, #43603, #22263, #21570, #54428, #54773 ) ),
 .UNSPECIFIED., .F., .F., .F.,
 ( 4, 4 ),
 ( 4, 1, 1, 1, 1, 1, 1, 1, 1, 1, 1, 1, 1, 1, 1, 1, 1, 1, 1, 1, 1, 1, 1, 1, 1, 1, 1, 1, 1, 1, 1, 1, 4 ),
 ( -0.02000000000000000042, 1.020000000000000018 ),
 ( 0.1633025096610999927, 0.1899619885200000136, 0.2166214673788000034, 0.2432809462376999965, 0.2699404250964999585, 0.2965999039553000038, 0.3232593828141999692, 0.3499188616730000145, 0.3765783405318000043, 0.4032378193906999697, 0.4298972982494999595, 0.4565567771083000048, 0.4832162559671999702, 0.5098757348260000155, 0.5365352136848999809, 0.5631946925437000262, 0.5898541714025000715, 0.6165136502614000369, 0.6431731291201999712, 0.6698326079790000165, 0.6964920868378999819, 0.7231515656967000272, 0.7498110445554999615, 0.7764705234143999268, 0.8031300022731999722, 0.8297894811320000175, 0.8564489599908999828, 0.8831084388497000282, 0.9097679177085999935, 0.9364273965674000388, 0.9630868754261999731, 0.9897463542851000495, 1.016405833144000015 ),
 .UNSPECIFIED. ) ;
#59647=VERTEX_POINT ( 'NONE', #33724 ) ;
#59685=CARTESIAN_POINT ( 'NONE',  ( 10.77101354018289925, 3.231816600031359066, -6.500416447002272058 ) ) ;
#59686=CARTESIAN_POINT ( 'NONE',  ( 11.33810207955129812, 4.796537143354000499, -7.825000000000000178 ) ) ;
#59711=CARTESIAN_POINT ( 'NONE',  ( 11.78179573085659904, 4.973133828855400118, -7.668383662421899061 ) ) ;
#59756=ORIENTED_EDGE ( 'NONE', *, *, #23791, .F. ) ;
#59758=CARTESIAN_POINT ( 'NONE',  ( 10.56059687351646481, 4.629523725463624118, -8.592232985442823434 ) ) ;
#59793=CARTESIAN_POINT ( 'NONE',  ( 10.96949144726329806, 3.419793223320000131, -6.681274802424499448 ) ) ;
#59802=CARTESIAN_POINT ( 'NONE',  ( 10.81764560330029923, 4.349570499512200428, -6.414140625063999401 ) ) ;
#59858=SURFACE_STYLE_USAGE ( .BOTH. , #27020 ) ;
#59884=CARTESIAN_POINT ( 'NONE',  ( 10.89835090130999973, 4.878966983716200190, -8.043647632228999811 ) ) ;
#59885=CARTESIAN_POINT ( 'NONE',  ( 9.609329965421999020, 3.302375896175799852, -8.222608407156599242 ) ) ;
#59909=CARTESIAN_POINT ( 'NONE',  ( 11.46595122972049907, 4.343798595649099425, -6.704952129760900270 ) ) ;
#59938=VERTEX_POINT ( 'NONE', #63364 ) ;
#60006=VECTOR ( 'NONE', #55457, 1000.000000000000000 ) ;
#60007=CARTESIAN_POINT ( 'NONE',  ( 11.63611496860034933, 5.171412538012999605, -6.899705789500199415 ) ) ;
#60020=CARTESIAN_POINT ( 'NONE',  ( 10.65413259636999932, 3.216622244594500302, -7.926858177843299380 ) ) ;
#60036=CARTESIAN_POINT ( 'NONE',  ( 11.12299956498149811, 5.207010770456999893, -7.825000000000000178 ) ) ;
#60064=CARTESIAN_POINT ( 'NONE',  ( 11.46179707368349909, 3.501542828836900156, -6.629085939160999530 ) ) ;
#60067=CARTESIAN_POINT ( 'NONE',  ( 10.03696314287999947, 5.117257953482000410, -7.264481182560499128 ) ) ;
#60147=CARTESIAN_POINT ( 'NONE',  ( 11.30995122972050027, 4.452766304612699955, -6.452959986593999275 ) ) ;
#60155=VERTEX_POINT ( 'NONE', #37250 ) ;
#60157=CARTESIAN_POINT ( 'NONE',  ( 10.54687750876899877, 3.382085645339300228, -8.458891008702400072 ) ) ;
#60211=CARTESIAN_POINT ( 'NONE',  ( 8.942941355974880935, 3.045333477771414721, -6.948775311896397078 ) ) ;
#60234=CARTESIAN_POINT ( 'NONE',  ( 11.59999999999999964, 5.064318446328999634, -8.155535082817699788 ) ) ;
#60240=CARTESIAN_POINT ( 'NONE',  ( 11.05946005378019947, 5.036385109519999403, -6.946587256304699309 ) ) ;
#60242=CARTESIAN_POINT ( 'NONE',  ( 9.052088727410998459, 2.999102593977000186, -7.583944523024719331 ) ) ;
#60251=CARTESIAN_POINT ( 'NONE',  ( 10.30371347217102596, 4.589291630936051192, -8.130653431319531776 ) ) ;
#60260=CARTESIAN_POINT ( 'NONE',  ( 8.789886373836322875, 4.000007821194417446, -8.439846342473931173 ) ) ;
#60263=CARTESIAN_POINT ( 'NONE',  ( 10.40749413291699987, 4.788043169210699723, -7.140435631538599281 ) ) ;
#60326=CARTESIAN_POINT ( 'NONE',  ( 10.14887885159599890, 5.269014563305000287, -7.348611220446799486 ) ) ;
#60332=CARTESIAN_POINT ( 'NONE',  ( 11.59999999999999964, 4.000000000000000000, -7.500000000000000000 ) ) ;
#60380=CARTESIAN_POINT ( 'NONE',  ( 10.84393020684979980, 2.750000000000000000, -7.500000000000000000 ) ) ;
#60396=LINE ( 'NONE', #38726, #66281 ) ;
#60407=CARTESIAN_POINT ( 'NONE',  ( 11.19102897915239936, 4.256858847510399890, -8.470038342183499935 ) ) ;
#60411=CARTESIAN_POINT ( 'NONE',  ( 10.34091290906799898, 3.277531639390499851, -8.384179803770500428 ) ) ;
#60474=CARTESIAN_POINT ( 'NONE',  ( 9.129282595918652987, 5.249943393780839074, -7.730023426265350217 ) ) ;
#60480=DIRECTION ( 'NONE',  ( 0.000000000000000000, 0.8514547570628037132, -0.5244280662542021298 ) ) ;
#60489=CARTESIAN_POINT ( 'NONE',  ( 11.03502897915239878, 4.327133900127000388, -8.735435061820998826 ) ) ;
#60497=CARTESIAN_POINT ( 'NONE',  ( 10.32118582084299874, 3.163839350524900063, -6.533484739457099622 ) ) ;
#60530=CARTESIAN_POINT ( 'NONE',  ( 11.03111947020579819, 3.091200775993899974, -7.174999999999999822 ) ) ;
#60553=ORIENTED_EDGE ( 'NONE', *, *, #43451, .F. ) ;
#60564=ORIENTED_EDGE ( 'NONE', *, *, #10722, .T. ) ;
#60582=CARTESIAN_POINT ( 'NONE',  ( 11.29364426047339975, 4.466097552695299733, -8.230103870496201068 ) ) ;
#60584=CARTESIAN_POINT ( 'NONE',  ( 10.56080513895999928, 5.026880838510000338, -6.929150654994399083 ) ) ;
#60585=CARTESIAN_POINT ( 'NONE',  ( 8.773468108405998223, 4.966402032527499344, -7.773695785133000413 ) ) ;
#60593=CARTESIAN_POINT ( 'NONE',  ( 9.606837339593626623, 3.135127465292355087, -7.367607524272325570 ) ) ;
#60605=CARTESIAN_POINT ( 'NONE',  ( 11.31410538575739899, 4.975963290822400076, -7.266662245194900116 ) ) ;
#60608=CARTESIAN_POINT ( 'NONE',  ( 11.36486084871759950, 2.792989229543000107, -7.825000000000000178 ) ) ;
#60611=EDGE_CURVE ( 'NONE', #59647, #23464, #36917, .T. ) ;
#60668=CARTESIAN_POINT ( 'NONE',  ( 10.61656919669529842, 5.225637333137999718, -7.862118085997298778 ) ) ;
#60697=CARTESIAN_POINT ( 'NONE',  ( 10.72191429142990060, 4.025072603369280522, -6.183971186511000084 ) ) ;
#60714=EDGE_CURVE ( 'NONE', #23464, #46101, #63378, .T. ) ;
#60747=CARTESIAN_POINT ( 'NONE',  ( 10.87518447801629939, 4.865987311498500389, -7.480906371072489236 ) ) ;
#60749=ADVANCED_FACE ( 'NONE', ( #59173 ), #61969, .T. ) ;
#60751=CARTESIAN_POINT ( 'NONE',  ( 10.39157120343299923, 3.944651031655580287, -8.640469672413999547 ) ) ;
#60836=CARTESIAN_POINT ( 'NONE',  ( 10.20226357027499908, 5.120085139777000194, -7.716099591766099053 ) ) ;
#60839=ADVANCED_FACE ( 'NONE', ( #65449 ), #64490, .F. ) ;
#60845=CARTESIAN_POINT ( 'NONE',  ( 11.61759063708296047, 5.217265640542000149, -7.842242470354300110 ) ) ;
#60889=CARTESIAN_POINT ( 'NONE',  ( 9.646013540183334456, 4.999583552997728830, -6.731816600031361730 ) ) ;
#60926=EDGE_CURVE ( 'NONE', #6549, #7747, #43211, .T. ) ;
#60928=CARTESIAN_POINT ( 'NONE',  ( 10.30903300763299946, 4.597717337857299746, -8.126922218169600143 ) ) ;
#60931=CARTESIAN_POINT ( 'NONE',  ( 10.77879632507499785, 4.423544049216699747, -8.285174533868300273 ) ) ;
#60932=CARTESIAN_POINT ( 'NONE',  ( 8.898101285863999621, 3.264788442324599860, -6.626387721327399838 ) ) ;
#60944=VERTEX_POINT ( 'NONE', #11729 ) ;
#60952=CARTESIAN_POINT ( 'NONE',  ( 11.53564291764652872, 3.004110626587600308, -7.376893506359599506 ) ) ;
#60953=CARTESIAN_POINT ( 'NONE',  ( 11.37299956498129916, 2.792989229543000107, -7.174999999999999822 ) ) ;
#61016=CARTESIAN_POINT ( 'NONE',  ( 10.76426088462129904, 4.002719309691810778, -6.221990224628999755 ) ) ;
#61046=CARTESIAN_POINT ( 'NONE',  ( 11.09590547754519996, 5.315605332491999846, -7.541753805330609239 ) ) ;
#61093=CARTESIAN_POINT ( 'NONE',  ( 10.45551210286900279, 3.782771630962270759, -8.756187319522085843 ) ) ;
#61095=CARTESIAN_POINT ( 'NONE',  ( 11.41256651104150066, 4.098999650273559503, -6.501426055769400136 ) ) ;
#61099=CARTESIAN_POINT ( 'NONE',  ( 8.922480666858998433, 4.380700808321400075, -8.576476893896000320 ) ) ;
#61101=CARTESIAN_POINT ( 'NONE',  ( 11.02319144466311052, 5.119973997747526262, -7.824989718906223857 ) ) ;
#61184=CARTESIAN_POINT ( 'NONE',  ( 11.55194988689359903, 4.580487242693600081, -8.638573882912000457 ) ) ;
#61191=CARTESIAN_POINT ( 'NONE',  ( 10.56733863405299800, 4.788475529394700558, -8.505794571537999005 ) ) ;
#61248=CARTESIAN_POINT ( 'NONE',  ( 8.837278925393345475, 4.883321897350202612, -6.987098574663183292 ) ) ;
#61252=CARTESIAN_POINT ( 'NONE',  ( 10.57088779216199903, 5.183207142131999845, -7.926693309523199282 ) ) ;
#61273=CARTESIAN_POINT ( 'NONE',  ( 10.82595391537419971, 4.716560378569699452, -7.986661909549199301 ) ) ;
#61276=CARTESIAN_POINT ( 'NONE',  ( 9.024747021775999301, 3.141778309999299967, -8.253120162257399528 ) ) ;
#61278=CARTESIAN_POINT ( 'NONE',  ( 11.12299956498149811, 5.207010770456999893, -7.825000000000000178 ) ) ;
#61286=CARTESIAN_POINT ( 'NONE',  ( 10.21473687196862734, 3.686226525417862998, -8.316748708918906274 ) ) ;
#61296=CARTESIAN_POINT ( 'NONE',  ( 11.36333594839950045, 4.659759757475400832, -6.743912759487099784 ) ) ;
#61301=ORIENTED_EDGE ( 'NONE', *, *, #65261, .T. ) ;
#61331=B_SPLINE_CURVE_WITH_KNOTS ( 'NONE', 3,
 ( #45520, #66830, #7064, #60211, #12317, #33648, #49365, #8108, #28054, #33300, #18256, #23144, #1478, #61248, #39576, #29452 ),
 .UNSPECIFIED., .F., .F.,
 ( 4, 2, 2, 2, 2, 2, 2, 4 ),
 ( 0.000000000000000000, 0.1250000000000004718, 0.2500000000000009437, 0.3750000000000014433, 0.5000000000000018874, 0.6250000000000015543, 0.7500000000000012212, 1.000000000000000000 ),
 .UNSPECIFIED. ) ;
#61335=B_SPLINE_CURVE_WITH_KNOTS ( 'NONE', 3,
 ( #46624, #62683, #35785, #45930, #18676, #9199, #45251, #51853, #30542, #40339 ),
 .UNSPECIFIED., .F., .F.,
 ( 4, 2, 2, 2, 4 ),
 ( 0.000000000000000000, 0.2500000000000000000, 0.5000000000000000000, 0.7500000000000000000, 1.000000000000000000 ),
 .UNSPECIFIED. ) ;
#61355=CARTESIAN_POINT ( 'NONE',  ( 10.29522949779699914, 4.480999174483200065, -8.221351791991999391 ) ) ;
#61380=CARTESIAN_POINT ( 'NONE',  ( 11.00000000000000000, 2.941427501403999667, -7.825000000000000178 ) ) ;
#61389=CARTESIAN_POINT ( 'NONE',  ( 11.84388784977539899, 2.744254309011999737, -7.428242901739219306 ) ) ;
#61406=CARTESIAN_POINT ( 'NONE',  ( 11.59999999999999964, 3.182579051151299687, -7.174999999999999822 ) ) ;
#61412=DIRECTION ( 'NONE',  ( 0.000000000000000000, 0.000000000000000000, -1.000000000000000000 ) ) ;
#61415=CARTESIAN_POINT ( 'NONE',  ( 10.93937577273821482, 3.538822733277925181, -8.699885912910445995 ) ) ;
#61439=CARTESIAN_POINT ( 'NONE',  ( 11.13764426047339917, 4.613828180779599997, -8.461511872390000022 ) ) ;
#61442=CARTESIAN_POINT ( 'NONE',  ( 9.731000818238999983, 3.111278474435999808, -7.967991827203400490 ) ) ;
#61482=CARTESIAN_POINT ( 'NONE',  ( 11.71922412107039868, 4.069539071394910223, -6.185573549454999487 ) ) ;
#61524=CARTESIAN_POINT ( 'NONE',  ( 10.76841504065829902, 4.914510326623699576, -6.818119527508899935 ) ) ;
#61532=CARTESIAN_POINT ( 'NONE',  ( 11.20733594839949809, 4.840266102192999575, -6.537051788466999191 ) ) ;
#61551=CARTESIAN_POINT ( 'NONE',  ( 11.59999999999999964, 3.182579051151299687, -7.174999999999999822 ) ) ;
#61555=B_SPLINE_CURVE_WITH_KNOTS ( 'NONE', 3,
 ( #48057, #37220, #10302, #503, #36884, #58537, #37905, #21819, #43152, #64457 ),
 .UNSPECIFIED., .F., .F.,
 ( 4, 2, 2, 2, 4 ),
 ( 0.000000000000000000, 0.2500000000000001665, 0.5000000000000003331, 0.7500000000000001110, 1.000000000000000000 ),
 .UNSPECIFIED. ) ;
#61592=CARTESIAN_POINT ( 'NONE',  ( 9.785684229509998389, 3.098260518542999886, -6.592668585875199661 ) ) ;
#61610=CARTESIAN_POINT ( 'NONE',  ( 10.97364560330029981, 4.265439025801100570, -6.675475461903199736 ) ) ;
#61612=CARTESIAN_POINT ( 'NONE',  ( 11.11123293495519881, 3.108594079907299967, -7.464165716332529676 ) ) ;
#61613=CARTESIAN_POINT ( 'NONE',  ( 9.733963142879998642, 5.117257953482000410, -7.264481182560499128 ) ) ;
#61710=LINE ( 'NONE', #44962, #40054 ) ;
#61724=CARTESIAN_POINT ( 'NONE',  ( 11.68277869730536977, 3.468607053297499743, -6.452143920160000157 ) ) ;
#61742=CARTESIAN_POINT ( 'NONE',  ( 10.46684687351657672, 3.231816600031355069, -8.499583552997723501 ) ) ;
#61776=CARTESIAN_POINT ( 'NONE',  ( 10.40333997687999990, 4.213854445120500003, -6.519583185858300212 ) ) ;
#61778=CARTESIAN_POINT ( 'NONE',  ( 8.998468108405997867, 5.098602956001000663, -7.811136554427399403 ) ) ;
#61837=CARTESIAN_POINT ( 'NONE',  ( 9.242292592096250203, 3.634505416671740097, -6.294013902202234334 ) ) ;
#61861=CARTESIAN_POINT ( 'NONE',  ( 10.47303166480599934, 2.862083839376000416, -7.580230465881790280 ) ) ;
#61877=CARTESIAN_POINT ( 'NONE',  ( 10.29184687351566652, 3.000416447002276943, -6.731816600031355513 ) ) ;
#61891=ORIENTED_EDGE ( 'NONE', *, *, #25587, .T. ) ;
#61937=CARTESIAN_POINT ( 'NONE',  ( 9.836342523874998633, 2.735516931877000513, -7.306436165809000016 ) ) ;
#61957=CARTESIAN_POINT ( 'NONE',  ( 11.63825819896753977, 3.148796120250299868, -7.660469764776300039 ) ) ;
#61962=CARTESIAN_POINT ( 'NONE',  ( 10.18144474310099845, 5.015709705366000470, -7.992914665944799602 ) ) ;
#61969=CONICAL_SURFACE ( 'NONE', #63089, 0.9999998338055000602, 0.7853981908209605178 ) ;
#62003=CARTESIAN_POINT ( 'NONE',  ( 9.414763540182331525, 2.782534154164605589, -7.827184855449099921 ) ) ;
#62024=DIRECTION ( 'NONE',  ( 0.000000000000000000, 1.000000000000000000, 0.000000000000000000 ) ) ;
#62070=CARTESIAN_POINT ( 'NONE',  ( 10.51414141025500015, 4.615773412711500434, -8.596754040696000132 ) ) ;
#62071=ORIENTED_EDGE ( 'NONE', *, *, #21851, .T. ) ;
#62119=CARTESIAN_POINT ( 'NONE',  ( 10.50180110216399854, 3.143606124884799957, -6.976989117212499814 ) ) ;
#62122=CARTESIAN_POINT ( 'NONE',  ( 9.123101285863999266, 3.353260484332500013, -6.731514281717299930 ) ) ;
#62205=CARTESIAN_POINT ( 'NONE',  ( 10.12426357027499790, 5.254871132332000094, -7.742104041724699570 ) ) ;
#62218=CARTESIAN_POINT ( 'NONE',  ( 10.19809687351566474, 4.327184855449106138, -6.282534154164607365 ) ) ;
#62250=CARTESIAN_POINT ( 'NONE',  ( 11.19955063476130164, 4.976598135215295038, -6.673569913327196623 ) ) ;
#62279=CARTESIAN_POINT ( 'NONE',  ( 9.633709346416999608, 5.155548326249999924, -6.951281079990299538 ) ) ;
#62299=CARTESIAN_POINT ( 'NONE',  ( 11.24025954179439957, 4.771812902496799680, -8.141292208271599051 ) ) ;
#62302=CARTESIAN_POINT ( 'NONE',  ( 8.695468108405998819, 5.098602956001000663, -7.811136554427399403 ) ) ;
#62311=CARTESIAN_POINT ( 'NONE',  ( 9.353545867770625577, 4.858658389798049981, -7.668041776205901883 ) ) ;
#62347=ORIENTED_EDGE ( 'NONE', *, *, #47994, .T. ) ;
#62404=( LENGTH_UNIT ( ) NAMED_UNIT ( * ) SI_UNIT ( .MILLI., .METRE. ) );
#62411=CARTESIAN_POINT ( 'NONE',  ( 10.72702344389999851, 2.995605560827999891, -6.890449684422599752 ) ) ;
#62429=FACE_OUTER_BOUND ( 'NONE', #47108, .T. ) ;
#62460=CARTESIAN_POINT ( 'NONE',  ( 11.58071932425156980, 3.832730087831799803, -8.628410767520000135 ) ) ;
#62462=CARTESIAN_POINT ( 'NONE',  ( 8.947809814040999399, 4.698458605182900705, -8.403266072559899769 ) ) ;
#62497=CARTESIAN_POINT ( 'NONE',  ( 10.51414141025500015, 4.615773412711500434, -8.596754040696000132 ) ) ;
#62550=CARTESIAN_POINT ( 'NONE',  ( 10.12426357027499790, 5.254871132332000094, -7.742104041724699570 ) ) ;
#62603=VERTEX_POINT ( 'NONE', #39489 ) ;
#62628=CARTESIAN_POINT ( 'NONE',  ( 10.28026357027499849, 4.985299147223100746, -7.690095141806899903 ) ) ;
#62631=CARTESIAN_POINT ( 'NONE',  ( 9.098721904869998767, 5.115452802765999785, -8.126218358304999612 ) ) ;
#62641=CARTESIAN_POINT ( 'NONE',  ( 8.973608660036624940, 4.220957842099207546, -6.653412791890684019 ) ) ;
#62650=EDGE_CURVE ( 'NONE', #28311, #7747, #18334, .T. ) ;
#62683=CARTESIAN_POINT ( 'NONE',  ( 10.06927318630900103, 4.756452637475338641, -8.526145288591964189 ) ) ;
#62712=CARTESIAN_POINT ( 'NONE',  ( 9.028772138681999238, 3.677371150249499898, -6.695252480703800302 ) ) ;
#62725=EDGE_CURVE ( 'NONE', #5638, #26310, #38242, .T. ) ;
#62746=CARTESIAN_POINT ( 'NONE',  ( 11.01790547754519878, 5.174295865741999734, -7.537269019642879542 ) ) ;
#62797=CARTESIAN_POINT ( 'NONE',  ( 10.21462282008599942, 4.523146351753199568, -8.343818446627699004 ) ) ;
#62799=CARTESIAN_POINT ( 'NONE',  ( 9.425038493598998812, 4.627468580434300094, -6.901676404381399621 ) ) ;
#62833=CARTESIAN_POINT ( 'NONE',  ( 8.810863317747999801, 4.960863370448500120, -7.500000000073117512 ) ) ;
#62838=CARTESIAN_POINT ( 'NONE',  ( 11.76588784977539781, 2.879134238109999799, -7.435950347916509884 ) ) ;
#62857=CARTESIAN_POINT ( 'NONE',  ( 11.39975833414730033, 4.796537143354000499, -7.174999999999999822 ) ) ;
#62931=ORIENTED_EDGE ( 'NONE', *, *, #39815, .F. ) ;
#62961=CARTESIAN_POINT ( 'NONE',  ( 11.15221028326116048, 3.091096528151293210, -7.175011397899978327 ) ) ;
#62964=CARTESIAN_POINT ( 'NONE',  ( 11.28949010443639978, 5.000675062740000065, -7.574834962826040297 ) ) ;
#62968=CARTESIAN_POINT ( 'NONE',  ( 9.554646554150998838, 4.619310611972400338, -8.619302797893999113 ) ) ;
#63015=FACE_OUTER_BOUND ( 'NONE', #42546, .T. ) ;
#63045=CARTESIAN_POINT ( 'NONE',  ( 11.80233327354039830, 2.898463260143000042, -6.779499720266399798 ) ) ;
#63046=CARTESIAN_POINT ( 'NONE',  ( 8.978113844317999082, 4.218953675027299788, -6.661091642253600398 ) ) ;
#63063=B_SPLINE_SURFACE_WITH_KNOTS ( 'NONE', 3, 3, ( 
 ( #22541, #54012, #540, #1571 ),
 ( #26777, #37592, #22889, #6463 ),
 ( #43187, #27810, #53338, #21852 ),
 ( #64154, #16612, #65185, #6809 ) ),
 .UNSPECIFIED., .F., .F., .F.,
 ( 4, 4 ),
 ( 4, 4 ),
 ( -0.01349945606786999951, 0.08053609420915000539 ),
 ( -0.0005287450254680999126, 0.02696599629895000266 ),
 .UNSPECIFIED. ) ;
#63089=AXIS2_PLACEMENT_3D ( 'NONE', #5001, #47661, #101 ) ;
#63136=CARTESIAN_POINT ( 'NONE',  ( 10.66995391537419913, 4.943675741382899780, -8.140910455049299443 ) ) ;
#63141=CARTESIAN_POINT ( 'NONE',  ( 8.802265421554999136, 3.811499292588199861, -8.475084258675400051 ) ) ;
#63155=CARTESIAN_POINT ( 'NONE',  ( 9.258504216683469679, 4.163629870566138536, -6.250027056024106464 ) ) ;
#63175=LINE ( 'NONE', #47465, #34208 ) ;
#63177=CARTESIAN_POINT ( 'NONE',  ( 11.72433327354039889, 3.016779570871600313, -6.856888818507299810 ) ) ;
#63222=CARTESIAN_POINT ( 'NONE',  ( 10.46887750876899936, 3.307728619566300043, -8.574279626736998949 ) ) ;
#63225=CARTESIAN_POINT ( 'NONE',  ( 11.59999999999999609, 3.168976350368595263, -7.997379651729209726 ) ) ;
#63242=DIRECTION ( 'NONE',  ( 1.000000000000000000, 0.000000000000000000, 0.000000000000000000 ) ) ;
#63258=VERTEX_POINT ( 'NONE', #8277 ) ;
#63259=CARTESIAN_POINT ( 'NONE',  ( 9.508513540182335078, 3.836375382625529795, -8.749999999999998224 ) ) ;
#63297=AXIS2_PLACEMENT_3D ( 'NONE', #56405, #22597, #13758 ) ;
#63312=CARTESIAN_POINT ( 'NONE',  ( 11.38795122972049967, 4.398282450130399646, -6.578956058177199751 ) ) ;
#63315=CARTESIAN_POINT ( 'NONE',  ( 9.276025935145998602, 3.814256956409300070, -6.234344474498000110 ) ) ;
#63320=AXIS2_PLACEMENT_3D ( 'NONE', #29467, #35045, #40282 ) ;
#63364=CARTESIAN_POINT ( 'NONE',  ( 11.33810207955129812, 4.796537143354000499, -7.825000000000000178 ) ) ;
#63378=LINE ( 'NONE', #20742, #20692 ) ;
#63400=CARTESIAN_POINT ( 'NONE',  ( 11.72433327354039889, 3.016779570871600313, -6.856888818507299810 ) ) ;
#63401=CARTESIAN_POINT ( 'NONE',  ( 9.434038493598999153, 4.627468580434300094, -6.901676404381399621 ) ) ;
#63487=CARTESIAN_POINT ( 'NONE',  ( 11.62579573085663043, 5.239377455231000624, -7.714452430741599365 ) ) ;
#63490=CARTESIAN_POINT ( 'NONE',  ( 9.222405316139999698, 3.815922504313999930, -8.347244604637999998 ) ) ;
#63515=FACE_OUTER_BOUND ( 'NONE', #11998, .T. ) ;
#63534=CARTESIAN_POINT ( 'NONE',  ( 11.64122412107036908, 4.062069863985690255, -6.326756392227999015 ) ) ;
#63574=CARTESIAN_POINT ( 'NONE',  ( 11.53979707368350027, 3.569730287184500472, -6.748224392138099326 ) ) ;
#63577=CARTESIAN_POINT ( 'NONE',  ( 11.59999999999999964, 3.137911629819546189, -7.912526219123482640 ) ) ;
#63611=CARTESIAN_POINT ( 'NONE',  ( 9.623096873515669003, 5.217465845835395299, -7.827184855449101697 ) ) ;
#63660=CARTESIAN_POINT ( 'NONE',  ( 10.16360887879199915, 3.741427262966100287, -6.387851364408000165 ) ) ;
#63661=CARTESIAN_POINT ( 'NONE',  ( 11.41256651104150066, 4.098999650273559503, -6.501426055769400136 ) ) ;
#63664=CARTESIAN_POINT ( 'NONE',  ( 9.909254614703000286, 2.760277452415999644, -7.815392442832299835 ) ) ;
#63673=B_SPLINE_CURVE_WITH_KNOTS ( 'NONE', 3,
 ( #44557, #65849, #17973, #23898, #28820, #6775, #66538, #18658, #39991, #39292 ),
 .UNSPECIFIED., .F., .F.,
 ( 4, 2, 2, 2, 4 ),
 ( 0.000000000000000000, 0.2499999999999995559, 0.4999999999999991118, 0.7499999999999995559, 1.000000000000000000 ),
 .UNSPECIFIED. ) ;
#63744=CARTESIAN_POINT ( 'NONE',  ( 11.76077869730539938, 3.404661623424200201, -6.326049646822999861 ) ) ;
#63745=CARTESIAN_POINT ( 'NONE',  ( 8.750151519676999001, 4.018750234858180725, -8.366807394121199337 ) ) ;
#63765=CARTESIAN_POINT ( 'NONE',  ( 8.786046699800500903, 4.845411057630703233, -7.961595344540238095 ) ) ;
#63768=CARTESIAN_POINT ( 'NONE',  ( 11.29364426047339975, 4.466097552695299733, -8.230103870496201068 ) ) ;
#63779=CARTESIAN_POINT ( 'NONE',  ( 10.60746886766490071, 3.501664543805500074, -6.594573315824700188 ) ) ;
#63780=ORIENTED_EDGE ( 'NONE', *, *, #15854, .T. ) ;
#63806=CARTESIAN_POINT ( 'NONE',  ( 11.60000000000000142, 3.327218134278213668, -6.851153339015914945 ) ) ;
#63830=CARTESIAN_POINT ( 'NONE',  ( 11.10887482311539998, 5.184953745778000389, -7.978749413531599721 ) ) ;
#63834=CARTESIAN_POINT ( 'NONE',  ( 9.703659112603999048, 3.623260508844300176, -8.280881105104999307 ) ) ;
#63871=CARTESIAN_POINT ( 'NONE',  ( 11.35545123989519922, 4.475221369382300196, -8.417769225118700405 ) ) ;
#63904=CARTESIAN_POINT ( 'NONE',  ( 8.768793171737998549, 3.595811914175000013, -8.374125585548998885 ) ) ;
#63906=ORIENTED_EDGE ( 'NONE', *, *, #62725, .T. ) ;
#63914=CARTESIAN_POINT ( 'NONE',  ( 11.31825954179440075, 4.666231193203100425, -8.053565341712399572 ) ) ;
#63916=CARTESIAN_POINT ( 'NONE',  ( 11.60000000000000142, 3.186931496511416828, -8.037608584222629915 ) ) ;
#63943=CARTESIAN_POINT ( 'NONE',  ( 10.74760529021567734, 4.040385281810796592, -8.373188771871163283 ) ) ;
#63993=CARTESIAN_POINT ( 'NONE',  ( 10.79718447801629999, 5.003225587801999552, -7.477880487566260115 ) ) ;
#63999=CARTESIAN_POINT ( 'NONE',  ( 9.327747021775998348, 3.141778309999299967, -8.253120162257399528 ) ) ;
#64001=CARTESIAN_POINT ( 'NONE',  ( 10.66995391537419913, 4.943675741382899780, -8.140910455049299443 ) ) ;
#64005=CARTESIAN_POINT ( 'NONE',  ( 9.959912909067998754, 3.190593056227700064, -8.490578012456198920 ) ) ;
#64036=COLOUR_RGB ( '', 0.31764706, 0.68627451, 0.89019608) ;
#64051=ORIENTED_EDGE ( 'NONE', *, *, #9860, .T. ) ;
#64058=CARTESIAN_POINT ( 'NONE',  ( 10.16476354018241501, 5.217465845835396188, -7.172815144550905408 ) ) ;
#64071=VECTOR ( 'NONE', #5782, 1000.000000000000000 ) ;
#64084=CARTESIAN_POINT ( 'NONE',  ( 8.724822372493999723, 3.750788346126100237, -8.315254653915399530 ) ) ;
#64108=CARTESIAN_POINT ( 'NONE',  ( 10.82595391537419971, 4.716560378569699452, -7.986661909549199301 ) ) ;
#64119=CARTESIAN_POINT ( 'NONE',  ( 10.44125056272499918, 5.033400911533000510, -7.515315513715298934 ) ) ;
#64147=CARTESIAN_POINT ( 'NONE',  ( 11.60000000000000142, 3.244119941477265456, -6.982116912833853384 ) ) ;
#64154=CARTESIAN_POINT ( 'NONE',  ( 8.734200250017998712, 4.093844212487689482, -8.386722339907899837 ) ) ;
#64173=CARTESIAN_POINT ( 'NONE',  ( 10.37457053952199892, 3.551693493661699730, -6.451042711717000167 ) ) ;
#64177=CARTESIAN_POINT ( 'NONE',  ( 9.804975701332999449, 4.636077325177999420, -8.089163458558500608 ) ) ;
#64213=CARTESIAN_POINT ( 'NONE',  ( 11.48522412107029922, 4.047131449166419870, -6.609122077774299164 ) ) ;
#64217=VERTEX_POINT ( 'NONE', #19548 ) ;
#64255=CARTESIAN_POINT ( 'NONE',  ( 11.12133729122639991, 3.134101783108900197, -7.477221318588949117 ) ) ;
#64282=CARTESIAN_POINT ( 'NONE',  ( 10.91991225946278199, 4.700767082376348327, -6.977491532540834207 ) ) ;
#64314=VERTEX_POINT ( 'NONE', #42933 ) ;
#64331=CARTESIAN_POINT ( 'NONE',  ( 10.57564694612699974, 3.068007311611700150, -7.871941502982999772 ) ) ;
#64338=CARTESIAN_POINT ( 'NONE',  ( 10.36624205625100004, 3.590523439766200031, -8.565862728991998409 ) ) ;
#64340=CARTESIAN_POINT ( 'NONE',  ( 10.98995257254739855, 2.904643075091000171, -7.818564472783199548 ) ) ;
#64411=ADVANCED_BREP_SHAPE_REPRESENTATION ( '', ( #31079, #9676 ), #52154 ) ;
#64423=FACE_OUTER_BOUND ( 'NONE', #12476, .T. ) ;
#64424=CARTESIAN_POINT ( 'NONE',  ( 9.178734463322998138, 4.104624583183299258, -8.498947444525299488 ) ) ;
#64444=CARTESIAN_POINT ( 'NONE',  ( 11.44133594839949986, 4.569506585117100173, -6.847343244997600387 ) ) ;
#64448=ORIENTED_EDGE ( 'NONE', *, *, #30159, .T. ) ;
#64457=CARTESIAN_POINT ( 'NONE',  ( 10.89393020684959978, 2.750000000000000000, -7.500000000000000000 ) ) ;
#64458=CARTESIAN_POINT ( 'NONE',  ( 10.98656920625009903, 4.032067152264009913, -6.608450613814399688 ) ) ;
#64476=EDGE_LOOP ( 'NONE', ( #4811, #3674, #13310, #16681, #21153 ) ) ;
#64485=CARTESIAN_POINT ( 'NONE',  ( 11.59999999999999964, 5.179498027601999510, -7.174999999999999822 ) ) ;
#64490=B_SPLINE_SURFACE_WITH_KNOTS ( 'NONE', 3, 3, ( 
 ( #61252, #34349, #49723, #55668, #2517, #45179, #7413, #66484, #13370, #49033, #33998, #2181, #7070, #1141, #23496, #33305, #65092, #1832, #17569, #17215, #38896, #33653, #54970, #28762, #23150, #44499, #65792, #24877, #40609, #45524, #61937, #56352, #61592, #24187, #45861, #19284, #3540, #56699, #62279, #8799, #14397, #14050, #30139, #19635, #51444, #67170, #8458, #40956, #66833, #18946, #50765, #35378, #46207, #51106, #24534, #29457, #2859, #40275, #13709, #35038, #67514, #29802, #3208, #21025, #55162, #55512, #42359 ),
 ( #7612, #48276, #22995, #17413, #382, #60751, #64338, #60411, #18112, #32215, #26962, #44345, #21361, #10870, #63660, #65985, #58420, #44691, #65642, #60067, #38737, #12865, #17769, #39087, #12517, #54817, #33848, #21698, #7267, #28606, #31865, #49918, #43034, #26622, #2030, #23347, #42691, #28960, #33502, #53182, #6917, #12172, #39430, #28249, #5280, #49569, #53529, #63999, #10525, #1679, #34194, #50263, #15776, #37106, #47941, #41, #16117, #37443, #58764, #5621, #61778, #13561, #62462, #61099, #29299, #45026, #40453 ),
 ( #23691, #35899, #25063, #51632, #35568, #13219, #40129, #24036, #13899, #67020, #39778, #46052, #45370, #57215, #46395, #9317, #29651, #3389, #19129, #50952, #41154, #45712, #40799, #67698, #34879, #8305, #24725, #2712, #61442, #66331, #19825, #34545, #14582, #67356, #35227, #56539, #30659, #2368, #18455, #8643, #19476, #55857, #7960, #56197, #14241, #3050, #24381, #29993, #50610, #66678, #18801, #51293, #62122, #56884, #8982, #30322, #3728, #10359, #10013, #5112, #11052, #21534, #53016, #4418, #58255, #63141, #25756 ),
 ( #15948, #42189, #68386, #26799, #4069, #31693, #68048, #36243, #26448, #47085, #10699, #47780, #20506, #69088, #15266, #41832, #32044, #42868, #36590, #21194, #52323, #41489, #64177, #37277, #52664, #42523, #63834, #53360, #58597, #5462, #48113, #214, #15609, #16291, #31351, #37614, #58946, #62799, #51968, #4760, #57562, #25408, #46742, #57914, #20162, #63490, #14920, #36940, #26101, #9663, #31011, #47427, #68736, #20853, #54037, #567, #49142, #65213, #12436, #49487, #18035, #1597, #39351, #38657, #44267, #1949, #22914 ) ),
 .UNSPECIFIED., .F., .F., .F.,
 ( 4, 4 ),
 ( 4, 1, 1, 1, 1, 1, 1, 1, 1, 1, 1, 1, 1, 1, 1, 1, 1, 1, 1, 1, 1, 1, 1, 1, 1, 1, 1, 1, 1, 1, 1, 1, 1, 1, 1, 1, 1, 1, 1, 1, 1, 1, 1, 1, 1, 1, 1, 1, 1, 1, 1, 1, 1, 1, 1, 1, 1, 1, 1, 1, 1, 1, 1, 1, 4 ),
 ( -0.02000000000000000042, 1.020000000000000018 ),
 ( -0.02000000000000000042, -0.003749999999999999861, 0.01250000000000000069, 0.02875000000000000125, 0.04499999999999999833, 0.06124999999999999889, 0.07749999999999999944, 0.09375000000000000000, 0.1100000000000000006, 0.1262500000000000011, 0.1424999999999999878, 0.1587500000000000022, 0.1749999999999999889, 0.1912500000000000033, 0.2074999999999999900, 0.2237500000000000044, 0.2399999999999999911, 0.2562499999999999778, 0.2725000000000000200, 0.2887500000000000067, 0.3049999999999999933, 0.3212499999999999800, 0.3375000000000000222, 0.3537500000000000089, 0.3699999999999999956, 0.3862499999999999822, 0.4025000000000000244, 0.4187500000000000111, 0.4349999999999999978, 0.4512499999999999845, 0.4675000000000000266, 0.4837500000000000133, 0.5000000000000000000, 0.5162499999999999867, 0.5324999999999999734, 0.5487499999999999600, 0.5649999999999999467, 0.5812500000000000444, 0.5975000000000000311, 0.6137500000000000178, 0.6300000000000000044, 0.6462499999999999911, 0.6624999999999999778, 0.6787499999999999645, 0.6949999999999999512, 0.7112500000000000488, 0.7275000000000000355, 0.7437500000000000222, 0.7600000000000000089, 0.7762499999999999956, 0.7924999999999999822, 0.8087499999999999689, 0.8249999999999999556, 0.8412500000000000533, 0.8575000000000000400, 0.8737500000000000266, 0.8900000000000000133, 0.9062500000000000000, 0.9224999999999999867, 0.9387499999999999734, 0.9549999999999999600, 0.9712499999999999467, 0.9875000000000000444, 1.003749999999999920, 1.020000000000000018 ),
 .UNSPECIFIED. ) ;
#64512=CARTESIAN_POINT ( 'NONE',  ( 10.76841504065829902, 4.914510326623699576, -6.818119527508899935 ) ) ;
#64560=ORIENTED_EDGE ( 'NONE', *, *, #4774, .F. ) ;
#64572=CARTESIAN_POINT ( 'NONE',  ( 10.61476354018239832, 5.217465845835394411, -7.172815144550904520 ) ) ;
#64600=CARTESIAN_POINT ( 'NONE',  ( 11.85159063708299954, 4.825025306051200502, -7.731961446576300467 ) ) ;
#64682=CARTESIAN_POINT ( 'NONE',  ( 10.98995257254739855, 2.904643075091000171, -7.818564472783199548 ) ) ;
#64690=CARTESIAN_POINT ( 'NONE',  ( 10.49764694612699856, 2.940513484064000149, -7.922821994243300914 ) ) ;
#64743=CARTESIAN_POINT ( 'NONE',  ( 10.81059687351629961, 3.370476274536378103, -6.407767014557176566 ) ) ;
#64770=CARTESIAN_POINT ( 'NONE',  ( 11.85159063708299954, 4.825025306051200502, -7.731961446576300467 ) ) ;
#64772=CARTESIAN_POINT ( 'NONE',  ( 11.02301463001509774, 4.547357026650399980, -6.623338154204899908 ) ) ;
#64773=CARTESIAN_POINT ( 'NONE',  ( 9.862621437244998290, 4.667147537636399335, -6.749162825004299648 ) ) ;
#64794=CARTESIAN_POINT ( 'NONE',  ( 11.36749010443639918, 4.863785690678500195, -7.564597762509089662 ) ) ;
#64834=CARTESIAN_POINT ( 'NONE',  ( 11.60000000000000142, 4.420828903570660273, -6.483899970161564497 ) ) ;
#64860=CARTESIAN_POINT ( 'NONE',  ( 10.54272335273199879, 4.444874504667400750, -8.698083075453000745 ) ) ;
#64900=CARTESIAN_POINT ( 'NONE',  ( 10.48280513895999988, 4.903310631086600146, -6.997844089834400094 ) ) ;
#64929=CARTESIAN_POINT ( 'NONE',  ( 10.57435795695566583, 5.250000000000000000, -7.807440182398264206 ) ) ;
#64939=CARTESIAN_POINT ( 'NONE',  ( 10.50595525820100029, 3.918212119278319694, -6.637672143048099827 ) ) ;
#64985=CARTESIAN_POINT ( 'NONE',  ( 10.60226354018307937, 5.092232985442822546, -8.129523725463620565 ) ) ;
#65012=LINE ( 'NONE', #26259, #12515 ) ;
#65023=CARTESIAN_POINT ( 'NONE',  ( 10.72333863405319931, 4.619094858989799768, -8.289729326049599223 ) ) ;
#65030=CARTESIAN_POINT ( 'NONE',  ( 11.58071932425156980, 3.832730087831799803, -8.628410767520000135 ) ) ;
#65085=CARTESIAN_POINT ( 'NONE',  ( 10.78976354018297634, 3.672815144550904076, -6.282534154164603812 ) ) ;
#65092=CARTESIAN_POINT ( 'NONE',  ( 10.19095058442699830, 4.507735863714500191, -6.325866838823999139 ) ) ;
#65116=CARTESIAN_POINT ( 'NONE',  ( 11.01790547754519878, 5.174295865741999734, -7.537269019642879542 ) ) ;
#65117=CARTESIAN_POINT ( 'NONE',  ( 8.925442991499998868, 3.936771438983030169, -6.497580701799000380 ) ) ;
#65141=CARTESIAN_POINT ( 'NONE',  ( 11.68748876160954886, 3.399618311400500303, -8.124372018288600117 ) ) ;
#65165=CARTESIAN_POINT ( 'NONE',  ( 11.59999999999999964, 4.000000000000000000, -7.500000000000000000 ) ) ;
#65172=CARTESIAN_POINT ( 'NONE',  ( 11.18424042080583369, 4.544092497359196514, -6.342116603374313044 ) ) ;
#65181=CARTESIAN_POINT ( 'NONE',  ( 11.59999999999999964, 4.834915812642036848, -6.701316188976606192 ) ) ;
#65185=CARTESIAN_POINT ( 'NONE',  ( 8.705629240797998492, 3.771058080785100408, -8.376522367004298530 ) ) ;
#65213=CARTESIAN_POINT ( 'NONE',  ( 8.918455549952998496, 4.674761969675400586, -6.955569812538500152 ) ) ;
#65255=CARTESIAN_POINT ( 'NONE',  ( 10.39969598649000027, 4.888000489779200208, -8.028730309000598808 ) ) ;
#65261=EDGE_CURVE ( 'NONE', #24634, #60155, #51784, .T. ) ;
#65294=CARTESIAN_POINT ( 'NONE',  ( 11.02287616594229824, 3.738072157442200005, -6.674353346984900348 ) ) ;
#65332=ORIENTED_EDGE ( 'NONE', *, *, #54309, .F. ) ;
#65368=CARTESIAN_POINT ( 'NONE',  ( 11.05336220499919797, 3.034597079077000270, -7.825000000000000178 ) ) ;
#65377=CARTESIAN_POINT ( 'NONE',  ( 11.43302763632549990, 2.964209339073000216, -7.022058766158599141 ) ) ;
#65385=CARTESIAN_POINT ( 'NONE',  ( 10.44841638348500013, 2.891666689023999925, -7.230023356477299323 ) ) ;
#65449=FACE_OUTER_BOUND ( 'NONE', #49603, .T. ) ;
#65452=CARTESIAN_POINT ( 'NONE',  ( 11.12299956498149811, 5.207010770456999893, -7.825000000000000178 ) ) ;
#65468=CARTESIAN_POINT ( 'NONE',  ( 10.37199293566600034, 4.633387186021100668, -8.276990458557699881 ) ) ;
#65469=CARTESIAN_POINT ( 'NONE',  ( 8.722809814040999754, 4.614409247670200109, -8.294571108394100278 ) ) ;
#65480=CARTESIAN_POINT ( 'NONE',  ( 9.784141369869628235, 4.423591863150092784, -8.265573120213877800 ) ) ;
#65492=CARTESIAN_POINT ( 'NONE',  ( 10.60441638348510018, 3.158410350011299883, -7.294998899090099798 ) ) ;
#65566=DIRECTION ( 'NONE',  ( -1.000000000000000000, 0.000000000000000000, 0.000000000000000000 ) ) ;
#65591=CARTESIAN_POINT ( 'NONE',  ( 11.01279632507519857, 4.624908853805600906, -8.658468685623999406 ) ) ;
#65595=EDGE_LOOP ( 'NONE', ( #20294, #48391, #13766, #29101 ) ) ;
#65613=CARTESIAN_POINT ( 'NONE',  ( 10.60434687351569494, 5.250000000000001776, -7.336375382625535124 ) ) ;
#65631=CARTESIAN_POINT ( 'NONE',  ( 8.706426979769998908, 3.641148095589300304, -8.276078370613198842 ) ) ;
#65640=CARTESIAN_POINT ( 'NONE',  ( 11.21564426047340035, 4.539962866738299851, -8.345807871442598724 ) ) ;
#65642=CARTESIAN_POINT ( 'NONE',  ( 10.06229229006299875, 4.987433183662999703, -6.926667499798199401 ) ) ;
#65725=CARTESIAN_POINT ( 'NONE',  ( 11.08425954179440076, 4.982976321082899673, -8.316745941391600283 ) ) ;
#65733=CARTESIAN_POINT ( 'NONE',  ( 11.45348876160960039, 3.114179898019400206, -8.421216112044099589 ) ) ;
#65792=CARTESIAN_POINT ( 'NONE',  ( 9.937659112603999034, 3.444147913214900214, -8.652134039551000910 ) ) ;
#65813=CARTESIAN_POINT ( 'NONE',  ( 11.12133729122639991, 3.134101783108900197, -7.477221318588949117 ) ) ;
#65817=CARTESIAN_POINT ( 'NONE',  ( 11.59603632436369125, 3.157359628034400068, -7.303218851299499548 ) ) ;
#65818=CARTESIAN_POINT ( 'NONE',  ( 8.874784697134998623, 4.545051930576500254, -6.656340890368899643 ) ) ;
#65826=CARTESIAN_POINT ( 'NONE',  ( 9.454862456499625978, 4.412447805680870694, -6.728365969834097626 ) ) ;
#65841=CARTESIAN_POINT ( 'NONE',  ( 10.30903300763299946, 4.597717337857299746, -8.126922218169600143 ) ) ;
#65849=CARTESIAN_POINT ( 'NONE',  ( 11.58457173739308210, 4.937225096800481161, -8.361882233189918523 ) ) ;
#65853=LINE ( 'NONE', #43509, #66405 ) ;
#65904=CARTESIAN_POINT ( 'NONE',  ( 11.05964426047339799, 4.687693494822500639, -8.577215873335999774 ) ) ;
#65924=CARTESIAN_POINT ( 'NONE',  ( 8.751496707488000126, 4.081676005979390176, -8.356402621895700378 ) ) ;
#65931=CARTESIAN_POINT ( 'NONE',  ( 10.80502344389999791, 2.874741265256000489, -6.817099149379099110 ) ) ;
#65972=CARTESIAN_POINT ( 'NONE',  ( 10.55478570706233299, 5.131706358131709500, -8.113400509224881318 ) ) ;
#65981=CARTESIAN_POINT ( 'NONE',  ( 11.73256516821459883, 4.706297556651700020, -8.212808089543500500 ) ) ;
#65985=CARTESIAN_POINT ( 'NONE',  ( 10.13827973160999818, 4.102460098134500299, -6.362794488108000301 ) ) ;
#66026=CARTESIAN_POINT ( 'NONE',  ( 11.05435090131019926, 5.119447121461000449, -8.192386390235398608 ) ) ;
#66070=CARTESIAN_POINT ( 'NONE',  ( 10.59610807141099897, 4.052703327804870526, -8.639522915742999132 ) ) ;
#66077=CARTESIAN_POINT ( 'NONE',  ( 11.47810404293059960, 3.436653965247300047, -8.647151967355000579 ) ) ;
#66122=ORIENTED_EDGE ( 'NONE', *, *, #50834, .F. ) ;
#66133=ADVANCED_FACE ( 'NONE', ( #68814 ), #11469, .F. ) ;
#66138=( LENGTH_UNIT ( ) NAMED_UNIT ( * ) SI_UNIT ( .MILLI., .METRE. ) );
#66157=CARTESIAN_POINT ( 'NONE',  ( 10.02101354018262569, 4.768183399968643599, -8.499583552997725278 ) ) ;
#66164=CARTESIAN_POINT ( 'NONE',  ( 10.89979975933730039, 4.819074589197400726, -7.218192605361100078 ) ) ;
#66166=CARTESIAN_POINT ( 'NONE',  ( 10.98146005378009882, 4.911671201000399556, -7.013182449205100255 ) ) ;
#66167=CARTESIAN_POINT ( 'NONE',  ( 10.06324205624999912, 3.590523439766200031, -8.565862728991998409 ) ) ;
#66175=CARTESIAN_POINT ( 'NONE',  ( 9.986774547327625484, 4.078513067950353843, -6.628582782427464792 ) ) ;
#66186=CARTESIAN_POINT ( 'NONE',  ( 11.60948876160955479, 3.304472173606900043, -8.223320049540498999 ) ) ;
#66207=LINE ( 'NONE', #28126, #37053 ) ;
#66229=DIRECTION ( 'NONE',  ( 1.000000000000000000, 0.000000000000000000, 0.000000000000000000 ) ) ;
#66281=VECTOR ( 'NONE', #34180, 1000.000000000000000 ) ;
#66296=EDGE_CURVE ( 'NONE', #43345, #5638, #39755, .T. ) ;
#66329=CARTESIAN_POINT ( 'NONE',  ( 11.51102763632551884, 3.088851714329700293, -7.079572058049399708 ) ) ;
#66331=CARTESIAN_POINT ( 'NONE',  ( 9.705671671056999017, 3.009461603020800347, -7.666361006367900188 ) ) ;
#66356=DIRECTION ( 'NONE',  ( 0.000000000000000000, -1.000000000000000000, 0.000000000000000000 ) ) ;
#66372=CARTESIAN_POINT ( 'NONE',  ( 11.26212378248529866, 3.384904051819500381, -6.336291382830999908 ) ) ;
#66405=VECTOR ( 'NONE', #49427, 1000.000000000000000 ) ;
#66416=CARTESIAN_POINT ( 'NONE',  ( 10.79303032197930001, 4.663532080728800544, -6.572090902022299730 ) ) ;
#66424=CARTESIAN_POINT ( 'NONE',  ( 10.78887616594230003, 3.613544262574699850, -6.281817606595999415 ) ) ;
#66468=CARTESIAN_POINT ( 'NONE',  ( 9.739763540183334456, 3.672815144550903632, -6.282534154164605589 ) ) ;
#66484=CARTESIAN_POINT ( 'NONE',  ( 10.41891290906799838, 3.190593056227700064, -8.490578012456198920 ) ) ;
#66505=CARTESIAN_POINT ( 'NONE',  ( 10.65364694612719809, 3.195501139158400061, -7.821061011719899980 ) ) ;
#66508=CARTESIAN_POINT ( 'NONE',  ( 9.987254614702999689, 2.893436332050999926, -7.781516069110699263 ) ) ;
#66512=ORIENTED_EDGE ( 'NONE', *, *, #9860, .F. ) ;
#66520=UNCERTAINTY_MEASURE_WITH_UNIT (LENGTH_MEASURE( 1.000000000000000082E-05 ), #11964, 'distance_accuracy_value', 'NONE');
#66530=CARTESIAN_POINT ( 'NONE',  ( 11.51102763632551884, 3.088851714329700293, -7.079572058049399708 ) ) ;
#66538=CARTESIAN_POINT ( 'NONE',  ( 11.47657389914466464, 3.351225026288215947, -8.595592487855949315 ) ) ;
#66591=CARTESIAN_POINT ( 'NONE',  ( 10.33744474310099903, 4.771257858050099721, -7.874284411628199365 ) ) ;
#66619=( NAMED_UNIT ( * ) PLANE_ANGLE_UNIT ( ) SI_UNIT ( $, .RADIAN. ) );
#66675=CARTESIAN_POINT ( 'NONE',  ( 10.25564828895399927, 4.880669054351300495, -7.981013126389099099 ) ) ;
#66678=CARTESIAN_POINT ( 'NONE',  ( 9.199088727410998700, 2.999102593977000186, -7.583944523024719331 ) ) ;
#66685=B_SPLINE_CURVE_WITH_KNOTS ( 'NONE', 3,
 ( #45899, #56392, #29499, #25606 ),
 .UNSPECIFIED., .F., .F.,
 ( 4, 4 ),
 ( 0.000000000000000000, 1.000000000000000000 ),
 .UNSPECIFIED. ) ;
#66698=AXIS2_PLACEMENT_3D ( 'NONE', #6275, #7673, #29358 ) ;
#66765=CARTESIAN_POINT ( 'NONE',  ( 10.13662282008599824, 4.594711216567399781, -8.459250300176799797 ) ) ;
#66772=CARTESIAN_POINT ( 'NONE',  ( 10.83810672858429847, 2.978701842912999886, -6.731711997412900494 ) ) ;
#66830=CARTESIAN_POINT ( 'NONE',  ( 8.962753061708919944, 2.887246877270963186, -7.353476507976682619 ) ) ;
#66833=CARTESIAN_POINT ( 'NONE',  ( 9.380417874594000338, 2.822750429186000165, -8.000467616829000761 ) ) ;
#66852=CARTESIAN_POINT ( 'NONE',  ( 11.14595257254739913, 3.168263696564200149, -7.741895249827200232 ) ) ;
#66854=CARTESIAN_POINT ( 'NONE',  ( 10.57102344389999971, 3.237334151971200225, -7.037150754511299233 ) ) ;
#66855=CARTESIAN_POINT ( 'NONE',  ( 8.923430433046998900, 3.028322657068899915, -6.900352112302299723 ) ) ;
#66898=DIRECTION ( 'NONE',  ( 0.000000000000000000, 1.000000000000000000, 0.000000000000000000 ) ) ;
#66968=CARTESIAN_POINT ( 'NONE',  ( 10.93479632507519916, 4.557787252275099732, -8.534037301706000278 ) ) ;
#66984=CARTESIAN_POINT ( 'NONE',  ( 10.41476354018330852, 2.782534154164605589, -7.827184855449099921 ) ) ;
#67018=CARTESIAN_POINT ( 'NONE',  ( 10.28026357027499849, 4.985299147223100746, -7.690095141806899903 ) ) ;
#67020=CARTESIAN_POINT ( 'NONE',  ( 10.21225461470299933, 3.026595211686900377, -7.747639695388999215 ) ) ;
#67075=CARTESIAN_POINT ( 'NONE',  ( 9.002376473208929752, 3.077871436655787996, -8.207577963560542145 ) ) ;
#67102=EDGE_CURVE ( 'NONE', #19484, #21434, #22145, .T. ) ;
#67103=CARTESIAN_POINT ( 'NONE',  ( 11.30579707368350029, 3.365167912142600137, -6.390809033205999690 ) ) ;
#67110=CARTESIAN_POINT ( 'NONE',  ( 10.44426222744799837, 3.013556901740999994, -8.312555471636301263 ) ) ;
#67114=CARTESIAN_POINT ( 'NONE',  ( 10.16684687351567007, 4.768183399968648040, -6.500416447002280051 ) ) ;
#67129=CARTESIAN_POINT ( 'NONE',  ( 11.58810207955109917, 3.203462856645999945, -7.174999999999999822 ) ) ;
#67140=CARTESIAN_POINT ( 'NONE',  ( 11.06049777433069892, 3.148547701490199913, -7.174999999999999822 ) ) ;
#67144=CARTESIAN_POINT ( 'NONE',  ( 11.23424042080529972, 4.544092497359197402, -6.342116603374311268 ) ) ;
#67152=CARTESIAN_POINT ( 'NONE',  ( 9.760596873516666605, 3.370476274536378547, -6.407767014557177454 ) ) ;
#67170=CARTESIAN_POINT ( 'NONE',  ( 9.456405316140999773, 3.728406863338599830, -8.750048621292000561 ) ) ;
#67183=ADVANCED_FACE ( 'NONE', ( #21252 ), #10757, .T. ) ;
#67189=CARTESIAN_POINT ( 'NONE',  ( 10.48133997687999930, 4.184599793140999502, -6.653701289769800020 ) ) ;
#67191=CARTESIAN_POINT ( 'NONE',  ( 11.15278751119019773, 3.209519379020799867, -7.913556523549700294 ) ) ;
#67192=CARTESIAN_POINT ( 'NONE',  ( 10.13922949779699856, 4.633452903845899584, -8.449985803660998940 ) ) ;
#67306=CARTESIAN_POINT ( 'NONE',  ( 11.27234208742519783, 3.445253572379500362, -8.372004648554700168 ) ) ;
#67322=CARTESIAN_POINT ( 'NONE',  ( 10.43559687351661758, 2.907767014557176566, -8.129523725463622341 ) ) ;
#67342=EDGE_CURVE ( 'NONE', #37649, #48127, #12841, .T. ) ;
#67354=CARTESIAN_POINT ( 'NONE',  ( 11.55610404293055993, 3.497163090439000310, -8.523936114709998790 ) ) ;
#67356=CARTESIAN_POINT ( 'NONE',  ( 9.604355082327998616, 3.550486524676900402, -6.601790705997299114 ) ) ;
#67397=CARTESIAN_POINT ( 'NONE',  ( 11.30367835872029936, 2.886444435522000251, -6.798177532456199934 ) ) ;
#67439=CARTESIAN_POINT ( 'NONE',  ( 10.34580110216399973, 2.909301855364999856, -6.833896451085399448 ) ) ;
#67514=CARTESIAN_POINT ( 'NONE',  ( 9.076468108405999047, 5.230803879475000251, -7.848577323721800170 ) ) ;
#67532=CARTESIAN_POINT ( 'NONE',  ( 11.70794988689359961, 4.455786710255300598, -8.393984925606600811 ) ) ;
#67535=CARTESIAN_POINT ( 'NONE',  ( 9.961925467520998723, 2.860918852493000486, -7.421078600323300023 ) ) ;
#67639=FACE_OUTER_BOUND ( 'NONE', #67917, .T. ) ;
#67645=CARTESIAN_POINT ( 'NONE',  ( 11.68788784977535933, 3.014014167207800465, -7.443657794094239222 ) ) ;
#67684=LINE ( 'NONE', #16620, #64071 ) ;
#67696=CARTESIAN_POINT ( 'NONE',  ( 10.67410807141119911, 4.046361247106100123, -8.502397868920999358 ) ) ;
#67698=CARTESIAN_POINT ( 'NONE',  ( 9.857646554150999663, 4.486270025758400060, -8.378853663802400931 ) ) ;
#67737=CARTESIAN_POINT ( 'NONE',  ( 10.89835090130999973, 4.878966983716200190, -8.043647632228999811 ) ) ;
#67752=CARTESIAN_POINT ( 'NONE',  ( 9.333766445374624965, 2.750000000000000444, -7.340348008080749054 ) ) ;
#67796=CARTESIAN_POINT ( 'NONE',  ( 11.45284386393252696, 4.902679577238613362, -7.175013233162909287 ) ) ;
#67797=CARTESIAN_POINT ( 'NONE',  ( 10.34393020684899867, 2.750000000000000000, -7.500000000000000000 ) ) ;
#67828=EDGE_CURVE ( 'NONE', #22792, #68105, #63175, .T. ) ;
#67874=CARTESIAN_POINT ( 'NONE',  ( 11.23052404082913291, 2.954319127720149041, -7.175009054135016662 ) ) ;
#67878=CARTESIAN_POINT ( 'NONE',  ( 11.06795257254739973, 3.036453385827900142, -7.780229861306499295 ) ) ;
#67882=CARTESIAN_POINT ( 'NONE',  ( 9.503988259786000370, 3.832626376493700082, -8.768215461831999846 ) ) ;
#67912=CARTESIAN_POINT ( 'NONE',  ( 8.969356963619999235, 2.880642974985999860, -7.499999999914821025 ) ) ;
#67917=EDGE_LOOP ( 'NONE', ( #53906, #55447, #26148, #10915, #46376 ) ) ;
#67994=CARTESIAN_POINT ( 'NONE',  ( 11.18412378248529926, 3.450971646934100079, -6.461285588983000316 ) ) ;
#68045=CARTESIAN_POINT ( 'NONE',  ( 10.57564694612699974, 3.068007311611700150, -7.871941502982999772 ) ) ;
#68048=CARTESIAN_POINT ( 'NONE',  ( 10.21024205624999937, 3.689072563647699976, -8.309340504471899536 ) ) ;
#68082=CARTESIAN_POINT ( 'NONE',  ( 11.43345123989529810, 4.540230239159599890, -8.543317325199000223 ) ) ;
#68103=CARTESIAN_POINT ( 'NONE',  ( 11.57240408529958842, 3.267527001822357224, -7.017887023514778555 ) ) ;
#68105=VERTEX_POINT ( 'NONE', #19432 ) ;
#68155=CARTESIAN_POINT ( 'NONE',  ( 11.08810207955139937, 3.203462856645999945, -7.174999999999999822 ) ) ;
#68172=CARTESIAN_POINT ( 'NONE',  ( 11.35565467195930189, 2.863826994586553987, -6.911917091190551865 ) ) ;
#68214=CARTESIAN_POINT ( 'NONE',  ( 10.21462282008599942, 4.523146351753199568, -8.343818446627699004 ) ) ;
#68217=CARTESIAN_POINT ( 'NONE',  ( 8.744113844317999096, 4.323050436788100193, -6.262250912840999106 ) ) ;
#68224=CARTESIAN_POINT ( 'NONE',  ( 11.59999999999999964, 5.386831235742000068, -7.174999999999999822 ) ) ;
#68227=CARTESIAN_POINT ( 'NONE',  ( 8.757986382567201744, 4.151567127026601689, -8.349715092260979077 ) ) ;
#68245=CARTESIAN_POINT ( 'NONE',  ( 11.59999999999999964, 5.250000000000000000, -7.500000000000000000 ) ) ;
#68297=CARTESIAN_POINT ( 'NONE',  ( 10.72191429142990060, 4.025072603369280522, -6.183971186511000084 ) ) ;
#68298=CARTESIAN_POINT ( 'NONE',  ( 10.01660887879199890, 3.803658216258800184, -6.655513263298900029 ) ) ;
#68316=CARTESIAN_POINT ( 'NONE',  ( 8.736413463905998711, 4.084156314540369870, -8.382409559052598880 ) ) ;
#68332=CARTESIAN_POINT ( 'NONE',  ( 11.55811496860034815, 5.045590851977999947, -6.964183526617899744 ) ) ;
#68384=CARTESIAN_POINT ( 'NONE',  ( 11.30579707368350029, 3.365167912142600137, -6.390809033205999690 ) ) ;
#68386=CARTESIAN_POINT ( 'NONE',  ( 10.31155864497999808, 4.682585200569199912, -8.034587760591801242 ) ) ;
#68400=CARTESIAN_POINT ( 'NONE',  ( 9.279336721442293268, 3.836368765436817263, -6.250006800841096499 ) ) ;
#68424=CARTESIAN_POINT ( 'NONE',  ( 11.27234208742519783, 3.445253572379500362, -8.372004648554700168 ) ) ;
#68465=CARTESIAN_POINT ( 'NONE',  ( 10.39503166480599994, 2.725152142215999884, -7.589885038193400213 ) ) ;
#68467=EDGE_CURVE ( 'NONE', #44304, #4423, #21880, .T. ) ;
#68474=CARTESIAN_POINT ( 'NONE',  ( 10.14887885159599890, 5.269014563305000287, -7.348611220446799486 ) ) ;
#68559=CARTESIAN_POINT ( 'NONE',  ( 11.60948876160955479, 3.304472173606900043, -8.223320049540498999 ) ) ;
#68562=CARTESIAN_POINT ( 'NONE',  ( 8.718784697134999817, 4.694174896253500151, -6.425520776924999566 ) ) ;
#68568=CYLINDRICAL_SURFACE ( 'NONE', #16024, 1.250000000000000222 ) ;
#68589=DIRECTION ( 'NONE',  ( -1.000000000000000000, 0.000000000000000000, 0.000000000000000000 ) ) ;
#68616=ORIENTED_EDGE ( 'NONE', *, *, #4429, .T. ) ;
#68644=CARTESIAN_POINT ( 'NONE',  ( 11.71922412107039868, 4.069539071394910223, -6.185573549454999487 ) ) ;
#68645=CARTESIAN_POINT ( 'NONE',  ( 9.560684229509998744, 3.388828644390000200, -6.885038603985500494 ) ) ;
#68680=CARTESIAN_POINT ( 'NONE',  ( 10.37199293566600034, 4.633387186021100668, -8.276990458557699881 ) ) ;
#68683=ORIENTED_EDGE ( 'NONE', *, *, #14666, .F. ) ;
#68732=CARTESIAN_POINT ( 'NONE',  ( 10.13662282008599824, 4.594711216567399781, -8.459250300176799797 ) ) ;
#68736=CARTESIAN_POINT ( 'NONE',  ( 9.045101285863999863, 3.441732526340400167, -6.836640842107200022 ) ) ;
#68770=DIRECTION ( 'NONE',  ( -0.4999999999999719669, 0.6407827956774649891, -0.5825782426110679424 ) ) ;
#68772=CARTESIAN_POINT ( 'NONE',  ( 11.18923293495519822, 2.967327562101000016, -7.458486839450950256 ) ) ;
#68792=CARTESIAN_POINT ( 'NONE',  ( 11.50962052873067520, 3.830320465062102109, -6.639752069194234885 ) ) ;
#68814=FACE_OUTER_BOUND ( 'NONE', #34913, .T. ) ;
#68816=CARTESIAN_POINT ( 'NONE',  ( 10.51810807141099779, 4.059045408506610109, -8.776647962565998995 ) ) ;
#68818=CARTESIAN_POINT ( 'NONE',  ( 11.59999999999999787, 3.125502297258556439, -7.869208573981370414 ) ) ;
#68832=CARTESIAN_POINT ( 'NONE',  ( 11.27769289846838241, 2.954326301843319680, -7.824982657629016458 ) ) ;
#68909=CARTESIAN_POINT ( 'NONE',  ( 10.45257053952200010, 3.605640676136899980, -6.577269499510100204 ) ) ;
#68912=CARTESIAN_POINT ( 'NONE',  ( 9.225367640781000134, 4.603017491986999943, -6.371835875489000323 ) ) ;
#68922=MECHANICAL_DESIGN_GEOMETRIC_PRESENTATION_REPRESENTATION('',(#5250),#14192);
#68971=CARTESIAN_POINT ( 'NONE',  ( 10.89393020684959978, 2.750000000000000000, -7.500000000000000000 ) ) ;
#68975=CARTESIAN_POINT ( 'NONE',  ( 10.22726354018266370, 4.629523725463627670, -6.407767014557179230 ) ) ;
#68996=CARTESIAN_POINT ( 'NONE',  ( 10.51414141025500015, 4.615773412711500434, -8.596754040696000132 ) ) ;
#68997=CARTESIAN_POINT ( 'NONE',  ( 10.04193802597399987, 3.549239910423600097, -6.759376420744099612 ) ) ;
#69002=CARTESIAN_POINT ( 'NONE',  ( 9.810596873515665450, 3.370476274536378103, -6.407767014557176566 ) ) ;
#69020=CARTESIAN_POINT ( 'NONE',  ( 10.85056919669530018, 4.830699382454300306, -7.745432529082900253 ) ) ;
#69023=CARTESIAN_POINT ( 'NONE',  ( 11.59999999999999964, 4.000000000000000000, -7.500000000000000000 ) ) ;
#69026=CARTESIAN_POINT ( 'NONE',  ( 10.09393020684899867, 5.250000000000000000, -7.500000000000000000 ) ) ;
#69085=CARTESIAN_POINT ( 'NONE',  ( 11.35502763632549872, 2.839566963815999934, -6.964545474268299508 ) ) ;
#69088=CARTESIAN_POINT ( 'NONE',  ( 10.03293802597399953, 3.549239910423600097, -6.759376420744099612 ) ) ;
#69094=EDGE_LOOP ( 'NONE', ( #33935, #13804, #10709 ) ) ;
#69111=DIRECTION ( 'NONE',  ( 0.000000000000000000, 1.000000000000000000, 0.000000000000000000 ) ) ;
#69126=CARTESIAN_POINT ( 'NONE',  ( 11.39189666366029918, 3.947847673382490541, -8.673729056199000809 ) ) ;
#69134=CARTESIAN_POINT ( 'NONE',  ( 9.416846873516664829, 3.231816600031355069, -8.499583552997725278 ) ) ;
#69144=CARTESIAN_POINT ( 'NONE',  ( 11.47822875044625945, 4.169680329100683203, -6.639682804525812720 ) ) ;
#69164=CARTESIAN_POINT ( 'NONE',  ( 11.36749010443639918, 4.863785690678500195, -7.564597762509089662 ) ) ;
#69191=CARTESIAN_POINT ( 'NONE',  ( 10.77222057153667656, 4.304280767886410786, -8.319452754344771606 ) ) ;
ENDSEC;
END-ISO-10303-21;
